ISO-10303-21;
HEADER;
FILE_DESCRIPTION (('STEP AP214'),
    '1' );
FILE_NAME ('Main Case.step',
    '2026-10-06T10:59:17',
    ( '' ),
    ( '' ),
    'SwSTEP 2.0',
    'SolidWorks 2026',
    '' );
FILE_SCHEMA (( 'AUTOMOTIVE_DESIGN' ));
ENDSEC;

DATA;
#14=DIRECTION ( 'NONE',  ( -5.084437235940625660E-16, 1.000000000000000000, 0.000000000000000000 ) ) ;
#15=CARTESIAN_POINT ( 'NONE',  ( 13.32277635493562684, 36.96218137147968008, 93.55433879953098142 ) ) ;
#19=CARTESIAN_POINT ( 'NONE',  ( 6.198496396448986090, 45.68315280215533392, 92.83621380123798872 ) ) ;
#22=DIRECTION ( 'NONE',  ( 1.000000000000000000, 1.402518428993831676E-16, 0.000000000000000000 ) ) ;
#25=CARTESIAN_POINT ( 'NONE',  ( 11.22215374030650281, 42.76218137147968434, 61.80715055817104542 ) ) ;
#30=EDGE_CURVE ( 'NONE', #19399, #15803, #16589, .T. ) ;
#31=CARTESIAN_POINT ( 'NONE',  ( -4.567115856812060670, 47.10047254335474065, 90.96121380123797451 ) ) ;
#33=DIRECTION ( 'NONE',  ( -1.000000000000000000, 0.000000000000000000, 0.000000000000000000 ) ) ;
#34=( BOUNDED_CURVE ( )  B_SPLINE_CURVE ( 2, ( #7482, #18864, #675, #2170, #8669, #8881, #884, #11966, #2587, #10382, #10705 ),
 .UNSPECIFIED., .F., .F. ) 
 B_SPLINE_CURVE_WITH_KNOTS ( ( 3, 2, 2, 2, 2, 3 ),
 ( 0.5133705948588321855, 0.5208165094390924121, 0.5468573349110280590, 0.5728981603829637059, 0.5989389858548992418, 0.6196804601785050881 ),
 .UNSPECIFIED. ) 
 CURVE ( )  GEOMETRIC_REPRESENTATION_ITEM ( )  RATIONAL_B_SPLINE_CURVE ( ( 0.9689162004317901644, 0.9782346953885442398, 1.000000000000000000, 0.9238795325112867385, 1.000000000000000000, 0.9238795325112867385, 1.000000000000000000, 0.9238795325112867385, 1.000000000000000000, 0.9393701738211195362, 0.9753234597474376155 ) ) 
 REPRESENTATION_ITEM ( '' )  );
#37=DIRECTION ( 'NONE',  ( 1.000000000000000000, 0.000000000000000000, 0.000000000000000000 ) ) ;
#47=FACE_OUTER_BOUND ( 'NONE', #1899, .T. ) ;
#52=CARTESIAN_POINT ( 'NONE',  ( 11.22215374030650281, 45.56218137147968861, 78.80433879953099563 ) ) ;
#57=VERTEX_POINT ( 'NONE', #8931 ) ;
#61=ORIENTED_EDGE ( 'NONE', *, *, #4152, .T. ) ;
#66=CARTESIAN_POINT ( 'NONE',  ( 11.22215374030649926, 45.56218137147968861, 78.80433879953099563 ) ) ;
#68=CARTESIAN_POINT ( 'NONE',  ( -0.8237052942265477018, 49.18499566818285018, 93.69558879953099506 ) ) ;
#70=ORIENTED_EDGE ( 'NONE', *, *, #17800, .F. ) ;
#73=ORIENTED_EDGE ( 'NONE', *, *, #14534, .T. ) ;
#75=DIRECTION ( 'NONE',  ( 1.334402673828313339E-16, 1.871524341742854397E-32, -1.000000000000000000 ) ) ;
#78=AXIS2_PLACEMENT_3D ( 'NONE', #12417, #15502, #20488 ) ;
#81=VECTOR ( 'NONE', #12886, 999.9999999999998863 ) ;
#90=AXIS2_PLACEMENT_3D ( 'NONE', #13292, #19764, #11704 ) ;
#91=VECTOR ( 'NONE', #3485, 1000.000000000000114 ) ;
#92=CARTESIAN_POINT ( 'NONE',  ( 0.5221537403065010796, 44.16218137147969003, 54.55433879953099563 ) ) ;
#102=CARTESIAN_POINT ( 'NONE',  ( -3.350035803220276609, 49.20851703305431357, 90.72683880123797451 ) ) ;
#115=DIRECTION ( 'NONE',  ( -1.000000000000000000, 0.000000000000000000, 0.000000000000000000 ) ) ;
#117=ORIENTED_EDGE ( 'NONE', *, *, #13949, .F. ) ;
#120=EDGE_CURVE ( 'NONE', #5204, #4614, #20185, .T. ) ;
#122=VERTEX_POINT ( 'NONE', #18600 ) ;
#123=CARTESIAN_POINT ( 'NONE',  ( -3.981178359372548492, 46.76218137147973408, 95.41433880294498238 ) ) ;
#126=EDGE_CURVE ( 'NONE', #1287, #15187, #18942, .T. ) ;
#129=VERTEX_POINT ( 'NONE', #13492 ) ;
#132=CARTESIAN_POINT ( 'NONE',  ( -5.154188915835984375, 42.64120994080404614, 91.11746380123797451 ) ) ;
#133=CARTESIAN_POINT ( 'NONE',  ( -3.350035803220276609, 49.20851703305431357, 94.47683880123798872 ) ) ;
#134=ORIENTED_EDGE ( 'NONE', *, *, #20923, .T. ) ;
#137=CARTESIAN_POINT ( 'NONE',  ( 4.483628625085211539, 47.60909685017714565, 92.55433879953102405 ) ) ;
#138=LINE ( 'NONE', #1946, #11877 ) ;
#142=CARTESIAN_POINT ( 'NONE',  ( 1.514255888186003984, 52.36218137147968577, 83.03825919817350609 ) ) ;
#157=LINE ( 'NONE', #5245, #2424 ) ;
#160=DIRECTION ( 'NONE',  ( 1.193617070626243484E-16, 1.000000000000000000, 0.000000000000000000 ) ) ;
#163=PLANE ( 'NONE',  #17008 ) ;
#166=DIRECTION ( 'NONE',  ( 1.000000000000000000, 0.000000000000000000, 0.000000000000000000 ) ) ;
#172=ORIENTED_EDGE ( 'NONE', *, *, #6800, .T. ) ;
#176=CARTESIAN_POINT ( 'NONE',  ( 2.043125170982144745, 38.48583871533720213, 95.02371380123798872 ) ) ;
#178=EDGE_CURVE ( 'NONE', #3564, #14970, #12223, .T. ) ;
#183=DIRECTION ( 'NONE',  ( -1.000000000000000000, -3.942553354492745503E-16, 0.000000000000000000 ) ) ;
#185=LINE ( 'NONE', #9890, #14702 ) ;
#189=CARTESIAN_POINT ( 'NONE',  ( 2.263363662449282110, 49.77488197367689793, 93.03606768333816035 ) ) ;
#194=DIRECTION ( 'NONE',  ( -0.000000000000000000, -0.000000000000000000, 1.000000000000000000 ) ) ;
#199=DIRECTION ( 'NONE',  ( -0.000000000000000000, -0.000000000000000000, 1.000000000000000000 ) ) ;
#201=CARTESIAN_POINT ( 'NONE',  ( 2.043125170982144745, 38.48583871533720213, 93.77371380123798872 ) ) ;
#210=ORIENTED_EDGE ( 'NONE', *, *, #3657, .F. ) ;
#217=VECTOR ( 'NONE', #7066, 1000.000000000000000 ) ;
#221=CARTESIAN_POINT ( 'NONE',  ( 6.102441102155617969, 43.42752260303680600, 94.86746380294499659 ) ) ;
#223=CARTESIAN_POINT ( 'NONE',  ( 31.22215374030650281, 42.76218137147968434, 78.80433879953099563 ) ) ;
#231=CARTESIAN_POINT ( 'NONE',  ( -4.524181921268124462, 40.28999182795290324, 94.78933880123798872 ) ) ;
#232=ORIENTED_EDGE ( 'NONE', *, *, #11068, .T. ) ;
#234=CARTESIAN_POINT ( 'NONE',  ( 30.92220646078100188, 42.96218137147968008, 57.80715055817105252 ) ) ;
#235=CARTESIAN_POINT ( 'NONE',  ( 5.175615907322522524, 46.72245102501825897, 92.55433879953095300 ) ) ;
#245=AXIS2_PLACEMENT_3D ( 'NONE', #9767, #1571, #19535 ) ;
#250=ORIENTED_EDGE ( 'NONE', *, *, #19232, .F. ) ;
#259=CARTESIAN_POINT ( 'NONE',  ( -0.8237052942265477018, 49.18499566818285018, 93.69558879953099506 ) ) ;
#261=ORIENTED_EDGE ( 'NONE', *, *, #19498, .F. ) ;
#265=VECTOR ( 'NONE', #12060, 1000.000000000000000 ) ;
#269=CARTESIAN_POINT ( 'NONE',  ( 5.025485839985549319, 41.56218137147963887, 93.22683879953099506 ) ) ;
#270=ADVANCED_FACE ( 'NONE', ( #47 ), #9957, .F. ) ;
#273=ORIENTED_EDGE ( 'NONE', *, *, #5878, .F. ) ;
#280=CARTESIAN_POINT ( 'NONE',  ( -1.677846259693499542, 50.36218137147968577, 37.95170767603170248 ) ) ;
#282=DIRECTION ( 'NONE',  ( -1.000000000000000000, 0.000000000000000000, 0.000000000000000000 ) ) ;
#284=ORIENTED_EDGE ( 'NONE', *, *, #126, .T. ) ;
#285=VECTOR ( 'NONE', #15681, 1000.000000000000000 ) ;
#293=CARTESIAN_POINT ( 'NONE',  ( 24.32215374030650068, 44.16218137147968292, 45.55433879953098852 ) ) ;
#295=FACE_OUTER_BOUND ( 'NONE', #12710, .T. ) ;
#297=CARTESIAN_POINT ( 'NONE',  ( -5.784195910403845176, 44.99242805365518194, 93.38308880123807398 ) ) ;
#299=DIRECTION ( 'NONE',  ( 1.000000000000000000, 1.213411507412056509E-16, 0.000000000000000000 ) ) ;
#301=CARTESIAN_POINT ( 'NONE',  ( 6.198496396448986090, 45.68315280215533392, 92.83621380123798872 ) ) ;
#303=CARTESIAN_POINT ( 'NONE',  ( -0.3080929418689875576, 37.85583172076933778, 92.44558880123798872 ) ) ;
#304=ORIENTED_EDGE ( 'NONE', *, *, #20230, .T. ) ;
#312=ORIENTED_EDGE ( 'NONE', *, *, #19961, .F. ) ;
#316=CARTESIAN_POINT ( 'NONE',  ( -1.183761187420877548, 49.81017696809242068, 83.28180655319408743 ) ) ;
#321=AXIS2_PLACEMENT_3D ( 'NONE', #17043, #16440, #10161 ) ;
#323=CARTESIAN_POINT ( 'NONE',  ( 1.352400422481993658, 50.46853102219002096, 91.82058880123801714 ) ) ;
#327=CARTESIAN_POINT ( 'NONE',  ( -0.9988176903691428077, 49.83852402762217082, 95.64871380123798872 ) ) ;
#332=DIRECTION ( 'NONE',  ( 1.000000000000000000, 0.000000000000000000, 0.000000000000000000 ) ) ;
#333=SHAPE_REPRESENTATION ( 'Main Case', ( #18366 ), #20720 ) ;
#334=ORIENTED_EDGE ( 'NONE', *, *, #12574, .F. ) ;
#345=VECTOR ( 'NONE', #5616, 1000.000000000000000 ) ;
#361=CARTESIAN_POINT ( 'NONE',  ( 11.22215374030650281, 42.96218137147968008, 69.40574467885102194 ) ) ;
#366=CARTESIAN_POINT ( 'NONE',  ( -2.077846259693550746, 39.65884927180063357, 91.66433879953099506 ) ) ;
#368=ORIENTED_EDGE ( 'NONE', *, *, #3626, .T. ) ;
#370=ORIENTED_EDGE ( 'NONE', *, *, #9504, .F. ) ;
#371=EDGE_CURVE ( 'NONE', #5117, #5383, #6092, .T. ) ;
#376=CARTESIAN_POINT ( 'NONE',  ( 6.102441102155617969, 43.42752260303680600, 90.80496379953099506 ) ) ;
#396=CARTESIAN_POINT ( 'NONE',  ( 3.460444912181559474, 49.25145096859824889, 94.39871380123798872 ) ) ;
#403=PLANE ( 'NONE',  #16543 ) ;
#412=EDGE_CURVE ( 'NONE', #9111, #1287, #34, .T. ) ;
#413=CARTESIAN_POINT ( 'NONE',  ( -4.567115856812060670, 47.10047254335474065, 90.80496380123797451 ) ) ;
#415=ORIENTED_EDGE ( 'NONE', *, *, #3915, .F. ) ;
#416=EDGE_CURVE ( 'NONE', #16577, #9962, #10597, .T. ) ;
#420=CARTESIAN_POINT ( 'NONE',  ( 33.61275266354798674, 51.36218137147967866, 93.55433879953098142 ) ) ;
#422=CARTESIAN_POINT ( 'NONE',  ( -2.416137431568557314, 39.07291177436112406, 95.02371380123797451 ) ) ;
#426=EDGE_CURVE ( 'NONE', #5140, #16560, #15574, .T. ) ;
#428=CARTESIAN_POINT ( 'NONE',  ( -4.677846259693495767, 44.16218127507053737, 93.01911326394946400 ) ) ;
#432=DIRECTION ( 'NONE',  ( 1.402518428993831676E-16, -1.000000000000000000, 0.000000000000000000 ) ) ;
#434=EDGE_LOOP ( 'NONE', ( #14163, #9298, #3077, #16289 ) ) ;
#436=CARTESIAN_POINT ( 'NONE',  ( -4.534306790193148196, 41.70530359416909505, 95.05433879953095300 ) ) ;
#438=CARTESIAN_POINT ( 'NONE',  ( -2.904223097202481174, 48.62752260303690122, 94.08621380294496817 ) ) ;
#441=CARTESIAN_POINT ( 'NONE',  ( 3.460444912181559474, 49.25145096859824889, 90.64871380123798872 ) ) ;
#443=EDGE_LOOP ( 'NONE', ( #16367, #7411, #15591, #11511, #1746, #13003, #15423, #20043, #7490, #3969, #11002, #891 ) ) ;
#447=CARTESIAN_POINT ( 'NONE',  ( 1.352400422481993658, 50.46853102219002096, 93.07058880123798872 ) ) ;
#450=VECTOR ( 'NONE', #6055, 1000.000000000000000 ) ;
#456=EDGE_LOOP ( 'NONE', ( #20112, #3738, #18199, #18118 ) ) ;
#463=( BOUNDED_CURVE ( )  B_SPLINE_CURVE ( 2, ( #19418, #4838, #6543, #14426, #13049, #9754, #20896, #8256, #17929, #12349, #4236, #4725, #16239, #11144, #19523, #4938, #6229 ),
 .UNSPECIFIED., .F., .F. ) 
 B_SPLINE_CURVE_WITH_KNOTS ( ( 3, 2, 2, 2, 2, 2, 2, 2, 3 ),
 ( 0.3050439912557053046, 0.3124899056634827810, 0.3385307311354293081, 0.3645715566073758906, 0.3906123820793224732, 0.4166532075512690003, 0.4426940330232155274, 0.4687348584951621655, 0.4934532648742180339 ),
 .UNSPECIFIED. ) 
 CURVE ( )  GEOMETRIC_REPRESENTATION_ITEM ( )  RATIONAL_B_SPLINE_CURVE ( ( 0.9689162008635190393, 0.9782346958927412572, 1.000000000000000000, 0.9238795325112867385, 1.000000000000000000, 0.9238795325112867385, 1.000000000000000000, 0.9238795325112867385, 1.000000000000000000, 0.9238795325112867385, 1.000000000000000000, 0.9238795325112867385, 1.000000000000000000, 0.9238795325112867385, 1.000000000000000000, 0.9277451227044731796, 0.9926614285408876803 ) ) 
 REPRESENTATION_ITEM ( '' )  );
#468=VERTEX_POINT ( 'NONE', #12173 ) ;
#470=ADVANCED_FACE ( 'NONE', ( #18651 ), #4070, .F. ) ;
#471=CARTESIAN_POINT ( 'NONE',  ( -0.8237052942265477018, 49.18499566818285018, 94.94558879953099506 ) ) ;
#472=CARTESIAN_POINT ( 'NONE',  ( -2.077846259693550746, 39.65884927180063357, 92.91433879953098085 ) ) ;
#473=ORIENTED_EDGE ( 'NONE', *, *, #4186, .T. ) ;
#479=CARTESIAN_POINT ( 'NONE',  ( 1.868012774839550749, 39.13936707477651566, 91.82058879953099506 ) ) ;
#482=CARTESIAN_POINT ( 'NONE',  ( 1.352400422481993658, 50.46853102219002096, 95.72683880123798872 ) ) ;
#484=CARTESIAN_POINT ( 'NONE',  ( -3.677846259693500652, 44.16218137147969003, 45.55433879953098852 ) ) ;
#491=ORIENTED_EDGE ( 'NONE', *, *, #20174, .T. ) ;
#493=CARTESIAN_POINT ( 'NONE',  ( 11.22215374030650281, 42.76218137147968434, 61.40715055817103263 ) ) ;
#497=DIRECTION ( 'NONE',  ( 0.4999999999999984457, 0.8660254037844394848, -0.000000000000000000 ) ) ;
#499=CARTESIAN_POINT ( 'NONE',  ( -5.154188915835984375, 42.64120994080404614, 94.86746380123797451 ) ) ;
#509=CARTESIAN_POINT ( 'NONE',  ( 2.563360104887116631, 38.63792983641089052, 92.55433879953098142 ) ) ;
#510=DIRECTION ( 'NONE',  ( 1.000000000000000000, 0.000000000000000000, 1.196361017915039239E-16 ) ) ;
#512=CARTESIAN_POINT ( 'NONE',  ( 6.198496396448986090, 45.68315280215533392, 91.58621380123798872 ) ) ;
#513=CARTESIAN_POINT ( 'NONE',  ( 0.5221537403065010796, 44.16218137147969003, 54.55433879953099563 ) ) ;
#519=CARTESIAN_POINT ( 'NONE',  ( 5.611423337425062385, 41.22389019960463230, 94.08621380123797451 ) ) ;
#531=VERTEX_POINT ( 'NONE', #5064 ) ;
#536=CARTESIAN_POINT ( 'NONE',  ( -0.8237052942265477018, 49.18499566818285018, 92.75808880294498238 ) ) ;
#538=CARTESIAN_POINT ( 'NONE',  ( -2.416137431568557314, 39.07291177436112406, 92.36746380123797451 ) ) ;
#539=CARTESIAN_POINT ( 'NONE',  ( 4.394343283833276992, 39.11584570990505938, 91.50808880123798872 ) ) ;
#547=CARTESIAN_POINT ( 'NONE',  ( 2.043125170982144745, 38.48583871533720213, 92.52371380123798872 ) ) ;
#551=VECTOR ( 'NONE', #6158, 1000.000000000000000 ) ;
#560=DIRECTION ( 'NONE',  ( -0.000000000000000000, -0.000000000000000000, 1.000000000000000000 ) ) ;
#570=CARTESIAN_POINT ( 'NONE',  ( 10.77494014480653561, 42.96218137147968008, 65.80574467885102763 ) ) ;
#571=CARTESIAN_POINT ( 'NONE',  ( 5.544968037009670780, 45.50804040601273925, 95.88308879953100927 ) ) ;
#572=CARTESIAN_POINT ( 'NONE',  ( 6.102441102155617969, 43.42752260303680600, 95.80496379953099506 ) ) ;
#575=CARTESIAN_POINT ( 'NONE',  ( 11.22215374030650281, 42.76218137147968434, 57.80715055817105252 ) ) ;
#580=CARTESIAN_POINT ( 'NONE',  ( -2.077846259693550746, 39.65884927180063357, 91.66433879953099506 ) ) ;
#581=ORIENTED_EDGE ( 'NONE', *, *, #5982, .F. ) ;
#583=CARTESIAN_POINT ( 'NONE',  ( 5.544968037009670780, 45.50804040601273925, 90.88308879953099506 ) ) ;
#588=( BOUNDED_SURFACE ( )  B_SPLINE_SURFACE ( 1, 2, ( 
 ( #3661, #10172, #3971, #17175, #10717, #11978, #8994, #15159, #12183, #2503, #571, #8571, #13770, #15058, #8892, #19926, #5354, #4081, #2279, #20142, #2391, #10391, #471, #3869, #15482, #10497, #5574, #10608, #12078, #7054, #13554, #20032, #18454, #18344, #3763, #13454, #16961, #6949, #10282, #11867, #18558, #15268, #15380, #794, #7278, #16759, #20242, #688, #2179, #5791, #893, #5673, #8679, #18661, #17077, #5464, #16860, #7167, #7381, #8778, #13871, #13667, #20352, #12296, #18776, #4191, #19088, #9097, #16001, #7803, #12490, #13984, #14181, #11016, #5996, #6296, #17487, #20466, #20765 ),
 ( #5901, #15801, #1214, #18977, #6199, #14397, #14289, #12398, #1422, #20569, #9208, #18877, #11220, #2601, #2913, #7907, #1000, #20866, #15585, #7494, #4388, #10914, #9315, #17383, #4284, #15695, #9518, #12797, #1114, #7703, #7603, #11116, #12701, #2810, #4694, #19280, #9411, #10811, #20660, #19178, #17277, #3012, #2701, #6094, #14086, #12599, #4496, #15899, #1319, #4592, #17584, #13016, #6609, #19490, #8330, #2233, #14710, #17798, #16314, #19388, #5528, #13116, #16425, #20965, #16206, #8011, #132, #3222, #31, #16816, #6509, #14605, #5119, #8115, #19700, #3321, #14497, #6400, #3537 ) ),
 .UNSPECIFIED., .F., .F., .T. ) 
 B_SPLINE_SURFACE_WITH_KNOTS ( ( 2, 2 ),
 ( 3, 2, 2, 2, 2, 2, 2, 2, 2, 2, 2, 2, 2, 2, 2, 2, 2, 2, 2, 2, 2, 2, 2, 2, 2, 2, 2, 2, 2, 2, 2, 2, 2, 2, 2, 2, 2, 2, 2, 3 ),
 ( 0.000000000000000000, 1.000000000000000000 ),
 ( 0.000000000000000000, 0.02500000000000000139, 0.05000000000000000278, 0.07499999999999999722, 0.1000000000000000056, 0.1250000000000000000, 0.1499999999999999944, 0.1749999999999999889, 0.2000000000000000111, 0.2250000000000000056, 0.2500000000000000000, 0.2750000000000000222, 0.2999999999999999889, 0.3250000000000000111, 0.3499999999999999778, 0.3750000000000000000, 0.4000000000000000222, 0.4249999999999999889, 0.4500000000000000111, 0.4749999999999999778, 0.5000000000000000000, 0.5250000000000000222, 0.5500000000000000444, 0.5749999999999999556, 0.5999999999999999778, 0.6250000000000000000, 0.6500000000000000222, 0.6750000000000000444, 0.6999999999999999556, 0.7249999999999999778, 0.7500000000000000000, 0.7750000000000000222, 0.8000000000000000444, 0.8249999999999999556, 0.8499999999999999778, 0.8750000000000000000, 0.9000000000000000222, 0.9250000000000000444, 0.9499999999999999556, 0.9600310108036838042 ),
 .UNSPECIFIED. ) 
 GEOMETRIC_REPRESENTATION_ITEM ( )  RATIONAL_B_SPLINE_SURFACE ( (
 ( 1.000000000000000000, 0.9238795325112867385, 1.000000000000000000, 0.9238795325112867385, 1.000000000000000000, 0.9238795325112867385, 1.000000000000000000, 0.9238795325112867385, 1.000000000000000000, 0.9238795325112867385, 1.000000000000000000, 0.9238795325112867385, 1.000000000000000000, 0.9238795325112867385, 1.000000000000000000, 0.9238795325112867385, 1.000000000000000000, 0.9238795325112867385, 1.000000000000000000, 0.9238795325112867385, 1.000000000000000000, 0.9238795325112867385, 1.000000000000000000, 0.9238795325112867385, 1.000000000000000000, 0.9238795325112867385, 1.000000000000000000, 0.9238795325112867385, 1.000000000000000000, 0.9238795325112867385, 1.000000000000000000, 0.9238795325112867385, 1.000000000000000000, 0.9238795325112867385, 1.000000000000000000, 0.9238795325112867385, 1.000000000000000000, 0.9238795325112867385, 1.000000000000000000, 0.9238795325112867385, 1.000000000000000000, 0.9238795325112867385, 1.000000000000000000, 0.9238795325112867385, 1.000000000000000000, 0.9238795325112867385, 1.000000000000000000, 0.9238795325112867385, 1.000000000000000000, 0.9238795325112867385, 1.000000000000000000, 0.9238795325112867385, 1.000000000000000000, 0.9238795325112867385, 1.000000000000000000, 0.9238795325112867385, 1.000000000000000000, 0.9238795325112867385, 1.000000000000000000, 0.9238795325112867385, 1.000000000000000000, 0.9238795325112867385, 1.000000000000000000, 0.9238795325112867385, 1.000000000000000000, 0.9238795325112867385, 1.000000000000000000, 0.9238795325112867385, 1.000000000000000000, 0.9238795325112867385, 1.000000000000000000, 0.9238795325112867385, 1.000000000000000000, 0.9238795325112867385, 1.000000000000000000, 0.9238795325112867385, 1.000000000000000000, 0.9694573907295700455, 0.9634246409442903669),
 ( 1.000000000000000000, 0.9238795325112867385, 1.000000000000000000, 0.9238795325112867385, 1.000000000000000000, 0.9238795325112867385, 1.000000000000000000, 0.9238795325112867385, 1.000000000000000000, 0.9238795325112867385, 1.000000000000000000, 0.9238795325112867385, 1.000000000000000000, 0.9238795325112867385, 1.000000000000000000, 0.9238795325112867385, 1.000000000000000000, 0.9238795325112867385, 1.000000000000000000, 0.9238795325112867385, 1.000000000000000000, 0.9238795325112867385, 1.000000000000000000, 0.9238795325112867385, 1.000000000000000000, 0.9238795325112867385, 1.000000000000000000, 0.9238795325112867385, 1.000000000000000000, 0.9238795325112867385, 1.000000000000000000, 0.9238795325112867385, 1.000000000000000000, 0.9238795325112867385, 1.000000000000000000, 0.9238795325112867385, 1.000000000000000000, 0.9238795325112867385, 1.000000000000000000, 0.9238795325112867385, 1.000000000000000000, 0.9238795325112867385, 1.000000000000000000, 0.9238795325112867385, 1.000000000000000000, 0.9238795325112867385, 1.000000000000000000, 0.9238795325112867385, 1.000000000000000000, 0.9238795325112867385, 1.000000000000000000, 0.9238795325112867385, 1.000000000000000000, 0.9238795325112867385, 1.000000000000000000, 0.9238795325112867385, 1.000000000000000000, 0.9238795325112867385, 1.000000000000000000, 0.9238795325112867385, 1.000000000000000000, 0.9238795325112867385, 1.000000000000000000, 0.9238795325112867385, 1.000000000000000000, 0.9238795325112867385, 1.000000000000000000, 0.9238795325112867385, 1.000000000000000000, 0.9238795325112867385, 1.000000000000000000, 0.9238795325112867385, 1.000000000000000000, 0.9238795325112867385, 1.000000000000000000, 0.9238795325112867385, 1.000000000000000000, 0.9694573907295700455, 0.9634246409442903669) ) ) 
 REPRESENTATION_ITEM ( '' )  SURFACE ( )  );
#591=EDGE_CURVE ( 'NONE', #11321, #18929, #15285, .T. ) ;
#599=LINE ( 'NONE', #15297, #5135 ) ;
#608=VECTOR ( 'NONE', #1076, 1000.000000000000000 ) ;
#612=DIRECTION ( 'NONE',  ( -1.000000000000000000, -1.402518428993831676E-16, -1.196361017915039239E-16 ) ) ;
#616=CARTESIAN_POINT ( 'NONE',  ( 1.352400422481993658, 50.46853102219002096, 93.07058880123798872 ) ) ;
#623=DIRECTION ( 'NONE',  ( 5.595882180570345180E-16, -1.000000000000000000, 6.798436021654163964E-32 ) ) ;
#626=CARTESIAN_POINT ( 'NONE',  ( -4.567115856812060670, 47.10047254335474065, 95.96121380123798872 ) ) ;
#627=DIRECTION ( 'NONE',  ( -1.000000000000000000, 0.000000000000000000, 0.000000000000000000 ) ) ;
#629=CARTESIAN_POINT ( 'NONE',  ( 11.22215374030650281, 42.96218137147968008, 69.40574467885102194 ) ) ;
#634=EDGE_CURVE ( 'NONE', #18929, #10043, #16879, .T. ) ;
#638=ORIENTED_EDGE ( 'NONE', *, *, #15893, .T. ) ;
#640=CARTESIAN_POINT ( 'NONE',  ( -1.219056181836355446, 49.77488197367695477, 93.15612966814926210 ) ) ;
#643=CARTESIAN_POINT ( 'NONE',  ( -5.058133621542618030, 44.89684013992257405, 90.49246380294498238 ) ) ;
#648=CARTESIAN_POINT ( 'NONE',  ( 3.460444912181559474, 49.25145096859824889, 92.99246380123798872 ) ) ;
#651=ORIENTED_EDGE ( 'NONE', *, *, #14253, .F. ) ;
#652=EDGE_CURVE ( 'NONE', #1084, #8801, #11683, .T. ) ;
#658=CARTESIAN_POINT ( 'NONE',  ( 4.987494971863720927, 47.58855820898865829, 95.02371380294496817 ) ) ;
#675=CARTESIAN_POINT ( 'NONE',  ( 3.460444912181559474, 49.25145096859824889, 93.14871380123798872 ) ) ;
#681=VECTOR ( 'NONE', #16748, 1000.000000000000000 ) ;
#688=CARTESIAN_POINT ( 'NONE',  ( -0.2125050281363792815, 38.58189400963055959, 92.99246379953098085 ) ) ;
#689=CARTESIAN_POINT ( 'NONE',  ( -2.077846259693550746, 39.65884927180063357, 94.16433879953098085 ) ) ;
#692=CARTESIAN_POINT ( 'NONE',  ( -0.3080929418689875576, 37.85583172076933778, 92.60183880123797451 ) ) ;
#697=DIRECTION ( 'NONE',  ( 1.334402673828313339E-16, 1.871524341742854397E-32, -1.000000000000000000 ) ) ;
#698=CARTESIAN_POINT ( 'NONE',  ( -2.416137431568557314, 39.07291177436112406, 95.02371380123797451 ) ) ;
#703=CARTESIAN_POINT ( 'NONE',  ( 5.568489401881125289, 48.03437091500646261, 91.66433880123796030 ) ) ;
#713=DIRECTION ( 'NONE',  ( -1.402518428993831676E-16, 1.000000000000000000, -1.677918375355662166E-32 ) ) ;
#714=CARTESIAN_POINT ( 'NONE',  ( 5.611423337425062385, 41.22389019960463230, 95.33621380123798872 ) ) ;
#718=DIRECTION ( 'NONE',  ( 1.334402673828313339E-16, 1.871524341742854397E-32, -1.000000000000000000 ) ) ;
#719=( BOUNDED_SURFACE ( )  B_SPLINE_SURFACE ( 1, 2, ( 
 ( #14747, #19313, #8261, #13054, #13154, #16246, #9759, #1781, #14537, #7947, #6756, #17831, #19424, #6436, #8049, #4843, #13263, #9663, #21001, #1878, #18151, #14430, #19735, #9867, #4944, #11569, #8151, #14641, #5154, #3357, #8366, #11362, #19629, #14848, #16458, #12833, #1667, #18044, #68, #3466, #16144, #20900, #4729, #11675, #269, #11466, #3161, #1564, #3260, #19528, #6548, #17936, #9977, #1978, #5473, #12085, #2287, #8471, #10504, #6859, #19836, #5679, #479, #18248, #580, #3979, #8582, #6957, #11989, #18461, #14244, #11080, #9582, #13565, #583, #376, #5476, #8586, #18464 ),
 ( #18569, #5259, #18251, #5682, #15068, #7064, #10295, #482, #3982, #17089, #2402, #8903, #16872, #3671, #15392, #2086, #698, #5584, #6960, #10402, #3879, #12089, #13465, #14956, #11775, #11878, #6864, #7291, #13368, #5364, #20154, #2290, #10184, #20045, #13680, #8789, #13779, #15279, #12192, #18671, #4090, #9325, #7506, #17595, #20776, #10824, #12409, #20479, #1013, #18888, #6212, #2610, #13994, #15909, #11125, #9007, #12712, #2821, #18988, #4508, #1126, #7613, #19190, #17394, #1328, #4297, #14192, #7816, #9421, #5800, #2714, #6106, #9220, #11026, #9109, #15494, #905, #4604, #14301 ) ),
 .UNSPECIFIED., .F., .F., .T. ) 
 B_SPLINE_SURFACE_WITH_KNOTS ( ( 2, 2 ),
 ( 3, 2, 2, 2, 2, 2, 2, 2, 2, 2, 2, 2, 2, 2, 2, 2, 2, 2, 2, 2, 2, 2, 2, 2, 2, 2, 2, 2, 2, 2, 2, 2, 2, 2, 2, 2, 2, 2, 2, 3 ),
 ( 0.000000000000000000, 1.000000000000000000 ),
 ( 0.000000000000000000, 0.02500000000000000139, 0.05000000000000000278, 0.07499999999999999722, 0.1000000000000000056, 0.1250000000000000000, 0.1499999999999999944, 0.1749999999999999889, 0.2000000000000000111, 0.2250000000000000056, 0.2500000000000000000, 0.2750000000000000222, 0.2999999999999999889, 0.3250000000000000111, 0.3499999999999999778, 0.3750000000000000000, 0.4000000000000000222, 0.4249999999999999889, 0.4500000000000000111, 0.4749999999999999778, 0.5000000000000000000, 0.5250000000000000222, 0.5500000000000000444, 0.5749999999999999556, 0.5999999999999999778, 0.6250000000000000000, 0.6500000000000000222, 0.6750000000000000444, 0.6999999999999999556, 0.7249999999999999778, 0.7500000000000000000, 0.7750000000000000222, 0.8000000000000000444, 0.8249999999999999556, 0.8499999999999999778, 0.8750000000000000000, 0.9000000000000000222, 0.9250000000000000444, 0.9499999999999999556, 0.9600310108036838042 ),
 .UNSPECIFIED. ) 
 GEOMETRIC_REPRESENTATION_ITEM ( )  RATIONAL_B_SPLINE_SURFACE ( (
 ( 1.000000000000000000, 0.9238795325112867385, 1.000000000000000000, 0.9238795325112867385, 1.000000000000000000, 0.9238795325112867385, 1.000000000000000000, 0.9238795325112867385, 1.000000000000000000, 0.9238795325112867385, 1.000000000000000000, 0.9238795325112867385, 1.000000000000000000, 0.9238795325112867385, 1.000000000000000000, 0.9238795325112867385, 1.000000000000000000, 0.9238795325112867385, 1.000000000000000000, 0.9238795325112867385, 1.000000000000000000, 0.9238795325112867385, 1.000000000000000000, 0.9238795325112867385, 1.000000000000000000, 0.9238795325112867385, 1.000000000000000000, 0.9238795325112867385, 1.000000000000000000, 0.9238795325112867385, 1.000000000000000000, 0.9238795325112867385, 1.000000000000000000, 0.9238795325112867385, 1.000000000000000000, 0.9238795325112867385, 1.000000000000000000, 0.9238795325112867385, 1.000000000000000000, 0.9238795325112867385, 1.000000000000000000, 0.9238795325112867385, 1.000000000000000000, 0.9238795325112867385, 1.000000000000000000, 0.9238795325112867385, 1.000000000000000000, 0.9238795325112867385, 1.000000000000000000, 0.9238795325112867385, 1.000000000000000000, 0.9238795325112867385, 1.000000000000000000, 0.9238795325112867385, 1.000000000000000000, 0.9238795325112867385, 1.000000000000000000, 0.9238795325112867385, 1.000000000000000000, 0.9238795325112867385, 1.000000000000000000, 0.9238795325112867385, 1.000000000000000000, 0.9238795325112867385, 1.000000000000000000, 0.9238795325112867385, 1.000000000000000000, 0.9238795325112867385, 1.000000000000000000, 0.9238795325112867385, 1.000000000000000000, 0.9238795325112867385, 1.000000000000000000, 0.9238795325112867385, 1.000000000000000000, 0.9238795325112867385, 1.000000000000000000, 0.9694573907295700455, 0.9634246409442903669),
 ( 1.000000000000000000, 0.9238795325112867385, 1.000000000000000000, 0.9238795325112867385, 1.000000000000000000, 0.9238795325112867385, 1.000000000000000000, 0.9238795325112867385, 1.000000000000000000, 0.9238795325112867385, 1.000000000000000000, 0.9238795325112867385, 1.000000000000000000, 0.9238795325112867385, 1.000000000000000000, 0.9238795325112867385, 1.000000000000000000, 0.9238795325112867385, 1.000000000000000000, 0.9238795325112867385, 1.000000000000000000, 0.9238795325112867385, 1.000000000000000000, 0.9238795325112867385, 1.000000000000000000, 0.9238795325112867385, 1.000000000000000000, 0.9238795325112867385, 1.000000000000000000, 0.9238795325112867385, 1.000000000000000000, 0.9238795325112867385, 1.000000000000000000, 0.9238795325112867385, 1.000000000000000000, 0.9238795325112867385, 1.000000000000000000, 0.9238795325112867385, 1.000000000000000000, 0.9238795325112867385, 1.000000000000000000, 0.9238795325112867385, 1.000000000000000000, 0.9238795325112867385, 1.000000000000000000, 0.9238795325112867385, 1.000000000000000000, 0.9238795325112867385, 1.000000000000000000, 0.9238795325112867385, 1.000000000000000000, 0.9238795325112867385, 1.000000000000000000, 0.9238795325112867385, 1.000000000000000000, 0.9238795325112867385, 1.000000000000000000, 0.9238795325112867385, 1.000000000000000000, 0.9238795325112867385, 1.000000000000000000, 0.9238795325112867385, 1.000000000000000000, 0.9238795325112867385, 1.000000000000000000, 0.9238795325112867385, 1.000000000000000000, 0.9238795325112867385, 1.000000000000000000, 0.9238795325112867385, 1.000000000000000000, 0.9238795325112867385, 1.000000000000000000, 0.9238795325112867385, 1.000000000000000000, 0.9238795325112867385, 1.000000000000000000, 0.9694573907295700455, 0.9634246409442903669) ) ) 
 REPRESENTATION_ITEM ( '' )  SURFACE ( )  );
#721=FACE_OUTER_BOUND ( 'NONE', #1347, .T. ) ;
#724=CARTESIAN_POINT ( 'NONE',  ( 5.611423337425062385, 41.22389019960463230, 95.33621380123798872 ) ) ;
#728=CARTESIAN_POINT ( 'NONE',  ( -2.077846259693550746, 39.65884927180063357, 91.97683880294496817 ) ) ;
#729=AXIS2_PLACEMENT_3D ( 'NONE', #13957, #7460, #4047 ) ;
#731=ORIENTED_EDGE ( 'NONE', *, *, #14178, .T. ) ;
#734=LINE ( 'NONE', #16201, #9841 ) ;
#737=CARTESIAN_POINT ( 'NONE',  ( 3.460444912181559474, 49.25145096859824889, 94.39871380123798872 ) ) ;
#742=CARTESIAN_POINT ( 'NONE',  ( 5.722153740306477054, 44.16218185475116798, 93.64411094854725093 ) ) ;
#743=EDGE_LOOP ( 'NONE', ( #1066, #16870, #8896, #16455 ) ) ;
#749=VECTOR ( 'NONE', #20984, 1000.000000000000000 ) ;
#750=CARTESIAN_POINT ( 'NONE',  ( -5.784195910403845176, 44.99242805365518194, 94.78933880123798872 ) ) ;
#753=CARTESIAN_POINT ( 'NONE',  ( 5.025485839985549319, 41.56218137147963887, 92.28933880294496817 ) ) ;
#757=CARTESIAN_POINT ( 'NONE',  ( 3.460444912181559474, 49.25145096859824889, 94.24246380123798872 ) ) ;
#764=ORIENTED_EDGE ( 'NONE', *, *, #13645, .F. ) ;
#765=DIRECTION ( 'NONE',  ( 0.000000000000000000, 0.000000000000000000, -1.000000000000000000 ) ) ;
#766=CARTESIAN_POINT ( 'NONE',  ( -2.416137431568557314, 39.07291177436112406, 91.11746380123798872 ) ) ;
#769=FACE_OUTER_BOUND ( 'NONE', #9422, .T. ) ;
#773=CARTESIAN_POINT ( 'NONE',  ( 10.77494014480653561, 42.76218137147968434, 66.20574467885103331 ) ) ;
#776=ORIENTED_EDGE ( 'NONE', *, *, #7548, .F. ) ;
#780=DIRECTION ( 'NONE',  ( -0.5735764363510442720, 0.8191520442889930198, -9.299032798180124612E-17 ) ) ;
#782=FACE_OUTER_BOUND ( 'NONE', #1025, .T. ) ;
#783=EDGE_CURVE ( 'NONE', #5897, #5621, #16225, .T. ) ;
#788=CARTESIAN_POINT ( 'NONE',  ( 11.22215374030650281, 42.96218137147968008, 57.80715055817105252 ) ) ;
#792=AXIS2_PLACEMENT_3D ( 'NONE', #14982, #5280, #2111 ) ;
#793=DIRECTION ( 'NONE',  ( -0.000000000000000000, -0.000000000000000000, 1.000000000000000000 ) ) ;
#794=CARTESIAN_POINT ( 'NONE',  ( 6.102441102155617969, 43.42752260303680600, 93.30496379953098085 ) ) ;
#796=ORIENTED_EDGE ( 'NONE', *, *, #371, .F. ) ;
#797=CARTESIAN_POINT ( 'NONE',  ( 6.198496396448986090, 45.68315280215533392, 94.24246380123798872 ) ) ;
#801=CARTESIAN_POINT ( 'NONE',  ( -1.677846259693499542, 47.73989013547934945, 45.55433879953098852 ) ) ;
#805=B_SPLINE_CURVE_WITH_KNOTS ( 'NONE', 3,
 ( #15016, #8846, #2143, #7341, #12045, #10458, #13833, #20311, #7014, #436, #6917, #7122, #13421, #16825, #19891, #2243, #4147, #10243, #13514, #13624, #16720, #11937, #18733, #5742, #5311, #19991 ),
 .UNSPECIFIED., .F., .F.,
 ( 4, 2, 2, 2, 2, 2, 2, 2, 2, 2, 2, 2, 4 ),
 ( 0.000000000000000000, 0.001364898262398260478, 0.002047347393597397439, 0.002729796524796534399, 0.004094694787194807888, 0.004777143918393935741, 0.005459593049593063595, 0.006824491311991337517, 0.007506940443190486187, 0.008189389574389634857, 0.008871838705588783527, 0.009554287836787932198, 0.01091918609918624342 ),
 .UNSPECIFIED. ) ;
#808=DIRECTION ( 'NONE',  ( 0.000000000000000000, 0.000000000000000000, 1.000000000000000000 ) ) ;
#818=EDGE_LOOP ( 'NONE', ( #19736, #7395, #18989, #273 ) ) ;
#821=CARTESIAN_POINT ( 'NONE',  ( -0.9988176903691428077, 49.83852402762217082, 92.05496380123798872 ) ) ;
#822=ORIENTED_EDGE ( 'NONE', *, *, #8018, .F. ) ;
#828=CARTESIAN_POINT ( 'NONE',  ( 6.828503391016846891, 43.33193468930419101, 92.75808880123807398 ) ) ;
#836=CARTESIAN_POINT ( 'NONE',  ( 1.868012774839550749, 39.13936707477651566, 92.13308880294498238 ) ) ;
#841=DIRECTION ( 'NONE',  ( 1.000000000000000000, 0.000000000000000000, -0.000000000000000000 ) ) ;
#844=CARTESIAN_POINT ( 'NONE',  ( -3.350035803220276609, 49.20851703305431357, 92.13308880123798872 ) ) ;
#848=EDGE_CURVE ( 'NONE', #7921, #15771, #17815, .T. ) ;
#850=ORIENTED_EDGE ( 'NONE', *, *, #17509, .F. ) ;
#855=DIRECTION ( 'NONE',  ( -1.000000000000000000, -1.402518428993831676E-16, -1.196361017915039239E-16 ) ) ;
#859=CARTESIAN_POINT ( 'NONE',  ( -3.943187491250720544, 40.73580453397070755, 91.89871380294498238 ) ) ;
#860=LINE ( 'NONE', #18737, #17293 ) ;
#869=CARTESIAN_POINT ( 'NONE',  ( 1.256812508749381774, 49.74246873332880625, 95.17996380294498238 ) ) ;
#871=DIRECTION ( 'NONE',  ( -1.000000000000000000, 0.000000000000000000, -1.621236893436268647E-16 ) ) ;
#873=EDGE_CURVE ( 'NONE', #57, #5204, #20786, .T. ) ;
#884=CARTESIAN_POINT ( 'NONE',  ( 5.611423337425062385, 41.22389019960463230, 92.83621380123797451 ) ) ;
#891=ORIENTED_EDGE ( 'NONE', *, *, #5714, .F. ) ;
#893=CARTESIAN_POINT ( 'NONE',  ( -4.500660556396669065, 42.81632233694663370, 92.75808879953098085 ) ) ;
#895=VERTEX_POINT ( 'NONE', #1649 ) ;
#896=CARTESIAN_POINT ( 'NONE',  ( 1.352400422481993658, 50.46853102219002096, 93.22683880123798872 ) ) ;
#899=VERTEX_POINT ( 'NONE', #11241 ) ;
#904=CARTESIAN_POINT ( 'NONE',  ( 11.22215374030650281, 42.76218137147968434, 78.80433879953099563 ) ) ;
#905=CARTESIAN_POINT ( 'NONE',  ( 5.611423337425062385, 41.22389019960463230, 90.33621380123798872 ) ) ;
#916=ORIENTED_EDGE ( 'NONE', *, *, #8534, .T. ) ;
#922=CARTESIAN_POINT ( 'NONE',  ( 5.568489401881125289, 48.03437091500646261, 93.07058880123797451 ) ) ;
#934=CARTESIAN_POINT ( 'NONE',  ( 1.514255888186008425, 52.36218137147968577, 52.53721119516358584 ) ) ;
#935=FACE_OUTER_BOUND ( 'NONE', #5234, .T. ) ;
#939=CARTESIAN_POINT ( 'NONE',  ( 4.987494971863720927, 47.58855820898865829, 93.77371380294498238 ) ) ;
#940=AXIS2_PLACEMENT_3D ( 'NONE', #20181, #13804, #18494 ) ;
#946=DIRECTION ( 'NONE',  ( -0.000000000000000000, -0.000000000000000000, 1.000000000000000000 ) ) ;
#950=AXIS2_PLACEMENT_3D ( 'NONE', #20455, #3858, #5889 ) ;
#959=FACE_OUTER_BOUND ( 'NONE', #20377, .T. ) ;
#964=CARTESIAN_POINT ( 'NONE',  ( -5.058133621542618030, 44.89684013992257405, 92.99246380294498238 ) ) ;
#965=CIRCLE ( 'NONE', #19972, 4.199999999999999289 ) ;
#968=CARTESIAN_POINT ( 'NONE',  ( -4.524181921268124462, 40.28999182795290324, 91.03933880123798872 ) ) ;
#970=VERTEX_POINT ( 'NONE', #12049 ) ;
#972=VERTEX_POINT ( 'NONE', #15550 ) ;
#973=DIRECTION ( 'NONE',  ( 0.000000000000000000, 0.000000000000000000, -1.000000000000000000 ) ) ;
#974=CARTESIAN_POINT ( 'NONE',  ( -5.058133621542618030, 44.89684013992257405, 92.99246380294498238 ) ) ;
#975=ORIENTED_EDGE ( 'NONE', *, *, #16774, .T. ) ;
#979=LINE ( 'NONE', #5557, #2694 ) ;
#980=DIRECTION ( 'NONE',  ( -1.000000000000000000, -1.402518428993831676E-16, -1.196361017915039239E-16 ) ) ;
#994=VECTOR ( 'NONE', #12378, 1000.000000000000000 ) ;
#997=ORIENTED_EDGE ( 'NONE', *, *, #416, .T. ) ;
#1000=CARTESIAN_POINT ( 'NONE',  ( -2.416137431568557314, 39.07291177436112406, 95.02371380123797451 ) ) ;
#1004=CARTESIAN_POINT ( 'NONE',  ( 3.460444912181559474, 49.25145096859824889, 94.39871380123798872 ) ) ;
#1006=CARTESIAN_POINT ( 'NONE',  ( 31.22215374030650281, 45.56218137147968861, 78.80433879953099563 ) ) ;
#1010=EDGE_LOOP ( 'NONE', ( #9860, #18448, #3398, #16229 ) ) ;
#1012=AXIS2_PLACEMENT_3D ( 'NONE', #7652, #20296, #841 ) ;
#1013=CARTESIAN_POINT ( 'NONE',  ( -2.416137431568557314, 39.07291177436112406, 92.52371380123797451 ) ) ;
#1014=EDGE_CURVE ( 'NONE', #1329, #11872, #20433, .T. ) ;
#1018=CARTESIAN_POINT ( 'NONE',  ( 3.788215052820487205, 39.19523464621513398, 90.08681233796825438 ) ) ;
#1025=EDGE_LOOP ( 'NONE', ( #12403, #18407, #14618, #9974 ) ) ;
#1029=EDGE_CURVE ( 'NONE', #18041, #20573, #10931, .T. ) ;
#1032=LINE ( 'NONE', #7521, #4797 ) ;
#1033=CARTESIAN_POINT ( 'NONE',  ( -0.9988176903691428077, 49.83852402762217082, 94.39871380123798872 ) ) ;
#1045=EDGE_CURVE ( 'NONE', #2768, #4997, #19885, .T. ) ;
#1050=CARTESIAN_POINT ( 'NONE',  ( -2.416137431568557314, 39.07291177436112406, 92.52371380123797451 ) ) ;
#1055=CARTESIAN_POINT ( 'NONE',  ( -3.981178359372548492, 46.76218137147973408, 90.41433880294496817 ) ) ;
#1059=VERTEX_POINT ( 'NONE', #3612 ) ;
#1063=CARTESIAN_POINT ( 'NONE',  ( -4.567115856812060670, 47.10047254335474065, 90.96121380123797451 ) ) ;
#1066=ORIENTED_EDGE ( 'NONE', *, *, #3550, .T. ) ;
#1068=CARTESIAN_POINT ( 'NONE',  ( -3.226449543290886179, 47.76606447477297479, 92.55433879953076826 ) ) ;
#1072=DIRECTION ( 'NONE',  ( -0.000000000000000000, -0.000000000000000000, 1.000000000000000000 ) ) ;
#1076=DIRECTION ( 'NONE',  ( -0.000000000000000000, -0.000000000000000000, 1.000000000000000000 ) ) ;
#1081=ORIENTED_EDGE ( 'NONE', *, *, #6899, .F. ) ;
#1084=VERTEX_POINT ( 'NONE', #17022 ) ;
#1087=AXIS2_PLACEMENT_3D ( 'NONE', #9091, #20345, #7269 ) ;
#1089=AXIS2_PLACEMENT_3D ( 'NONE', #10663, #17226, #9366 ) ;
#1090=CARTESIAN_POINT ( 'NONE',  ( 5.025485839985549319, 41.56218137147963887, 93.53933880294496817 ) ) ;
#1095=DIRECTION ( 'NONE',  ( -1.213411507412056509E-16, 1.000000000000000000, 0.000000000000000000 ) ) ;
#1098=ORIENTED_EDGE ( 'NONE', *, *, #14279, .F. ) ;
#1103=CARTESIAN_POINT ( 'NONE',  ( -3.350035803220276609, 49.20851703305431357, 94.47683880123798872 ) ) ;
#1105=CARTESIAN_POINT ( 'NONE',  ( -5.368445182934982185, 36.96218137147968008, 93.55433879953098142 ) ) ;
#1106=VECTOR ( 'NONE', #16880, 1000.000000000000000 ) ;
#1109=VECTOR ( 'NONE', #10561, 1000.000000000000000 ) ;
#1110=ORIENTED_EDGE ( 'NONE', *, *, #11608, .F. ) ;
#1114=CARTESIAN_POINT ( 'NONE',  ( 5.611423337425062385, 41.22389019960463230, 94.08621380123797451 ) ) ;
#1117=CARTESIAN_POINT ( 'NONE',  ( 6.198496396448986090, 45.68315280215533392, 92.99246380123798872 ) ) ;
#1121=EDGE_CURVE ( 'NONE', #20921, #20010, #12537, .T. ) ;
#1125=CARTESIAN_POINT ( 'NONE',  ( 1.868012774839550749, 39.13936707477651566, 93.07058879953099506 ) ) ;
#1126=CARTESIAN_POINT ( 'NONE',  ( 5.611423337425062385, 41.22389019960463230, 91.58621380123798872 ) ) ;
#1134=DIRECTION ( 'NONE',  ( 0.000000000000000000, 0.000000000000000000, 1.000000000000000000 ) ) ;
#1141=CARTESIAN_POINT ( 'NONE',  ( 4.394343283833276992, 39.11584570990505938, 91.50808880123798872 ) ) ;
#1143=ORIENTED_EDGE ( 'NONE', *, *, #16420, .T. ) ;
#1158=CARTESIAN_POINT ( 'NONE',  ( 5.568489401881125289, 48.03437091500646261, 91.82058880123797451 ) ) ;
#1161=CARTESIAN_POINT ( 'NONE',  ( 6.102441102155617969, 43.42752260303680600, 93.61746380294498238 ) ) ;
#1165=( BOUNDED_SURFACE ( )  B_SPLINE_SURFACE ( 1, 2, ( 
 ( #13582, #4001, #5602, #2308, #18482, #3897, #8919, #3793, #13478, #19951, #8804, #10419, #714, #1997, #7195, #18375, #16989, #6975, #499, #3586, #12107, #2420, #10314, #18585, #396, #2203, #15407, #8704, #15184, #5174, #13385, #11694, #19855, #5275, #11790, #18266, #16683, #2107, #8607, #15085, #7729, #922, #7306, #9439, #4524, #19004, #10939, #12423, #5816, #6125, #18902, #7410, #20494, #2527, #821, #10841, #20592, #15723, #13795, #1237, #2935, #1141, #14211, #7522, #11041, #17203, #6020, #13899, #20383, #18690, #12322, #17306, #5701, #20270, #5926, #15614, #12208, #4106, #12628, #10636, #18802 ),
 ( #4314, #4215, #15826, #9340, #2626, #7629, #19112, #20687, #17411, #14110, #12520, #17104, #2732, #14011, #9235, #2836, #4424, #17513, #9023, #15509, #10740, #9127, #1033, #11502, #11941, #11710, #16592, #3397, #5092, #16281, #201, #14781, #10012, #17867, #14995, #6477, #14677, #16177, #8402, #8085, #3290, #16489, #13191, #8512, #1601, #14880, #9796, #303, #11609, #6795, #8299, #1817, #1909, #19561, #12982, #19460, #6685, #16390, #9909, #4982, #19665, #4875, #18084, #3503, #11397, #13300, #19773, #5192, #18185, #102, #3602, #8187, #10110, #2013, #6582, #13087, #16226, #1650, #3243, #17918, #3340 ) ),
 .UNSPECIFIED., .F., .F., .F. ) 
 B_SPLINE_SURFACE_WITH_KNOTS ( ( 2, 2 ),
 ( 3, 2, 2, 2, 2, 2, 2, 2, 2, 2, 2, 2, 2, 2, 2, 2, 2, 2, 2, 2, 2, 2, 2, 2, 2, 2, 2, 2, 2, 2, 2, 2, 2, 2, 2, 2, 2, 2, 2, 2, 3 ),
 ( 0.000000000000000000, 1.000000000000000000 ),
 ( 0.000000000000000000, 0.02500000000000000139, 0.05000000000000000278, 0.07499999999999999722, 0.1000000000000000056, 0.1250000000000000000, 0.1499999999999999944, 0.1749999999999999889, 0.2000000000000000111, 0.2250000000000000056, 0.2500000000000000000, 0.2750000000000000222, 0.2999999999999999889, 0.3250000000000000111, 0.3499999999999999778, 0.3750000000000000000, 0.4000000000000000222, 0.4249999999999999889, 0.4500000000000000111, 0.4749999999999999778, 0.5000000000000000000, 0.5250000000000000222, 0.5500000000000000444, 0.5749999999999999556, 0.5999999999999999778, 0.6250000000000000000, 0.6500000000000000222, 0.6750000000000000444, 0.6999999999999999556, 0.7249999999999999778, 0.7500000000000000000, 0.7750000000000000222, 0.8000000000000000444, 0.8249999999999999556, 0.8499999999999999778, 0.8750000000000000000, 0.9000000000000000222, 0.9250000000000000444, 0.9499999999999999556, 0.9600309411673831894, 0.9696312505790569691 ),
 .UNSPECIFIED. ) 
 GEOMETRIC_REPRESENTATION_ITEM ( )  RATIONAL_B_SPLINE_SURFACE ( (
 ( 1.000000000000000000, 0.9238795325112867385, 1.000000000000000000, 0.9238795325112867385, 1.000000000000000000, 0.9238795325112867385, 1.000000000000000000, 0.9238795325112867385, 1.000000000000000000, 0.9238795325112867385, 1.000000000000000000, 0.9238795325112867385, 1.000000000000000000, 0.9238795325112867385, 1.000000000000000000, 0.9238795325112867385, 1.000000000000000000, 0.9238795325112867385, 1.000000000000000000, 0.9238795325112867385, 1.000000000000000000, 0.9238795325112867385, 1.000000000000000000, 0.9238795325112867385, 1.000000000000000000, 0.9238795325112867385, 1.000000000000000000, 0.9238795325112867385, 1.000000000000000000, 0.9238795325112867385, 1.000000000000000000, 0.9238795325112867385, 1.000000000000000000, 0.9238795325112867385, 1.000000000000000000, 0.9238795325112867385, 1.000000000000000000, 0.9238795325112867385, 1.000000000000000000, 0.9238795325112867385, 1.000000000000000000, 0.9238795325112867385, 1.000000000000000000, 0.9238795325112867385, 1.000000000000000000, 0.9238795325112867385, 1.000000000000000000, 0.9238795325112867385, 1.000000000000000000, 0.9238795325112867385, 1.000000000000000000, 0.9238795325112867385, 1.000000000000000000, 0.9238795325112867385, 1.000000000000000000, 0.9238795325112867385, 1.000000000000000000, 0.9238795325112867385, 1.000000000000000000, 0.9238795325112867385, 1.000000000000000000, 0.9238795325112867385, 1.000000000000000000, 0.9238795325112867385, 1.000000000000000000, 0.9238795325112867385, 1.000000000000000000, 0.9238795325112867385, 1.000000000000000000, 0.9238795325112867385, 1.000000000000000000, 0.9238795325112867385, 1.000000000000000000, 0.9238795325112867385, 1.000000000000000000, 0.9238795325112867385, 1.000000000000000000, 0.9694576027594803413, 0.9634247247054007479, 0.9634247247054007479, 0.9634247247054007479),
 ( 1.000000000000000000, 0.9238795325112867385, 1.000000000000000000, 0.9238795325112867385, 1.000000000000000000, 0.9238795325112867385, 1.000000000000000000, 0.9238795325112867385, 1.000000000000000000, 0.9238795325112867385, 1.000000000000000000, 0.9238795325112867385, 1.000000000000000000, 0.9238795325112867385, 1.000000000000000000, 0.9238795325112867385, 1.000000000000000000, 0.9238795325112867385, 1.000000000000000000, 0.9238795325112867385, 1.000000000000000000, 0.9238795325112867385, 1.000000000000000000, 0.9238795325112867385, 1.000000000000000000, 0.9238795325112867385, 1.000000000000000000, 0.9238795325112867385, 1.000000000000000000, 0.9238795325112867385, 1.000000000000000000, 0.9238795325112867385, 1.000000000000000000, 0.9238795325112867385, 1.000000000000000000, 0.9238795325112867385, 1.000000000000000000, 0.9238795325112867385, 1.000000000000000000, 0.9238795325112867385, 1.000000000000000000, 0.9238795325112867385, 1.000000000000000000, 0.9238795325112867385, 1.000000000000000000, 0.9238795325112867385, 1.000000000000000000, 0.9238795325112867385, 1.000000000000000000, 0.9238795325112867385, 1.000000000000000000, 0.9238795325112867385, 1.000000000000000000, 0.9238795325112867385, 1.000000000000000000, 0.9238795325112867385, 1.000000000000000000, 0.9238795325112867385, 1.000000000000000000, 0.9238795325112867385, 1.000000000000000000, 0.9238795325112867385, 1.000000000000000000, 0.9238795325112867385, 1.000000000000000000, 0.9238795325112867385, 1.000000000000000000, 0.9238795325112867385, 1.000000000000000000, 0.9238795325112867385, 1.000000000000000000, 0.9238795325112867385, 1.000000000000000000, 0.9238795325112867385, 1.000000000000000000, 0.9238795325112867385, 1.000000000000000000, 0.9694576027594803413, 0.9634247247054007479, 0.9634247247054007479, 0.9634247247054007479) ) ) 
 REPRESENTATION_ITEM ( '' )  SURFACE ( )  );
#1167=AXIS2_PLACEMENT_3D ( 'NONE', #223, #8004, #1838 ) ;
#1168=PLANE ( 'NONE',  #1012 ) ;
#1172=CARTESIAN_POINT ( 'NONE',  ( 5.184346195580738836, 46.85389944054460898, 94.68362681315549878 ) ) ;
#1179=CARTESIAN_POINT ( 'NONE',  ( 0.5221537403065097394, 44.16218137147969003, 92.55433879953098142 ) ) ;
#1181=LINE ( 'NONE', #17652, #14883 ) ;
#1182=CARTESIAN_POINT ( 'NONE',  ( 6.198496396448986090, 45.68315280215533392, 92.83621380123798872 ) ) ;
#1183=CARTESIAN_POINT ( 'NONE',  ( -3.350035803220276609, 49.20851703305431357, 90.72683880123797451 ) ) ;
#1190=CARTESIAN_POINT ( 'NONE',  ( -10.17784625969349754, 36.96218137147968008, 80.55433879953099563 ) ) ;
#1192=CARTESIAN_POINT ( 'NONE',  ( 1.868012774839550749, 39.13936707477651566, 93.38308880294498238 ) ) ;
#1193=ORIENTED_EDGE ( 'NONE', *, *, #18475, .F. ) ;
#1197=CYLINDRICAL_SURFACE ( 'NONE', #14231, 5.199999999999999289 ) ;
#1198=LINE ( 'NONE', #16086, #19909 ) ;
#1199=FACE_BOUND ( 'NONE', #14600, .T. ) ;
#1203=VERTEX_POINT ( 'NONE', #17616 ) ;
#1204=CARTESIAN_POINT ( 'NONE',  ( -0.9988176903691428077, 49.83852402762217082, 95.64871380123798872 ) ) ;
#1205=CARTESIAN_POINT ( 'NONE',  ( 11.22215374030650281, 42.76218137147968434, 64.80574467885102763 ) ) ;
#1206=CARTESIAN_POINT ( 'NONE',  ( 11.22215374030650281, 42.96218137147968008, 74.20433879953100131 ) ) ;
#1214=CARTESIAN_POINT ( 'NONE',  ( -5.154188915835984375, 42.64120994080404614, 96.11746380123797451 ) ) ;
#1234=ORIENTED_EDGE ( 'NONE', *, *, #3605, .T. ) ;
#1237=CARTESIAN_POINT ( 'NONE',  ( 6.828503391016846891, 43.33193468930419101, 91.66433880123796030 ) ) ;
#1240=ORIENTED_EDGE ( 'NONE', *, *, #783, .F. ) ;
#1244=ORIENTED_EDGE ( 'NONE', *, *, #18450, .F. ) ;
#1253=CARTESIAN_POINT ( 'NONE',  ( 6.828503391016846891, 43.33193468930419101, 90.41433880123798872 ) ) ;
#1264=PLANE ( 'NONE',  #1089 ) ;
#1265=ORIENTED_EDGE ( 'NONE', *, *, #7512, .T. ) ;
#1278=DIRECTION ( 'NONE',  ( -1.000000000000000000, 1.193617070626243484E-16, 0.000000000000000000 ) ) ;
#1281=CARTESIAN_POINT ( 'NONE',  ( -2.416137431568557314, 39.07291177436112406, 92.36746380123797451 ) ) ;
#1287=VERTEX_POINT ( 'NONE', #18043 ) ;
#1290=CARTESIAN_POINT ( 'NONE',  ( -0.2125050281363792815, 38.58189400963055959, 93.30496380294501080 ) ) ;
#1293=CARTESIAN_POINT ( 'NONE',  ( -4.500660556396669065, 42.81632233694663370, 94.00808879953098085 ) ) ;
#1295=DIRECTION ( 'NONE',  ( 1.000000000000000000, 0.000000000000000000, 0.000000000000000000 ) ) ;
#1299=ORIENTED_EDGE ( 'NONE', *, *, #11045, .F. ) ;
#1302=EDGE_CURVE ( 'NONE', #11635, #15007, #5361, .T. ) ;
#1305=EDGE_CURVE ( 'NONE', #12967, #3115, #17935, .T. ) ;
#1310=B_SPLINE_CURVE_WITH_KNOTS ( 'NONE', 3,
 ( #11866, #18343, #5039, #18033, #3456, #9967 ),
 .UNSPECIFIED., .F., .F.,
 ( 4, 2, 4 ),
 ( 0.000000000000000000, 0.001391361808504451786, 0.002782723617008903572 ),
 .UNSPECIFIED. ) ;
#1313=EDGE_CURVE ( 'NONE', #10052, #4005, #8365, .T. ) ;
#1319=CARTESIAN_POINT ( 'NONE',  ( -2.416137431568557314, 39.07291177436112406, 92.52371380123797451 ) ) ;
#1326=EDGE_LOOP ( 'NONE', ( #5467, #17768, #6729, #1865 ) ) ;
#1327=DIRECTION ( 'NONE',  ( -1.402518428993831676E-16, 1.000000000000000000, 0.000000000000000000 ) ) ;
#1328=CARTESIAN_POINT ( 'NONE',  ( -2.416137431568557314, 39.07291177436112406, 91.27371380123798872 ) ) ;
#1329=VERTEX_POINT ( 'NONE', #1780 ) ;
#1337=EDGE_CURVE ( 'NONE', #16241, #9835, #19835, .T. ) ;
#1342=ORIENTED_EDGE ( 'NONE', *, *, #19961, .T. ) ;
#1343=CARTESIAN_POINT ( 'NONE',  ( 11.22215374030650281, 42.96218137147968008, 57.80715055817105252 ) ) ;
#1347=EDGE_LOOP ( 'NONE', ( #6464, #10404, #6947, #17473 ) ) ;
#1362=CARTESIAN_POINT ( 'NONE',  ( 11.22215374030649926, 42.76218137147968434, 80.55433879953099563 ) ) ;
#1364=CARTESIAN_POINT ( 'NONE',  ( 5.611423337425062385, 41.22389019960463230, 90.33621380123798872 ) ) ;
#1365=CARTESIAN_POINT ( 'NONE',  ( 5.025485839985549319, 41.56218137147963887, 89.78933880294498238 ) ) ;
#1367=VECTOR ( 'NONE', #14316, 1000.000000000000000 ) ;
#1382=CARTESIAN_POINT ( 'NONE',  ( 11.22215374030650281, 42.96218137147968008, 65.80574467885102763 ) ) ;
#1387=VERTEX_POINT ( 'NONE', #2510 ) ;
#1394=DIRECTION ( 'NONE',  ( 1.193617070626243484E-16, 1.000000000000000000, 0.000000000000000000 ) ) ;
#1395=CARTESIAN_POINT ( 'NONE',  ( -5.058133621542618030, 44.89684013992257405, 91.74246380294499659 ) ) ;
#1400=LINE ( 'NONE', #19165, #81 ) ;
#1406=ORIENTED_EDGE ( 'NONE', *, *, #4152, .F. ) ;
#1407=DIRECTION ( 'NONE',  ( -4.818676322157797375E-16, -1.000000000000000000, 0.000000000000000000 ) ) ;
#1409=CARTESIAN_POINT ( 'NONE',  ( 28.52215374030649997, 44.16218137147968292, 93.55433879953098142 ) ) ;
#1418=EDGE_CURVE ( 'NONE', #5621, #11839, #2399, .T. ) ;
#1422=CARTESIAN_POINT ( 'NONE',  ( 3.460444912181559474, 49.25145096859824889, 95.64871380123798872 ) ) ;
#1423=CARTESIAN_POINT ( 'NONE',  ( -1.677846259693499542, 44.16218137147969003, 37.95170767603170248 ) ) ;
#1426=CARTESIAN_POINT ( 'NONE',  ( 11.22215374030649926, 42.76218137147968434, 80.55433879953099563 ) ) ;
#1432=CARTESIAN_POINT ( 'NONE',  ( -3.857944742499960888, 47.10944688436405414, 92.55433879953096721 ) ) ;
#1447=ADVANCED_FACE ( 'NONE', ( #9106 ), #20249, .F. ) ;
#1452=DIRECTION ( 'NONE',  ( -0.7071067811865434649, -0.7071067811865515695, 0.000000000000000000 ) ) ;
#1458=ORIENTED_EDGE ( 'NONE', *, *, #3170, .T. ) ;
#1463=ORIENTED_EDGE ( 'NONE', *, *, #14279, .T. ) ;
#1465=FACE_OUTER_BOUND ( 'NONE', #443, .T. ) ;
#1472=CARTESIAN_POINT ( 'NONE',  ( -3.350035803220276609, 49.20851703305431357, 93.38308880123798872 ) ) ;
#1479=VERTEX_POINT ( 'NONE', #8685 ) ;
#1480=FACE_OUTER_BOUND ( 'NONE', #2363, .T. ) ;
#1489=LINE ( 'NONE', #9580, #3300 ) ;
#1492=CARTESIAN_POINT ( 'NONE',  ( 2.891178777371211428, 49.58011692477155208, 94.26356103946022813 ) ) ;
#1515=CARTESIAN_POINT ( 'NONE',  ( -4.524181921268124462, 40.28999182795290324, 96.03933880123798872 ) ) ;
#1517=CARTESIAN_POINT ( 'NONE',  ( -4.567115856812060670, 47.10047254335474065, 92.05496380123798872 ) ) ;
#1526=EDGE_CURVE ( 'NONE', #2157, #1583, #5812, .T. ) ;
#1532=CARTESIAN_POINT ( 'NONE',  ( 5.956414982595287455, 44.61570594562444114, 92.55433879953099563 ) ) ;
#1535=ORIENTED_EDGE ( 'NONE', *, *, #12438, .T. ) ;
#1556=CARTESIAN_POINT ( 'NONE',  ( -2.077846259693550746, 39.65884927180063357, 96.66433879953098085 ) ) ;
#1564=CARTESIAN_POINT ( 'NONE',  ( -0.2125050281363792815, 38.58189400963055959, 92.99246379953098085 ) ) ;
#1569=ORIENTED_EDGE ( 'NONE', *, *, #4396, .T. ) ;
#1571=DIRECTION ( 'NONE',  ( 0.000000000000000000, 0.000000000000000000, 1.000000000000000000 ) ) ;
#1575=CARTESIAN_POINT ( 'NONE',  ( 3.460444912181559474, 49.25145096859824889, 92.99246380123798872 ) ) ;
#1582=DIRECTION ( 'NONE',  ( -1.196361017915039239E-16, 0.000000000000000000, 1.000000000000000000 ) ) ;
#1583=VERTEX_POINT ( 'NONE', #16526 ) ;
#1590=AXIS2_PLACEMENT_3D ( 'NONE', #92, #11283, #19552 ) ;
#1595=FACE_OUTER_BOUND ( 'NONE', #19586, .T. ) ;
#1596=CARTESIAN_POINT ( 'NONE',  ( 3.460444912181559474, 49.25145096859824889, 94.24246380123807398 ) ) ;
#1601=CARTESIAN_POINT ( 'NONE',  ( 5.611423337425062385, 41.22389019960463230, 92.67996380123798872 ) ) ;
#1602=ORIENTED_EDGE ( 'NONE', *, *, #15630, .T. ) ;
#1603=EDGE_CURVE ( 'NONE', #11193, #1479, #19597, .T. ) ;
#1611=VECTOR ( 'NONE', #20422, 1000.000000000000000 ) ;
#1614=DIRECTION ( 'NONE',  ( -0.000000000000000000, 0.000000000000000000, 1.000000000000000000 ) ) ;
#1617=CARTESIAN_POINT ( 'NONE',  ( 11.22215374030650281, 42.76218137147968434, 58.20715055817105110 ) ) ;
#1619=CARTESIAN_POINT ( 'NONE',  ( 6.828503391016846891, 43.33193468930419101, 90.25808880123800293 ) ) ;
#1631=CARTESIAN_POINT ( 'NONE',  ( -4.524181921268124462, 40.28999182795290324, 96.03933880123798872 ) ) ;
#1633=EDGE_CURVE ( 'NONE', #10210, #11635, #138, .T. ) ;
#1637=CARTESIAN_POINT ( 'NONE',  ( 4.786818451252839779, 47.27669862923430344, 92.55433879953093879 ) ) ;
#1643=ORIENTED_EDGE ( 'NONE', *, *, #634, .T. ) ;
#1645=DIRECTION ( 'NONE',  ( 0.000000000000000000, 0.000000000000000000, 1.000000000000000000 ) ) ;
#1648=CARTESIAN_POINT ( 'NONE',  ( -7.677846259693480668, 36.96218137147968008, 50.15433879953098995 ) ) ;
#1649=CARTESIAN_POINT ( 'NONE',  ( 11.22215374030650281, 42.76218137147968434, 78.80433879953099563 ) ) ;
#1650=CARTESIAN_POINT ( 'NONE',  ( 5.146043734657006041, 40.41782908280415398, 90.15009084312077903 ) ) ;
#1653=ORIENTED_EDGE ( 'NONE', *, *, #6778, .T. ) ;
#1655=EDGE_LOOP ( 'NONE', ( #2425, #7689, #3789, #6402 ) ) ;
#1661=VERTEX_POINT ( 'NONE', #3639 ) ;
#1664=ORIENTED_EDGE ( 'NONE', *, *, #2095, .T. ) ;
#1665=DIRECTION ( 'NONE',  ( 0.000000000000000000, 0.000000000000000000, -1.000000000000000000 ) ) ;
#1667=CARTESIAN_POINT ( 'NONE',  ( -3.981178359372548492, 46.76218137147973408, 93.85183879953099506 ) ) ;
#1677=CARTESIAN_POINT ( 'NONE',  ( 5.568489401881125289, 48.03437091500646261, 94.16433880123797451 ) ) ;
#1678=( LENGTH_UNIT ( ) NAMED_UNIT ( * ) SI_UNIT ( .MILLI., .METRE. ) );
#1683=CARTESIAN_POINT ( 'NONE',  ( -7.677846259693481556, 40.96218137147969429, 95.05433879953098142 ) ) ;
#1684=VECTOR ( 'NONE', #4285, 1000.000000000000000 ) ;
#1687=CARTESIAN_POINT ( 'NONE',  ( -4.477846259693498254, 37.66218137147969713, 53.35433879953099989 ) ) ;
#1688=CARTESIAN_POINT ( 'NONE',  ( 0.5221537403065020788, 52.36218137147968577, 83.03825919817350609 ) ) ;
#1693=EDGE_CURVE ( 'NONE', #10499, #8207, #11747, .T. ) ;
#1714=DIRECTION ( 'NONE',  ( -1.000000000000000000, 0.000000000000000000, 0.000000000000000000 ) ) ;
#1718=EDGE_CURVE ( 'NONE', #10129, #2084, #3229, .T. ) ;
#1724=CARTESIAN_POINT ( 'NONE',  ( 11.22215374030650281, 42.96218137147968008, 73.80433879953100984 ) ) ;
#1733=CARTESIAN_POINT ( 'NONE',  ( 1.352400422481993658, 50.46853102219002096, 90.57058880123798872 ) ) ;
#1740=ORIENTED_EDGE ( 'NONE', *, *, #8730, .T. ) ;
#1746=ORIENTED_EDGE ( 'NONE', *, *, #3507, .T. ) ;
#1750=CARTESIAN_POINT ( 'NONE',  ( 13.32277635493561974, 51.36218137147968577, 93.55433879953098142 ) ) ;
#1751=EDGE_CURVE ( 'NONE', #5897, #13415, #979, .T. ) ;
#1753=ORIENTED_EDGE ( 'NONE', *, *, #9653, .F. ) ;
#1755=CYLINDRICAL_SURFACE ( 'NONE', #5195, 0.9921021478795063464 ) ;
#1758=DIRECTION ( 'NONE',  ( -1.000000000000000000, 4.956352788505161887E-15, 0.000000000000000000 ) ) ;
#1766=ORIENTED_EDGE ( 'NONE', *, *, #19143, .F. ) ;
#1767=CARTESIAN_POINT ( 'NONE',  ( 8.722153740306486824, 36.96218137147968008, 95.05433879953098142 ) ) ;
#1771=EDGE_CURVE ( 'NONE', #19569, #13327, #8659, .T. ) ;
#1772=CARTESIAN_POINT ( 'NONE',  ( 11.22215374030649926, 51.36218137147968577, 80.55433879953099563 ) ) ;
#1773=CARTESIAN_POINT ( 'NONE',  ( -4.677846259693497544, 44.16218137147969003, 77.84651775085080772 ) ) ;
#1779=DIRECTION ( 'NONE',  ( 0.000000000000000000, 0.000000000000000000, -1.000000000000000000 ) ) ;
#1780=CARTESIAN_POINT ( 'NONE',  ( 31.22215374030650281, 42.76218137147968434, 72.80433879953100984 ) ) ;
#1781=CARTESIAN_POINT ( 'NONE',  ( 1.256812508749381774, 49.74246873332880625, 96.11746379953099506 ) ) ;
#1782=ORIENTED_EDGE ( 'NONE', *, *, #20369, .T. ) ;
#1787=CARTESIAN_POINT ( 'NONE',  ( 35.92215374030650565, 51.36218137147967866, 92.39963826115175038 ) ) ;
#1790=CARTESIAN_POINT ( 'NONE',  ( -4.567115856812060670, 47.10047254335474065, 94.55496380123798872 ) ) ;
#1793=VECTOR ( 'NONE', #11391, 1000.000000000000000 ) ;
#1801=LINE ( 'NONE', #14865, #91 ) ;
#1802=ORIENTED_EDGE ( 'NONE', *, *, #14580, .T. ) ;
#1804=PLANE ( 'NONE',  #15413 ) ;
#1805=ORIENTED_EDGE ( 'NONE', *, *, #19154, .F. ) ;
#1806=VECTOR ( 'NONE', #13020, 1000.000000000000000 ) ;
#1808=DIRECTION ( 'NONE',  ( 0.8660254037844399289, 0.4999999999999977796, 0.000000000000000000 ) ) ;
#1811=CYLINDRICAL_SURFACE ( 'NONE', #13006, 5.199999999999999289 ) ;
#1813=CARTESIAN_POINT ( 'NONE',  ( 2.263363662449209279, 49.77488197367684819, 94.28606768333811772 ) ) ;
#1814=CARTESIAN_POINT ( 'NONE',  ( -7.677846259693480668, 38.96218137147968008, 93.55433879953098142 ) ) ;
#1817=CARTESIAN_POINT ( 'NONE',  ( -5.784195910403845176, 44.99242805365518194, 92.13308880123798872 ) ) ;
#1835=CARTESIAN_POINT ( 'NONE',  ( 6.198496396448986090, 45.68315280215533392, 90.33621380123798872 ) ) ;
#1836=EDGE_CURVE ( 'NONE', #15570, #468, #4368, .T. ) ;
#1838=DIRECTION ( 'NONE',  ( 1.000000000000000000, 1.402518428993831676E-16, 0.000000000000000000 ) ) ;
#1839=ADVANCED_FACE ( 'NONE', ( #14066 ), #1197, .F. ) ;
#1840=DIRECTION ( 'NONE',  ( 0.000000000000000000, 0.000000000000000000, -1.000000000000000000 ) ) ;
#1841=VERTEX_POINT ( 'NONE', #4575 ) ;
#1847=CARTESIAN_POINT ( 'NONE',  ( -5.784195910403845176, 44.99242805365518194, 95.88308880123798872 ) ) ;
#1849=ORIENTED_EDGE ( 'NONE', *, *, #6078, .T. ) ;
#1865=ORIENTED_EDGE ( 'NONE', *, *, #2067, .T. ) ;
#1869=CARTESIAN_POINT ( 'NONE',  ( 31.22215374030650281, 42.96218137147968008, 73.80433879953100984 ) ) ;
#1871=CARTESIAN_POINT ( 'NONE',  ( 3.948530577815480225, 39.69684013992245752, 95.64871379953100927 ) ) ;
#1873=CARTESIAN_POINT ( 'NONE',  ( -4.524181921268124462, 40.28999182795290324, 96.19558880123798872 ) ) ;
#1878=CARTESIAN_POINT ( 'NONE',  ( -5.058133621542618030, 44.89684013992257405, 95.17996379953099506 ) ) ;
#1880=DIRECTION ( 'NONE',  ( -0.000000000000000000, -0.000000000000000000, 1.000000000000000000 ) ) ;
#1884=CARTESIAN_POINT ( 'NONE',  ( 2.263363662449209279, 49.77488197367684819, 94.28606768333811772 ) ) ;
#1885=CARTESIAN_POINT ( 'NONE',  ( 4.394343283833276992, 39.11584570990505938, 93.85183880123797451 ) ) ;
#1899=EDGE_LOOP ( 'NONE', ( #5010, #17264, #11538, #20190 ) ) ;
#1902=FACE_OUTER_BOUND ( 'NONE', #6911, .T. ) ;
#1908=CARTESIAN_POINT ( 'NONE',  ( 6.198496396448986090, 45.68315280215533392, 94.08621380123798872 ) ) ;
#1909=CARTESIAN_POINT ( 'NONE',  ( -4.567115856812060670, 47.10047254335474065, 92.05496380123798872 ) ) ;
#1924=AXIS2_PLACEMENT_3D ( 'NONE', #17258, #5973, #1295 ) ;
#1927=CARTESIAN_POINT ( 'NONE',  ( 1.868012774839550749, 39.13936707477651566, 94.63308880294498238 ) ) ;
#1930=EDGE_CURVE ( 'NONE', #5867, #13124, #19678, .T. ) ;
#1931=CARTESIAN_POINT ( 'NONE',  ( 5.146043734657006041, 40.41782908280415398, 90.30634084312077903 ) ) ;
#1942=CARTESIAN_POINT ( 'NONE',  ( 5.591308205070053994, 40.32050054405898720, 54.55433879953099563 ) ) ;
#1946=CARTESIAN_POINT ( 'NONE',  ( -7.677846259693483333, 47.36218137147966445, 93.55433879953098142 ) ) ;
#1949=ORIENTED_EDGE ( 'NONE', *, *, #13892, .F. ) ;
#1954=EDGE_CURVE ( 'NONE', #20010, #15290, #19843, .T. ) ;
#1962=ORIENTED_EDGE ( 'NONE', *, *, #9217, .F. ) ;
#1967=ORIENTED_EDGE ( 'NONE', *, *, #10805, .T. ) ;
#1969=FACE_OUTER_BOUND ( 'NONE', #8698, .T. ) ;
#1970=CARTESIAN_POINT ( 'NONE',  ( 5.025485839985549319, 41.56218137147963887, 91.97683879953100927 ) ) ;
#1977=EDGE_CURVE ( 'NONE', #8963, #10468, #19137, .T. ) ;
#1978=CARTESIAN_POINT ( 'NONE',  ( -2.904223097202481174, 48.62752260303690122, 92.52371379953099506 ) ) ;
#1983=CARTESIAN_POINT ( 'NONE',  ( 2.578515286158505670, 49.45973034996755047, 94.15269390996789411 ) ) ;
#1984=ADVANCED_FACE ( 'NONE', ( #6041 ), #16158, .F. ) ;
#1985=VECTOR ( 'NONE', #11567, 1000.000000000000114 ) ;
#1997=CARTESIAN_POINT ( 'NONE',  ( 4.394343283833276992, 39.11584570990505938, 95.25808880123800293 ) ) ;
#2002=ORIENTED_EDGE ( 'NONE', *, *, #15969, .T. ) ;
#2004=DIRECTION ( 'NONE',  ( -0.000000000000000000, 0.000000000000000000, -1.000000000000000000 ) ) ;
#2007=CARTESIAN_POINT ( 'NONE',  ( 35.92215374030650565, 40.96218137147972982, 45.55433879953098852 ) ) ;
#2010=PLANE ( 'NONE',  #6118 ) ;
#2011=CARTESIAN_POINT ( 'NONE',  ( -0.9988176903691428077, 49.83852402762217082, 93.14871380123798872 ) ) ;
#2013=CARTESIAN_POINT ( 'NONE',  ( 5.568489401881125289, 48.03437091500646261, 90.41433880123798872 ) ) ;
#2014=ORIENTED_EDGE ( 'NONE', *, *, #1029, .T. ) ;
#2020=CARTESIAN_POINT ( 'NONE',  ( 2.043125170982144745, 38.48583871533720213, 92.67996380123798872 ) ) ;
#2021=VECTOR ( 'NONE', #15116, 1000.000000000000000 ) ;
#2024=CARTESIAN_POINT ( 'NONE',  ( 5.722153871299536121, 42.76884579772442407, 93.58987682607209990 ) ) ;
#2031=DIRECTION ( 'NONE',  ( 0.000000000000000000, 0.000000000000000000, -1.000000000000000000 ) ) ;
#2034=AXIS2_PLACEMENT_3D ( 'NONE', #11051, #6028, #19216 ) ;
#2036=EDGE_LOOP ( 'NONE', ( #17023, #19666, #5561, #5661, #11166, #11199 ) ) ;
#2037=CARTESIAN_POINT ( 'NONE',  ( -4.500660556396669065, 42.81632233694663370, 94.32058880294496817 ) ) ;
#2040=CARTESIAN_POINT ( 'NONE',  ( -0.3080929418689875576, 37.85583172076933778, 91.35183880123798872 ) ) ;
#2048=CARTESIAN_POINT ( 'NONE',  ( 5.568489401881125289, 48.03437091500646261, 91.66433880123796030 ) ) ;
#2049=EDGE_LOOP ( 'NONE', ( #19952, #16557 ) ) ;
#2054=DIRECTION ( 'NONE',  ( 1.000000000000000000, -0.000000000000000000, -0.000000000000000000 ) ) ;
#2057=CARTESIAN_POINT ( 'NONE',  ( -3.445544706522349454, 39.98463554099927109, 92.55433879953096721 ) ) ;
#2064=VECTOR ( 'NONE', #13822, 1000.000000000000000 ) ;
#2067=EDGE_CURVE ( 'NONE', #14315, #18045, #3155, .T. ) ;
#2069=FACE_OUTER_BOUND ( 'NONE', #7311, .T. ) ;
#2070=PRODUCT_DEFINITION_FORMATION_WITH_SPECIFIED_SOURCE ( 'ANY', '', #3597, .NOT_KNOWN. ) ;
#2076=CARTESIAN_POINT ( 'NONE',  ( -0.8237052942265477018, 49.18499566818285018, 94.94558879953099506 ) ) ;
#2079=CARTESIAN_POINT ( 'NONE',  ( -3.350035803220276609, 49.20851703305431357, 95.88308880123798872 ) ) ;
#2084=VERTEX_POINT ( 'NONE', #12629 ) ;
#2086=CARTESIAN_POINT ( 'NONE',  ( -0.3080929418689875576, 37.85583172076933778, 95.10183880123796030 ) ) ;
#2088=LINE ( 'NONE', #484, #12128 ) ;
#2091=( BOUNDED_SURFACE ( )  B_SPLINE_SURFACE ( 1, 2, ( 
 ( #4682, #1515, #11203, #3108, #9611, #20557, #1204, #9400, #2996, #18964, #6080, #10901, #16093, #9303, #8001, #14487, #20954, #9196, #4791, #6389, #7690, #1103, #12891, #15885, #19373, #14272, #7790, #20753, #11313, #2688, #20650, #6186, #15683, #7592, #12585, #11006, #17477, #2903, #12691, #17886, #11732, #6494, #19, #11415, #18203, #3308, #19579, #3418, #17787, #14696, #4895, #3624, #17995, #13212, #3212, #323, #10133, #19687, #9930, #14797, #16194, #5111, #8104, #14900, #13107, #9816, #5313, #10029, #16300, #8212, #16413, #1733, #5000, #11629, #1835, #1619, #13322, #18106, #9714 ),
 ( #6706, #3526, #6815, #15019, #123, #14594, #13004, #8321, #19479, #11520, #6599, #221, #19893, #16512, #1927, #8423, #19793, #5215, #2037, #16616, #8532, #438, #6920, #13424, #16827, #4149, #12257, #2245, #7237, #3726, #8744, #2145, #8647, #13734, #20429, #964, #11829, #18735, #536, #15442, #5745, #3835, #18304, #11940, #753, #2350, #17033, #17140, #3936, #859, #2462, #10245, #16722, #13626, #8956, #7343, #7126, #20207, #5638, #2562, #10567, #15548, #20103, #7451, #15230, #12147, #15126, #643, #7017, #13516, #18626, #19992, #13948, #5421, #10677, #18417, #13835, #9059, #10357 ) ),
 .UNSPECIFIED., .F., .F., .F. ) 
 B_SPLINE_SURFACE_WITH_KNOTS ( ( 2, 2 ),
 ( 3, 2, 2, 2, 2, 2, 2, 2, 2, 2, 2, 2, 2, 2, 2, 2, 2, 2, 2, 2, 2, 2, 2, 2, 2, 2, 2, 2, 2, 2, 2, 2, 2, 2, 2, 2, 2, 2, 2, 3 ),
 ( 0.000000000000000000, 1.000000000000000000 ),
 ( 0.000000000000000000, 0.02500000000000000139, 0.05000000000000000278, 0.07499999999999999722, 0.1000000000000000056, 0.1250000000000000000, 0.1499999999999999944, 0.1749999999999999889, 0.2000000000000000111, 0.2250000000000000056, 0.2500000000000000000, 0.2750000000000000222, 0.2999999999999999889, 0.3250000000000000111, 0.3499999999999999778, 0.3750000000000000000, 0.4000000000000000222, 0.4249999999999999889, 0.4500000000000000111, 0.4749999999999999778, 0.5000000000000000000, 0.5250000000000000222, 0.5500000000000000444, 0.5749999999999999556, 0.5999999999999999778, 0.6250000000000000000, 0.6500000000000000222, 0.6750000000000000444, 0.6999999999999999556, 0.7249999999999999778, 0.7500000000000000000, 0.7750000000000000222, 0.8000000000000000444, 0.8249999999999999556, 0.8499999999999999778, 0.8750000000000000000, 0.9000000000000000222, 0.9250000000000000444, 0.9499999999999999556, 0.9600309957089442348 ),
 .UNSPECIFIED. ) 
 GEOMETRIC_REPRESENTATION_ITEM ( )  RATIONAL_B_SPLINE_SURFACE ( (
 ( 1.000000000000000000, 0.9238795325112867385, 1.000000000000000000, 0.9238795325112867385, 1.000000000000000000, 0.9238795325112867385, 1.000000000000000000, 0.9238795325112867385, 1.000000000000000000, 0.9238795325112867385, 1.000000000000000000, 0.9238795325112867385, 1.000000000000000000, 0.9238795325112867385, 1.000000000000000000, 0.9238795325112867385, 1.000000000000000000, 0.9238795325112867385, 1.000000000000000000, 0.9238795325112867385, 1.000000000000000000, 0.9238795325112867385, 1.000000000000000000, 0.9238795325112867385, 1.000000000000000000, 0.9238795325112867385, 1.000000000000000000, 0.9238795325112867385, 1.000000000000000000, 0.9238795325112867385, 1.000000000000000000, 0.9238795325112867385, 1.000000000000000000, 0.9238795325112867385, 1.000000000000000000, 0.9238795325112867385, 1.000000000000000000, 0.9238795325112867385, 1.000000000000000000, 0.9238795325112867385, 1.000000000000000000, 0.9238795325112867385, 1.000000000000000000, 0.9238795325112867385, 1.000000000000000000, 0.9238795325112867385, 1.000000000000000000, 0.9238795325112867385, 1.000000000000000000, 0.9238795325112867385, 1.000000000000000000, 0.9238795325112867385, 1.000000000000000000, 0.9238795325112867385, 1.000000000000000000, 0.9238795325112867385, 1.000000000000000000, 0.9238795325112867385, 1.000000000000000000, 0.9238795325112867385, 1.000000000000000000, 0.9238795325112867385, 1.000000000000000000, 0.9238795325112867385, 1.000000000000000000, 0.9238795325112867385, 1.000000000000000000, 0.9238795325112867385, 1.000000000000000000, 0.9238795325112867385, 1.000000000000000000, 0.9238795325112867385, 1.000000000000000000, 0.9238795325112867385, 1.000000000000000000, 0.9238795325112867385, 1.000000000000000000, 0.9694574366903154772, 0.9634246591005992677),
 ( 1.000000000000000000, 0.9238795325112867385, 1.000000000000000000, 0.9238795325112867385, 1.000000000000000000, 0.9238795325112867385, 1.000000000000000000, 0.9238795325112867385, 1.000000000000000000, 0.9238795325112867385, 1.000000000000000000, 0.9238795325112867385, 1.000000000000000000, 0.9238795325112867385, 1.000000000000000000, 0.9238795325112867385, 1.000000000000000000, 0.9238795325112867385, 1.000000000000000000, 0.9238795325112867385, 1.000000000000000000, 0.9238795325112867385, 1.000000000000000000, 0.9238795325112867385, 1.000000000000000000, 0.9238795325112867385, 1.000000000000000000, 0.9238795325112867385, 1.000000000000000000, 0.9238795325112867385, 1.000000000000000000, 0.9238795325112867385, 1.000000000000000000, 0.9238795325112867385, 1.000000000000000000, 0.9238795325112867385, 1.000000000000000000, 0.9238795325112867385, 1.000000000000000000, 0.9238795325112867385, 1.000000000000000000, 0.9238795325112867385, 1.000000000000000000, 0.9238795325112867385, 1.000000000000000000, 0.9238795325112867385, 1.000000000000000000, 0.9238795325112867385, 1.000000000000000000, 0.9238795325112867385, 1.000000000000000000, 0.9238795325112867385, 1.000000000000000000, 0.9238795325112867385, 1.000000000000000000, 0.9238795325112867385, 1.000000000000000000, 0.9238795325112867385, 1.000000000000000000, 0.9238795325112867385, 1.000000000000000000, 0.9238795325112867385, 1.000000000000000000, 0.9238795325112867385, 1.000000000000000000, 0.9238795325112867385, 1.000000000000000000, 0.9238795325112867385, 1.000000000000000000, 0.9238795325112867385, 1.000000000000000000, 0.9238795325112867385, 1.000000000000000000, 0.9238795325112867385, 1.000000000000000000, 0.9238795325112867385, 1.000000000000000000, 0.9694574366903154772, 0.9634246591005992677) ) ) 
 REPRESENTATION_ITEM ( '' )  SURFACE ( )  );
#2095=EDGE_CURVE ( 'NONE', #10737, #7917, #17515, .T. ) ;
#2106=DIRECTION ( 'NONE',  ( 1.402518428993854849E-16, -1.000000000000000000, -1.734723475976787846E-14 ) ) ;
#2107=CARTESIAN_POINT ( 'NONE',  ( -3.350035803220276609, 49.20851703305431357, 93.38308880123798872 ) ) ;
#2111=DIRECTION ( 'NONE',  ( -1.193617070626243484E-16, -1.000000000000000000, 0.000000000000000000 ) ) ;
#2113=CARTESIAN_POINT ( 'NONE',  ( 2.263363662449363822, 49.77488197367694767, 93.19231768333818877 ) ) ;
#2117=CARTESIAN_POINT ( 'NONE',  ( 11.22215374030649926, 39.96218137147969429, 80.55433879953099563 ) ) ;
#2121=DIRECTION ( 'NONE',  ( -1.196361017915039239E-16, 0.000000000000000000, 1.000000000000000000 ) ) ;
#2122=CARTESIAN_POINT ( 'NONE',  ( 5.611423337425062385, 41.22389019960463230, 91.42996380123798872 ) ) ;
#2124=LINE ( 'NONE', #12123, #12319 ) ;
#2131=CARTESIAN_POINT ( 'NONE',  ( 4.394343283833276992, 39.11584570990505938, 92.75808880123797451 ) ) ;
#2132=AXIS2_PLACEMENT_3D ( 'NONE', #16318, #5124, #37 ) ;
#2143=CARTESIAN_POINT ( 'NONE',  ( -2.389205813017604374, 39.09668198135606332, 95.05433879953093879 ) ) ;
#2144=CARTESIAN_POINT ( 'NONE',  ( 4.199109002476567376, 47.83913663364971569, 95.05036078555451695 ) ) ;
#2145=CARTESIAN_POINT ( 'NONE',  ( -0.2125050281363792815, 38.58189400963055959, 93.30496380294501080 ) ) ;
#2149=CARTESIAN_POINT ( 'NONE',  ( 5.611423337425062385, 41.22389019960463230, 93.92996380123798872 ) ) ;
#2155=CARTESIAN_POINT ( 'NONE',  ( -1.219056181836355446, 49.77488197367695477, 93.15612966814926210 ) ) ;
#2156=CARTESIAN_POINT ( 'NONE',  ( -2.077846259693550746, 39.65884927180063357, 95.72683880294496817 ) ) ;
#2157=VERTEX_POINT ( 'NONE', #2811 ) ;
#2158=CARTESIAN_POINT ( 'NONE',  ( 6.722153740306509917, 44.16218137147969003, 80.55433879953099563 ) ) ;
#2163=CARTESIAN_POINT ( 'NONE',  ( 31.22215374030650281, 42.96218137147968008, 77.40433879953098995 ) ) ;
#2166=EDGE_CURVE ( 'NONE', #122, #3564, #20766, .T. ) ;
#2167=ORIENTED_EDGE ( 'NONE', *, *, #8591, .T. ) ;
#2168=CARTESIAN_POINT ( 'NONE',  ( -3.677846259693500652, 44.16218137147969003, 54.55433879953099563 ) ) ;
#2170=CARTESIAN_POINT ( 'NONE',  ( 5.568489401881125289, 48.03437091500647682, 93.07058880123797451 ) ) ;
#2175=VERTEX_POINT ( 'NONE', #20570 ) ;
#2176=CARTESIAN_POINT ( 'NONE',  ( 11.22215374030650281, 42.96218137147968008, 61.40715055817103263 ) ) ;
#2177=ORIENTED_EDGE ( 'NONE', *, *, #126, .F. ) ;
#2178=PLANE ( 'NONE',  #2728 ) ;
#2179=CARTESIAN_POINT ( 'NONE',  ( -2.077846259693550746, 39.65884927180063357, 92.91433879953098085 ) ) ;
#2180=CARTESIAN_POINT ( 'NONE',  ( -3.981178359372548492, 46.76218137147973408, 95.10183879953099506 ) ) ;
#2188=VERTEX_POINT ( 'NONE', #4389 ) ;
#2193=CARTESIAN_POINT ( 'NONE',  ( 4.394343283833276992, 39.11584570990505938, 91.35183880123798872 ) ) ;
#2199=CARTESIAN_POINT ( 'NONE',  ( 5.722153740306500147, 44.16218137147968292, 93.33161078214054385 ) ) ;
#2203=CARTESIAN_POINT ( 'NONE',  ( 5.568489401881125289, 48.03437091500646261, 94.32058880123798872 ) ) ;
#2209=ADVANCED_FACE ( 'NONE', ( #9412 ), #16002, .F. ) ;
#2211=EDGE_CURVE ( 'NONE', #18929, #2282, #6718, .T. ) ;
#2218=CARTESIAN_POINT ( 'NONE',  ( 1.443767556222832260, 38.34550624821717690, 92.55433879953092458 ) ) ;
#2221=CARTESIAN_POINT ( 'NONE',  ( 4.394343283833276992, 39.11584570990505938, 93.85183880123797451 ) ) ;
#2228=CARTESIAN_POINT ( 'NONE',  ( 1.514255888186003984, 52.36218137147968577, 83.03825919817350609 ) ) ;
#2230=CARTESIAN_POINT ( 'NONE',  ( 5.611423337425062385, 41.22389019960463230, 95.33621380123798872 ) ) ;
#2233=CARTESIAN_POINT ( 'NONE',  ( 1.352400422481993658, 50.46853102219002096, 91.97683880123797451 ) ) ;
#2236=EDGE_LOOP ( 'NONE', ( #1193, #16651, #19748, #1602, #7326 ) ) ;
#2241=ORIENTED_EDGE ( 'NONE', *, *, #12352, .T. ) ;
#2243=CARTESIAN_POINT ( 'NONE',  ( -4.927956858767000625, 44.38046240684710142, 95.05433879953103826 ) ) ;
#2245=CARTESIAN_POINT ( 'NONE',  ( 6.102441102155617969, 43.42752260303680600, 93.61746380294498238 ) ) ;
#2248=CARTESIAN_POINT ( 'NONE',  ( 2.043125170982144745, 38.48583871533720213, 95.02371380123798872 ) ) ;
#2250=CARTESIAN_POINT ( 'NONE',  ( 10.77494014480653561, 42.76218137147968434, 69.80574467885101342 ) ) ;
#2253=ORIENTED_EDGE ( 'NONE', *, *, #20354, .T. ) ;
#2254=CARTESIAN_POINT ( 'NONE',  ( -4.477846259693498254, 50.66218137147966871, 53.35433879953099989 ) ) ;
#2255=CARTESIAN_POINT ( 'NONE',  ( 3.122153740306552905, 48.66551347115873227, 95.10183880294498238 ) ) ;
#2272=VECTOR ( 'NONE', #7583, 1000.000000000000000 ) ;
#2275=DIRECTION ( 'NONE',  ( 0.000000000000000000, 0.000000000000000000, -1.000000000000000000 ) ) ;
#2279=CARTESIAN_POINT ( 'NONE',  ( -4.500660556396669065, 42.81632233694663370, 95.25808879953098085 ) ) ;
#2280=CARTESIAN_POINT ( 'NONE',  ( -0.8237052942265477018, 49.18499566818285018, 92.44558879953099506 ) ) ;
#2282=VERTEX_POINT ( 'NONE', #16315 ) ;
#2283=FACE_OUTER_BOUND ( 'NONE', #12410, .T. ) ;
#2284=CARTESIAN_POINT ( 'NONE',  ( 30.92220646078100188, 42.76218137147968434, 62.80715055817104542 ) ) ;
#2285=LINE ( 'NONE', #17083, #16612 ) ;
#2287=CARTESIAN_POINT ( 'NONE',  ( 3.122153740306552905, 48.66551347115873227, 92.28933879953099506 ) ) ;
#2290=CARTESIAN_POINT ( 'NONE',  ( -0.3080929418689875576, 37.85583172076933778, 93.85183880123797451 ) ) ;
#2294=CARTESIAN_POINT ( 'NONE',  ( 0.5221537403065010796, 44.16218137147969003, 45.55433879953098852 ) ) ;
#2295=CARTESIAN_POINT ( 'NONE',  ( -2.416137431568557314, 39.07291177436112406, 91.11746380123798872 ) ) ;
#2297=CARTESIAN_POINT ( 'NONE',  ( -0.4699484075730042676, 52.36218137147968577, 52.53721119516358584 ) ) ;
#2308=CARTESIAN_POINT ( 'NONE',  ( -5.784195910403845176, 44.99242805365518194, 96.03933880123796030 ) ) ;
#2315=ADVANCED_FACE ( 'NONE', ( #16426 ), #5301, .T. ) ;
#2318=DIRECTION ( 'NONE',  ( 0.6546536707079709805, 0.6546536707079818607, -0.3779644730092299176 ) ) ;
#2319=CARTESIAN_POINT ( 'NONE',  ( -5.154188915835984375, 42.64120994080404614, 94.86746380123797451 ) ) ;
#2323=CARTESIAN_POINT ( 'NONE',  ( -0.2125050281363792815, 38.58189400963055959, 94.55496380294496817 ) ) ;
#2326=( LENGTH_UNIT ( ) NAMED_UNIT ( * ) SI_UNIT ( .MILLI., .METRE. ) );
#2332=CARTESIAN_POINT ( 'NONE',  ( 30.92220646078100188, 42.76218137147968434, 56.80715055817104542 ) ) ;
#2333=PLANE ( 'NONE',  #7182 ) ;
#2335=CARTESIAN_POINT ( 'NONE',  ( -3.350035803220276609, 49.20851703305431357, 93.38308880123798872 ) ) ;
#2340=CARTESIAN_POINT ( 'NONE',  ( 3.948530577815479337, 39.69684013992245752, 93.46121380294498238 ) ) ;
#2350=CARTESIAN_POINT ( 'NONE',  ( 3.948530577815480225, 39.69684013992245752, 92.21121380294495395 ) ) ;
#2353=CARTESIAN_POINT ( 'NONE',  ( -2.416137431568557314, 39.07291177436112406, 93.61746380123797451 ) ) ;
#2358=VECTOR ( 'NONE', #13013, 1000.000000000000000 ) ;
#2359=ORIENTED_EDGE ( 'NONE', *, *, #16564, .F. ) ;
#2360=DIRECTION ( 'NONE',  ( -0.000000000000000000, -2.168404344970984413E-15, -1.000000000000000000 ) ) ;
#2362=CARTESIAN_POINT ( 'NONE',  ( 5.544968037009670780, 45.50804040601273925, 94.94558880294498238 ) ) ;
#2363=EDGE_LOOP ( 'NONE', ( #12852, #210, #5950, #18962 ) ) ;
#2369=DIRECTION ( 'NONE',  ( -1.000000000000000000, 0.000000000000000000, -0.000000000000000000 ) ) ;
#2385=VECTOR ( 'NONE', #7392, 1000.000000000000000 ) ;
#2389=CARTESIAN_POINT ( 'NONE',  ( 30.92220646078100188, 42.96218137147968008, 58.20715055817105110 ) ) ;
#2391=CARTESIAN_POINT ( 'NONE',  ( -3.981178359372548492, 46.76218137147973408, 95.10183879953099506 ) ) ;
#2392=CARTESIAN_POINT ( 'NONE',  ( -3.981178359372548492, 46.76218137147973408, 91.35183879953098085 ) ) ;
#2394=AXIS2_PLACEMENT_3D ( 'NONE', #17774, #1394, #9289 ) ;
#2395=CARTESIAN_POINT ( 'NONE',  ( -4.567115856812060670, 47.10047254335474065, 94.71121380123797451 ) ) ;
#2399=LINE ( 'NONE', #801, #20706 ) ;
#2402=CARTESIAN_POINT ( 'NONE',  ( 6.198496396448986090, 45.68315280215533392, 95.49246380123798872 ) ) ;
#2403=VECTOR ( 'NONE', #9178, 1000.000000000000000 ) ;
#2408=CARTESIAN_POINT ( 'NONE',  ( -7.677846259693478892, 49.36218137147968577, 93.55433879953098142 ) ) ;
#2415=ORIENTED_EDGE ( 'NONE', *, *, #16270, .T. ) ;
#2420=CARTESIAN_POINT ( 'NONE',  ( -3.350035803220276609, 49.20851703305431357, 94.63308880123798872 ) ) ;
#2422=VERTEX_POINT ( 'NONE', #11012 ) ;
#2424=VECTOR ( 'NONE', #5350, 1000.000000000000000 ) ;
#2425=ORIENTED_EDGE ( 'NONE', *, *, #12252, .T. ) ;
#2431=CARTESIAN_POINT ( 'NONE',  ( 6.198496396448986090, 45.68315280215533392, 95.49246380123798872 ) ) ;
#2437=CARTESIAN_POINT ( 'NONE',  ( 1.256812508749381774, 49.74246873332880625, 91.42996380294499659 ) ) ;
#2440=( NAMED_UNIT ( * ) PLANE_ANGLE_UNIT ( ) SI_UNIT ( $, .RADIAN. ) );
#2442=VERTEX_POINT ( 'NONE', #12793 ) ;
#2443=CARTESIAN_POINT ( 'NONE',  ( 5.184346195548571679, 46.85389944066466228, 94.99612681657399094 ) ) ;
#2447=CARTESIAN_POINT ( 'NONE',  ( -4.524181921268124462, 40.28999182795290324, 94.94558880123797451 ) ) ;
#2451=CARTESIAN_POINT ( 'NONE',  ( -3.943187491250720544, 40.73580453397070755, 93.14871380294496817 ) ) ;
#2454=VECTOR ( 'NONE', #7597, 1000.000000000000000 ) ;
#2458=AXIS2_PLACEMENT_3D ( 'NONE', #18855, #4062, #14162 ) ;
#2462=CARTESIAN_POINT ( 'NONE',  ( -4.500660556396669065, 42.81632233694663370, 91.82058880294496817 ) ) ;
#2464=DIRECTION ( 'NONE',  ( -1.193617070626243484E-16, -1.000000000000000000, -0.000000000000000000 ) ) ;
#2466=CARTESIAN_POINT ( 'NONE',  ( -5.154188915835984375, 42.64120994080404614, 92.21121380123797451 ) ) ;
#2472=FACE_OUTER_BOUND ( 'NONE', #3003, .T. ) ;
#2475=CARTESIAN_POINT ( 'NONE',  ( 5.611423337425062385, 41.22389019960463230, 92.67996380123798872 ) ) ;
#2493=DIRECTION ( 'NONE',  ( 1.000000000000000000, 0.000000000000000000, 0.000000000000000000 ) ) ;
#2501=AXIS2_PLACEMENT_3D ( 'NONE', #13027, #4916, #16013 ) ;
#2503=CARTESIAN_POINT ( 'NONE',  ( 4.987494971863720927, 47.58855820898865829, 95.96121379953099506 ) ) ;
#2505=CARTESIAN_POINT ( 'NONE',  ( -0.3080929418689875576, 37.85583172076933778, 93.85183880123797451 ) ) ;
#2510=CARTESIAN_POINT ( 'NONE',  ( -3.677846259693500652, 44.16218137147969003, 45.55433879953098852 ) ) ;
#2513=VERTEX_POINT ( 'NONE', #13405 ) ;
#2516=AXIS2_PLACEMENT_3D ( 'NONE', #11801, #14774, #18277 ) ;
#2521=CARTESIAN_POINT ( 'NONE',  ( 11.22215374030650281, 45.56218137147968861, 78.80433879953099563 ) ) ;
#2522=ORIENTED_EDGE ( 'NONE', *, *, #1302, .F. ) ;
#2527=CARTESIAN_POINT ( 'NONE',  ( -3.350035803220276609, 49.20851703305431357, 92.13308880123798872 ) ) ;
#2533=CARTESIAN_POINT ( 'NONE',  ( -1.677846259693499542, 47.73989013547934945, 50.15433879953098995 ) ) ;
#2534=LINE ( 'NONE', #14221, #20125 ) ;
#2541=CARTESIAN_POINT ( 'NONE',  ( 3.948530577815480225, 39.69684013992245752, 93.46121380294496817 ) ) ;
#2545=ORIENTED_EDGE ( 'NONE', *, *, #1954, .T. ) ;
#2550=EDGE_CURVE ( 'NONE', #19372, #10780, #8827, .T. ) ;
#2560=DIRECTION ( 'NONE',  ( 2.838338907332122006E-16, -1.000000000000000000, 0.000000000000000000 ) ) ;
#2562=CARTESIAN_POINT ( 'NONE',  ( 6.102441102155617969, 43.42752260303680600, 91.11746380294498238 ) ) ;
#2569=ORIENTED_EDGE ( 'NONE', *, *, #3990, .F. ) ;
#2570=EDGE_CURVE ( 'NONE', #11438, #5268, #734, .T. ) ;
#2572=CARTESIAN_POINT ( 'NONE',  ( -2.904223097202481174, 48.62752260303690122, 91.58621380294496817 ) ) ;
#2575=CARTESIAN_POINT ( 'NONE',  ( 5.025485839985549319, 41.56218137147963887, 94.47683879953099506 ) ) ;
#2580=VERTEX_POINT ( 'NONE', #2332 ) ;
#2585=DIRECTION ( 'NONE',  ( 1.193617070626243484E-16, 1.000000000000000000, 0.000000000000000000 ) ) ;
#2587=CARTESIAN_POINT ( 'NONE',  ( 2.043125170982144745, 38.48583871533720213, 92.67996380123798872 ) ) ;
#2590=DIRECTION ( 'NONE',  ( -1.000000000000000000, 0.000000000000000000, -1.196361017915039239E-16 ) ) ;
#2595=EDGE_CURVE ( 'NONE', #18174, #2513, #3369, .T. ) ;
#2601=CARTESIAN_POINT ( 'NONE',  ( 4.394343283833276992, 39.11584570990505938, 95.25808880123800293 ) ) ;
#2603=CARTESIAN_POINT ( 'NONE',  ( 6.198496396448986090, 45.68315280215533392, 91.74246380123798872 ) ) ;
#2610=CARTESIAN_POINT ( 'NONE',  ( -5.784195910403845176, 44.99242805365518194, 92.28933880123798872 ) ) ;
#2611=ORIENTED_EDGE ( 'NONE', *, *, #14253, .T. ) ;
#2619=LINE ( 'NONE', #2521, #10976 ) ;
#2622=EDGE_LOOP ( 'NONE', ( #13279, #1805, #3995, #7696 ) ) ;
#2626=CARTESIAN_POINT ( 'NONE',  ( -4.567115856812060670, 47.10047254335474065, 95.80496380123798872 ) ) ;
#2639=CARTESIAN_POINT ( 'NONE',  ( -4.477846259693498254, 50.66218137147966871, 53.35433879953099989 ) ) ;
#2646=CARTESIAN_POINT ( 'NONE',  ( -3.943187491250720544, 40.73580453397070755, 94.39871380294496817 ) ) ;
#2657=LINE ( 'NONE', #12136, #9258 ) ;
#2661=CARTESIAN_POINT ( 'NONE',  ( -2.013565751266337411, 38.84048690637051493, 95.03863327408461714 ) ) ;
#2662=LINE ( 'NONE', #1382, #12497 ) ;
#2664=CARTESIAN_POINT ( 'NONE',  ( 35.92215374030650565, 40.96218137147972982, 93.55433879953098142 ) ) ;
#2665=CIRCLE ( 'NONE', #14562, 0.9921021478795020165 ) ;
#2668=CARTESIAN_POINT ( 'NONE',  ( 5.568489401881125289, 48.03437091500646261, 90.41433880123798872 ) ) ;
#2674=CARTESIAN_POINT ( 'NONE',  ( 5.544968037009670780, 45.50804040601273925, 93.69558880294498238 ) ) ;
#2675=ORIENTED_EDGE ( 'NONE', *, *, #10607, .F. ) ;
#2676=FACE_BOUND ( 'NONE', #2833, .T. ) ;
#2684=LINE ( 'NONE', #20855, #13926 ) ;
#2688=CARTESIAN_POINT ( 'NONE',  ( 4.394343283833276992, 39.11584570990505938, 93.85183880123797451 ) ) ;
#2694=VECTOR ( 'NONE', #7470, 1000.000000000000000 ) ;
#2695=ORIENTED_EDGE ( 'NONE', *, *, #4425, .F. ) ;
#2699=LINE ( 'NONE', #13666, #15975 ) ;
#2700=ADVANCED_FACE ( 'NONE', ( #4130, #15530 ), #1168, .F. ) ;
#2701=CARTESIAN_POINT ( 'NONE',  ( 6.198496396448986090, 45.68315280215533392, 92.99246380123798872 ) ) ;
#2705=CARTESIAN_POINT ( 'NONE',  ( -5.784195910403845176, 44.99242805365518194, 94.78933880123798872 ) ) ;
#2713=CARTESIAN_POINT ( 'NONE',  ( 5.722153740306500147, 44.16218137147968292, 93.33161078214054385 ) ) ;
#2714=CARTESIAN_POINT ( 'NONE',  ( -0.9988176903691428077, 49.83852402762217082, 90.80496380123797451 ) ) ;
#2723=EDGE_CURVE ( 'NONE', #7833, #10210, #20614, .T. ) ;
#2728=AXIS2_PLACEMENT_3D ( 'NONE', #570, #14941, #10281 ) ;
#2732=CARTESIAN_POINT ( 'NONE',  ( 5.611423337425062385, 41.22389019960463230, 95.17996380123798872 ) ) ;
#2741=CARTESIAN_POINT ( 'NONE',  ( -0.4699484075729998822, 52.36218137147968577, 83.03825919817350609 ) ) ;
#2747=CARTESIAN_POINT ( 'NONE',  ( -0.9988176903691428077, 49.83852402762217082, 95.64871380123798872 ) ) ;
#2751=LINE ( 'NONE', #12538, #345 ) ;
#2752=ADVANCED_BREP_SHAPE_REPRESENTATION ( '', ( #4882, #18366 ), #20720 ) ;
#2754=CARTESIAN_POINT ( 'NONE',  ( -0.8237052942265477018, 49.18499566818285018, 92.75808880294498238 ) ) ;
#2758=EDGE_CURVE ( 'NONE', #20573, #16680, #14026, .T. ) ;
#2759=CARTESIAN_POINT ( 'NONE',  ( -4.677846259693495767, 44.16218127507053737, 93.01911326394946400 ) ) ;
#2760=B_SPLINE_CURVE_WITH_KNOTS ( 'NONE', 3,
 ( #14528, #3457, #13252, #19520, #10067, #14739 ),
 .UNSPECIFIED., .F., .F.,
 ( 4, 2, 4 ),
 ( 0.000000000000000000, 0.001346084890031584453, 0.002692169780063168906 ),
 .UNSPECIFIED. ) ;
#2762=CARTESIAN_POINT ( 'NONE',  ( 5.544968037009670780, 45.50804040601273925, 93.38308879953099506 ) ) ;
#2764=CARTESIAN_POINT ( 'NONE',  ( 11.32022995165975843, 49.36218137147968577, 93.55433879953098142 ) ) ;
#2765=EDGE_CURVE ( 'NONE', #8464, #2084, #14233, .T. ) ;
#2768=VERTEX_POINT ( 'NONE', #7327 ) ;
#2781=CARTESIAN_POINT ( 'NONE',  ( 3.460444912181559474, 49.25145096859824889, 91.74246380123798872 ) ) ;
#2789=CARTESIAN_POINT ( 'NONE',  ( -0.8237052942265477018, 49.18499566818285018, 92.75808880294498238 ) ) ;
#2790=ORIENTED_EDGE ( 'NONE', *, *, #12998, .F. ) ;
#2791=DIRECTION ( 'NONE',  ( 1.000000000000000000, 1.402518428993831676E-16, 0.000000000000000000 ) ) ;
#2793=CARTESIAN_POINT ( 'NONE',  ( 0.5221537403065010796, 44.16218137147969003, 77.84651775085080772 ) ) ;
#2797=ORIENTED_EDGE ( 'NONE', *, *, #17800, .T. ) ;
#2806=VERTEX_POINT ( 'NONE', #19034 ) ;
#2810=CARTESIAN_POINT ( 'NONE',  ( -4.524181921268124462, 40.28999182795290324, 93.69558880123800293 ) ) ;
#2811=CARTESIAN_POINT ( 'NONE',  ( 2.916646314871006229, 38.79555996194933698, 95.05433879953095300 ) ) ;
#2820=CARTESIAN_POINT ( 'NONE',  ( -4.677846259693498432, 44.16218137147969003, 92.70661078214052964 ) ) ;
#2821=CARTESIAN_POINT ( 'NONE',  ( 5.568489401881125289, 48.03437091500646261, 91.82058880123797451 ) ) ;
#2824=CARTESIAN_POINT ( 'NONE',  ( 6.004165720785556104, 44.16394627378592475, 95.05433879953098142 ) ) ;
#2833=EDGE_LOOP ( 'NONE', ( #14116, #261, #8428, #8236, #19876, #764 ) ) ;
#2836=CARTESIAN_POINT ( 'NONE',  ( -0.3080929418689875576, 37.85583172076933778, 94.94558880123797451 ) ) ;
#2849=ORIENTED_EDGE ( 'NONE', *, *, #12126, .F. ) ;
#2853=CARTESIAN_POINT ( 'NONE',  ( 6.828503391016846891, 43.33193468930419101, 95.25808880123800293 ) ) ;
#2864=CARTESIAN_POINT ( 'NONE',  ( -3.350035803220276609, 49.20851703305431357, 90.88308880123797451 ) ) ;
#2866=ADVANCED_FACE ( 'NONE', ( #1480 ), #16260, .F. ) ;
#2870=EDGE_CURVE ( 'NONE', #5518, #20498, #19545, .T. ) ;
#2878=LINE ( 'NONE', #20625, #15552 ) ;
#2883=CARTESIAN_POINT ( 'NONE',  ( -0.3080929418689875576, 37.85583172076933778, 92.44558880123798872 ) ) ;
#2889=CARTESIAN_POINT ( 'NONE',  ( -5.058133621542618030, 44.89684013992257405, 94.24246380294498238 ) ) ;
#2896=EDGE_CURVE ( 'NONE', #15717, #3265, #3180, .T. ) ;
#2903=CARTESIAN_POINT ( 'NONE',  ( -3.350035803220276609, 49.20851703305431357, 93.22683880123798872 ) ) ;
#2906=DIRECTION ( 'NONE',  ( -1.000000000000000000, -6.608470384673549446E-15, 0.000000000000000000 ) ) ;
#2911=ORIENTED_EDGE ( 'NONE', *, *, #12657, .T. ) ;
#2913=CARTESIAN_POINT ( 'NONE',  ( 2.043125170982144745, 38.48583871533720213, 95.17996380123798872 ) ) ;
#2919=ORIENTED_EDGE ( 'NONE', *, *, #8591, .F. ) ;
#2920=CARTESIAN_POINT ( 'NONE',  ( -4.677846259693817288, 43.47758838402644699, 92.73325776475002158 ) ) ;
#2924=CARTESIAN_POINT ( 'NONE',  ( 2.916646314871006229, 38.79555996194933698, 95.05433879953095300 ) ) ;
#2931=LINE ( 'NONE', #8538, #3105 ) ;
#2935=CARTESIAN_POINT ( 'NONE',  ( 5.611423337425062385, 41.22389019960463230, 91.58621380123798872 ) ) ;
#2951=CARTESIAN_POINT ( 'NONE',  ( -4.567115856812060670, 47.10047254335474065, 93.46121380123797451 ) ) ;
#2962=CARTESIAN_POINT ( 'NONE',  ( 5.611423337425062385, 41.22389019960463230, 90.33621380123798872 ) ) ;
#2963=EDGE_LOOP ( 'NONE', ( #9868, #6230, #2177, #20028 ) ) ;
#2972=VECTOR ( 'NONE', #4737, 1000.000000000000000 ) ;
#2974=DIRECTION ( 'NONE',  ( 1.000000000000000000, -1.193617070626243484E-16, 0.000000000000000000 ) ) ;
#2975=LINE ( 'NONE', #15967, #6569 ) ;
#2985=CARTESIAN_POINT ( 'NONE',  ( 3.948530577815480225, 39.69684013992245752, 92.21121380294495395 ) ) ;
#2986=ORIENTED_EDGE ( 'NONE', *, *, #17560, .F. ) ;
#2987=CARTESIAN_POINT ( 'NONE',  ( -2.825834663281995951, 48.16810349223128895, 95.03225227128623942 ) ) ;
#2990=PLANE ( 'NONE',  #9061 ) ;
#2995=ORIENTED_EDGE ( 'NONE', *, *, #178, .T. ) ;
#2996=CARTESIAN_POINT ( 'NONE',  ( 3.460444912181559474, 49.25145096859824889, 95.49246380123798872 ) ) ;
#2997=EDGE_CURVE ( 'NONE', #8207, #9962, #16785, .T. ) ;
#3003=EDGE_LOOP ( 'NONE', ( #11625, #3949, #9552, #17418 ) ) ;
#3004=EDGE_CURVE ( 'NONE', #13604, #9419, #15083, .T. ) ;
#3008=EDGE_CURVE ( 'NONE', #14315, #14996, #6770, .T. ) ;
#3012=CARTESIAN_POINT ( 'NONE',  ( 5.568489401881125289, 48.03437091500646261, 93.07058880123797451 ) ) ;
#3016=CARTESIAN_POINT ( 'NONE',  ( -7.677846259693483333, 47.36218137147966445, 93.55433879953098142 ) ) ;
#3020=VERTEX_POINT ( 'NONE', #14762 ) ;
#3021=CARTESIAN_POINT ( 'NONE',  ( -4.956284031279793112, 43.92723849310139883, 92.55433879953098142 ) ) ;
#3041=DIRECTION ( 'NONE',  ( 0.000000000000000000, 0.000000000000000000, -1.000000000000000000 ) ) ;
#3044=VECTOR ( 'NONE', #17333, 1000.000000000000000 ) ;
#3060=CARTESIAN_POINT ( 'NONE',  ( 5.146043734657006041, 40.41782908280415398, 90.30634084312077903 ) ) ;
#3061=DIRECTION ( 'NONE',  ( 1.000000000000000000, 0.000000000000000000, 0.000000000000000000 ) ) ;
#3064=VECTOR ( 'NONE', #13782, 1000.000000000000000 ) ;
#3073=CARTESIAN_POINT ( 'NONE',  ( -3.154801521863568325, 47.83913663364971569, 94.11286078555450274 ) ) ;
#3077=ORIENTED_EDGE ( 'NONE', *, *, #8887, .F. ) ;
#3078=ADVANCED_FACE ( 'NONE', ( #16573 ), #8489, .F. ) ;
#3080=CARTESIAN_POINT ( 'NONE',  ( 1.514255888186008425, 52.36218137147968577, 48.36106904222365444 ) ) ;
#3082=CARTESIAN_POINT ( 'NONE',  ( 28.52215374030649997, 44.16218137147968292, 45.55433879953098852 ) ) ;
#3091=ORIENTED_EDGE ( 'NONE', *, *, #10308, .F. ) ;
#3105=VECTOR ( 'NONE', #8109, 1000.000000000000000 ) ;
#3108=CARTESIAN_POINT ( 'NONE',  ( -5.784195910403845176, 44.99242805365518194, 95.88308880123798872 ) ) ;
#3109=CARTESIAN_POINT ( 'NONE',  ( -2.416137431568557314, 39.07291177436112406, 93.61746380123797451 ) ) ;
#3112=EDGE_CURVE ( 'NONE', #531, #7336, #5924, .T. ) ;
#3115=VERTEX_POINT ( 'NONE', #15612 ) ;
#3130=VERTEX_POINT ( 'NONE', #10937 ) ;
#3131=CARTESIAN_POINT ( 'NONE',  ( -4.769179815246321397, 42.34626837109277631, 92.55433879953098142 ) ) ;
#3136=CARTESIAN_POINT ( 'NONE',  ( 5.933406720878987350, 44.83544050270759840, 95.05433879953098142 ) ) ;
#3143=DIRECTION ( 'NONE',  ( 1.402518428993831676E-16, -1.000000000000000000, 0.000000000000000000 ) ) ;
#3155=LINE ( 'NONE', #17308, #11527 ) ;
#3161=CARTESIAN_POINT ( 'NONE',  ( 1.868012774839550749, 39.13936707477651566, 93.07058879953099506 ) ) ;
#3170=EDGE_CURVE ( 'NONE', #10809, #122, #20796, .T. ) ;
#3171=CARTESIAN_POINT ( 'NONE',  ( -4.524181921268124462, 40.28999182795290324, 92.44558880123798872 ) ) ;
#3173=CARTESIAN_POINT ( 'NONE',  ( 4.001626195812781006, 40.29782224849783745, 89.72723091094957226 ) ) ;
#3176=VERTEX_POINT ( 'NONE', #7727 ) ;
#3180=LINE ( 'NONE', #20823, #13578 ) ;
#3189=PLANE ( 'NONE',  #4864 ) ;
#3197=EDGE_CURVE ( 'NONE', #13434, #19503, #20992, .T. ) ;
#3198=ORIENTED_EDGE ( 'NONE', *, *, #1718, .T. ) ;
#3212=CARTESIAN_POINT ( 'NONE',  ( -0.9988176903691428077, 49.83852402762217082, 91.89871380123798872 ) ) ;
#3220=ORIENTED_EDGE ( 'NONE', *, *, #17025, .F. ) ;
#3222=CARTESIAN_POINT ( 'NONE',  ( -5.784195910403845176, 44.99242805365518194, 91.03933880123798872 ) ) ;
#3227=CARTESIAN_POINT ( 'NONE',  ( 5.880020243381231637, 42.59485829234928644, 92.55433879953100984 ) ) ;
#3229=LINE ( 'NONE', #16212, #19998 ) ;
#3230=DIRECTION ( 'NONE',  ( 0.000000000000000000, 0.000000000000000000, 1.000000000000000000 ) ) ;
#3232=CARTESIAN_POINT ( 'NONE',  ( -3.868085380944014329, 40.51689021754913256, 92.55433879953095300 ) ) ;
#3236=CARTESIAN_POINT ( 'NONE',  ( -4.477846259693498254, 36.96218137147968008, 53.35433879953099989 ) ) ;
#3240=EDGE_CURVE ( 'NONE', #10210, #4927, #16233, .T. ) ;
#3243=CARTESIAN_POINT ( 'NONE',  ( 4.454354847297358866, 39.79502961122975790, 90.11785626197793420 ) ) ;
#3248=ORIENTED_EDGE ( 'NONE', *, *, #1836, .F. ) ;
#3250=EDGE_CURVE ( 'NONE', #7497, #15145, #6321, .T. ) ;
#3255=FACE_OUTER_BOUND ( 'NONE', #11593, .T. ) ;
#3260=CARTESIAN_POINT ( 'NONE',  ( -2.077846259693550746, 39.65884927180063357, 92.91433879953098085 ) ) ;
#3265=VERTEX_POINT ( 'NONE', #9749 ) ;
#3268=DIRECTION ( 'NONE',  ( 0.000000000000000000, 1.734723475976787846E-14, -1.000000000000000000 ) ) ;
#3281=ORIENTED_EDGE ( 'NONE', *, *, #19722, .T. ) ;
#3290=CARTESIAN_POINT ( 'NONE',  ( 3.460444912181559474, 49.25145096859824889, 92.99246380123798872 ) ) ;
#3300=VECTOR ( 'NONE', #16066, 1000.000000000000000 ) ;
#3308=CARTESIAN_POINT ( 'NONE',  ( 4.394343283833276992, 39.11584570990505938, 92.60183880123797451 ) ) ;
#3321=CARTESIAN_POINT ( 'NONE',  ( 6.828503391016846891, 43.33193468930419101, 90.41433880123798872 ) ) ;
#3322=CARTESIAN_POINT ( 'NONE',  ( 2.043125170982144745, 38.48583871533720213, 93.77371380123798872 ) ) ;
#3331=CARTESIAN_POINT ( 'NONE',  ( 31.22215374030650281, 42.76218137147968434, 78.80433879953099563 ) ) ;
#3332=LINE ( 'NONE', #12808, #8958 ) ;
#3338=PLANE ( 'NONE',  #9669 ) ;
#3340=CARTESIAN_POINT ( 'NONE',  ( 3.122075258343615545, 38.59543968120053847, 90.05576841395854615 ) ) ;
#3344=ORIENTED_EDGE ( 'NONE', *, *, #3960, .F. ) ;
#3347=ORIENTED_EDGE ( 'NONE', *, *, #3170, .F. ) ;
#3349=CARTESIAN_POINT ( 'NONE',  ( 10.77494014480653561, 42.96218137147968008, 73.80433879953100984 ) ) ;
#3354=ORIENTED_EDGE ( 'NONE', *, *, #1751, .T. ) ;
#3357=CARTESIAN_POINT ( 'NONE',  ( 3.948530577815480225, 39.69684013992245752, 94.39871379953098085 ) ) ;
#3365=CARTESIAN_POINT ( 'NONE',  ( 3.870209548259372578, 48.16803608786690205, 93.81846558602697428 ) ) ;
#3366=CARTESIAN_POINT ( 'NONE',  ( -0.3080929418689875576, 37.85583172076933778, 93.69558880123800293 ) ) ;
#3369=CIRCLE ( 'NONE', #9511, 5.199999999999999289 ) ;
#3373=LINE ( 'NONE', #4860, #15014 ) ;
#3380=VERTEX_POINT ( 'NONE', #13356 ) ;
#3381=EDGE_CURVE ( 'NONE', #15424, #9111, #8251, .T. ) ;
#3385=EDGE_CURVE ( 'NONE', #12858, #11872, #8676, .T. ) ;
#3388=CARTESIAN_POINT ( 'NONE',  ( -4.677846311233719412, 45.55551708285126722, 94.21487682030836197 ) ) ;
#3396=AXIS2_PLACEMENT_3D ( 'NONE', #3331, #9836, #5022 ) ;
#3397=CARTESIAN_POINT ( 'NONE',  ( 6.828503391016846891, 43.33193468930419101, 94.00808880123798872 ) ) ;
#3398=ORIENTED_EDGE ( 'NONE', *, *, #1337, .T. ) ;
#3401=DIRECTION ( 'NONE',  ( 1.402518428993831676E-16, -1.000000000000000000, 0.000000000000000000 ) ) ;
#3403=CIRCLE ( 'NONE', #2394, 0.9921021478795020165 ) ;
#3414=ORIENTED_EDGE ( 'NONE', *, *, #9033, .T. ) ;
#3418=CARTESIAN_POINT ( 'NONE',  ( -0.3080929418689875576, 37.85583172076933778, 92.44558880123798872 ) ) ;
#3419=ADVANCED_FACE ( 'NONE', ( #10066 ), #15158, .F. ) ;
#3425=EDGE_LOOP ( 'NONE', ( #7049, #651, #13669, #18859, #13354, #11994, #5330, #9559, #20620, #16461, #17819, #13726 ) ) ;
#3427=CARTESIAN_POINT ( 'NONE',  ( 4.199109002476567376, 47.83913663364971569, 94.73786078214052964 ) ) ;
#3432=DIRECTION ( 'NONE',  ( -0.4999999999999977240, 0.8660254037844398178, -0.000000000000000000 ) ) ;
#3433=CARTESIAN_POINT ( 'NONE',  ( 5.925645890915349767, 42.81779480767480095, 92.55433879953095300 ) ) ;
#3435=CARTESIAN_POINT ( 'NONE',  ( 2.900946498003590612, 49.13729913812269245, 93.38297921192027218 ) ) ;
#3436=ORIENTED_EDGE ( 'NONE', *, *, #9011, .F. ) ;
#3437=B_SPLINE_CURVE_WITH_KNOTS ( 'NONE', 3,
 ( #16010, #12914, #3435, #16433, #4913, #6304 ),
 .UNSPECIFIED., .F., .F.,
 ( 4, 2, 4 ),
 ( 0.000000000000000000, 0.001381175314065562080, 0.002762350628131124159 ),
 .UNSPECIFIED. ) ;
#3442=DIRECTION ( 'NONE',  ( -1.402518428993831430E-16, 1.000000000000000000, -2.891205793294680792E-16 ) ) ;
#3445=VECTOR ( 'NONE', #19800, 1000.000000000000000 ) ;
#3449=( BOUNDED_CURVE ( )  B_SPLINE_CURVE ( 2, ( #19524, #17080, #18780, #12300, #8683, #5578, #9000, #12082, #13876, #13558, #20470 ),
 .UNSPECIFIED., .F., .T. ) 
 B_SPLINE_CURVE_WITH_KNOTS ( ( 3, 2, 2, 2, 2, 3 ),
 ( 0.1769864399931200261, 0.1822857915258468686, 0.2083266188866827739, 0.2343674462475186793, 0.2604082736083545568, 0.2851266819498630145 ),
 .UNSPECIFIED. ) 
 CURVE ( )  GEOMETRIC_REPRESENTATION_ITEM ( )  RATIONAL_B_SPLINE_CURVE ( ( 0.9753234597474281786, 0.9845093586901592086, 1.000000000000000000, 0.9238795325112867385, 1.000000000000000000, 0.9238795325112867385, 1.000000000000000000, 0.9238795325112867385, 1.000000000000000000, 0.9277451222090459249, 0.9926614294311060238 ) ) 
 REPRESENTATION_ITEM ( '' )  );
#3454=ADVANCED_FACE ( 'NONE', ( #18141 ), #2178, .F. ) ;
#3455=EDGE_LOOP ( 'NONE', ( #5787, #20580, #7887, #11727 ) ) ;
#3456=CARTESIAN_POINT ( 'NONE',  ( -1.534364324400819823, 49.45957383111225170, 93.44516862097951559 ) ) ;
#3457=CARTESIAN_POINT ( 'NONE',  ( 3.816979860036839423, 48.22126577608943876, 92.57632317950277923 ) ) ;
#3459=ORIENTED_EDGE ( 'NONE', *, *, #1313, .T. ) ;
#3460=CARTESIAN_POINT ( 'NONE',  ( -5.784195910403845176, 44.99242805365518194, 96.03933880123796030 ) ) ;
#3466=CARTESIAN_POINT ( 'NONE',  ( 1.256812508749381774, 49.74246873332880625, 93.61746379953098085 ) ) ;
#3472=ORIENTED_EDGE ( 'NONE', *, *, #5066, .F. ) ;
#3477=DIRECTION ( 'NONE',  ( 2.838338907332122006E-16, -1.000000000000000000, 0.000000000000000000 ) ) ;
#3484=CARTESIAN_POINT ( 'NONE',  ( 35.92215374030650565, 40.96218137147972982, 93.55433879953098142 ) ) ;
#3485=DIRECTION ( 'NONE',  ( -0.5735764363510446051, -0.8191520442889927978, -0.000000000000000000 ) ) ;
#3488=VERTEX_POINT ( 'NONE', #17924 ) ;
#3496=DIRECTION ( 'NONE',  ( 1.000000000000000000, 0.000000000000000000, 0.000000000000000000 ) ) ;
#3498=CARTESIAN_POINT ( 'NONE',  ( 5.611423337425062385, 41.22389019960463230, 93.92996380123805977 ) ) ;
#3500=DIRECTION ( 'NONE',  ( 0.000000000000000000, 0.000000000000000000, -1.000000000000000000 ) ) ;
#3501=LINE ( 'NONE', #8081, #11505 ) ;
#3502=CARTESIAN_POINT ( 'NONE',  ( 5.611423337425062385, 41.22389019960463230, 93.92996380123798872 ) ) ;
#3503=CARTESIAN_POINT ( 'NONE',  ( -0.3080929418689875576, 37.85583172076933778, 91.19558880123798872 ) ) ;
#3507=EDGE_CURVE ( 'NONE', #12731, #1203, #1310, .T. ) ;
#3523=VECTOR ( 'NONE', #20858, 1000.000000000000000 ) ;
#3526=CARTESIAN_POINT ( 'NONE',  ( -3.943187491250720544, 40.73580453397070755, 95.64871380294496817 ) ) ;
#3528=CARTESIAN_POINT ( 'NONE',  ( 6.198496396448986090, 45.68315280215533392, 90.49246380123798872 ) ) ;
#3529=B_SPLINE_CURVE_WITH_KNOTS ( 'NONE', 3,
 ( #11680, #3365, #19940, #19536, #1983, #1884 ),
 .UNSPECIFIED., .F., .F.,
 ( 4, 2, 4 ),
 ( 0.000000000000000000, 0.001391245437276853120, 0.002782490874553706240 ),
 .UNSPECIFIED. ) ;
#3537=CARTESIAN_POINT ( 'NONE',  ( 4.454345183533989783, 39.79502090995749342, 90.27410581162071423 ) ) ;
#3538=DIRECTION ( 'NONE',  ( -1.193617070626243484E-16, -1.000000000000000000, -0.000000000000000000 ) ) ;
#3540=CARTESIAN_POINT ( 'NONE',  ( 24.32215374030650068, 44.16218137147968292, 87.05433879953099563 ) ) ;
#3541=CARTESIAN_POINT ( 'NONE',  ( 1.514255888186003762, 51.36218137147968577, 83.03825919817350609 ) ) ;
#3547=VERTEX_POINT ( 'NONE', #16960 ) ;
#3550=EDGE_CURVE ( 'NONE', #15252, #16139, #2699, .T. ) ;
#3558=CARTESIAN_POINT ( 'NONE',  ( 8.722153740306486824, 36.96218137147968719, 95.05433879953098142 ) ) ;
#3559=DIRECTION ( 'NONE',  ( -5.595882180570345180E-16, 1.000000000000000000, 0.000000000000000000 ) ) ;
#3563=CARTESIAN_POINT ( 'NONE',  ( 5.544968037009670780, 45.50804040601273925, 95.88308879953100927 ) ) ;
#3564=VERTEX_POINT ( 'NONE', #2389 ) ;
#3576=( BOUNDED_CURVE ( )  B_SPLINE_CURVE ( 2, ( #15756, #1172, #19040, #4452, #10972 ),
 .UNSPECIFIED., .F., .F. ) 
 B_SPLINE_CURVE_WITH_KNOTS ( ( 3, 2, 3 ),
 ( 0.3083811345117428160, 0.3250000000000000111, 0.3333811345117426717 ),
 .UNSPECIFIED. ) 
 CURVE ( )  GEOMETRIC_REPRESENTATION_ITEM ( )  RATIONAL_B_SPLINE_CURVE ( ( 0.9660722070828657859, 0.9493985675960727733, 1.000000000000000000, 0.9744809649152144093, 0.9660722070828662300 ) ) 
 REPRESENTATION_ITEM ( '' )  );
#3582=ORIENTED_EDGE ( 'NONE', *, *, #15869, .T. ) ;
#3586=CARTESIAN_POINT ( 'NONE',  ( -5.784195910403845176, 44.99242805365518194, 94.78933880123798872 ) ) ;
#3589=CARTESIAN_POINT ( 'NONE',  ( -2.500166695032102204, 48.49377146048119158, 94.97752763193327041 ) ) ;
#3597=PRODUCT ( 'Main Case', 'Main Case', '', ( #13783 ) ) ;
#3599=CARTESIAN_POINT ( 'NONE',  ( 1.514255888186003984, 52.36218137147968577, 83.03825919817350609 ) ) ;
#3601=CARTESIAN_POINT ( 'NONE',  ( 5.611423337425062385, 41.22389019960463230, 90.17996380123798872 ) ) ;
#3602=CARTESIAN_POINT ( 'NONE',  ( -0.9988176903691428077, 49.83852402762217082, 90.64871380123798872 ) ) ;
#3605=EDGE_CURVE ( 'NONE', #8675, #13055, #15694, .T. ) ;
#3608=CARTESIAN_POINT ( 'NONE',  ( 4.394343283833276992, 39.11584570990505938, 94.00808880123797451 ) ) ;
#3612=CARTESIAN_POINT ( 'NONE',  ( 2.722153740306499703, 47.73989013547934945, 50.15433879953098995 ) ) ;
#3621=AXIS2_PLACEMENT_3D ( 'NONE', #19655, #1808, #8288 ) ;
#3623=ORIENTED_EDGE ( 'NONE', *, *, #371, .T. ) ;
#3624=CARTESIAN_POINT ( 'NONE',  ( -5.784195910403845176, 44.99242805365518194, 92.13308880123798872 ) ) ;
#3626=EDGE_CURVE ( 'NONE', #14613, #17415, #4283, .T. ) ;
#3627=CARTESIAN_POINT ( 'NONE',  ( 4.454354847297358866, 39.79502961122975790, 90.27410626197791998 ) ) ;
#3639=CARTESIAN_POINT ( 'NONE',  ( 4.199109002476567376, 47.83913663364971569, 94.73786078214052964 ) ) ;
#3644=AXIS2_PLACEMENT_3D ( 'NONE', #1179, #1072, #17452 ) ;
#3645=EDGE_LOOP ( 'NONE', ( #3663, #19723, #20216, #18662 ) ) ;
#3657=EDGE_CURVE ( 'NONE', #17415, #468, #14604, .T. ) ;
#3660=CARTESIAN_POINT ( 'NONE',  ( 10.77494014480653917, 42.96218137147968008, 61.40715055817103263 ) ) ;
#3661=CARTESIAN_POINT ( 'NONE',  ( -2.077846259693550746, 39.65884927180063357, 96.66433879953098085 ) ) ;
#3662=CARTESIAN_POINT ( 'NONE',  ( -4.500660556396669065, 42.81632233694663370, 96.50808879953099506 ) ) ;
#3663=ORIENTED_EDGE ( 'NONE', *, *, #11832, .F. ) ;
#3667=LINE ( 'NONE', #18042, #10151 ) ;
#3668=CARTESIAN_POINT ( 'NONE',  ( 35.92215374030650565, 51.36218137147967866, 45.55433879953098852 ) ) ;
#3671=CARTESIAN_POINT ( 'NONE',  ( 4.394343283833276992, 39.11584570990505938, 95.25808880123800293 ) ) ;
#3683=DIRECTION ( 'NONE',  ( 0.000000000000000000, -1.000000000000000000, 0.000000000000000000 ) ) ;
#3684=DIRECTION ( 'NONE',  ( -0.000000000000000000, -0.000000000000000000, -1.000000000000000000 ) ) ;
#3686=ORIENTED_EDGE ( 'NONE', *, *, #10607, .T. ) ;
#3694=CARTESIAN_POINT ( 'NONE',  ( -5.368445182934982185, 36.96218137147968008, 93.55433879953098142 ) ) ;
#3699=CARTESIAN_POINT ( 'NONE',  ( -0.3080929418689875576, 37.85583172076933778, 92.44558880123798872 ) ) ;
#3700=AXIS2_PLACEMENT_3D ( 'NONE', #15846, #1582, #6455 ) ;
#3706=DIRECTION ( 'NONE',  ( -1.000000000000000000, 1.193617070626243484E-16, 0.000000000000000000 ) ) ;
#3708=CARTESIAN_POINT ( 'NONE',  ( 5.568489401881125289, 48.03437091500646261, 94.32058880123798872 ) ) ;
#3716=AXIS2_PLACEMENT_3D ( 'NONE', #1687, #14349, #15951 ) ;
#3718=CYLINDRICAL_SURFACE ( 'NONE', #16203, 4.199999999999999289 ) ;
#3719=DIRECTION ( 'NONE',  ( -1.402518428993831676E-16, 1.000000000000000000, 0.000000000000000000 ) ) ;
#3720=EDGE_LOOP ( 'NONE', ( #4159, #8568, #15375, #20223 ) ) ;
#3726=CARTESIAN_POINT ( 'NONE',  ( 3.948530577815480225, 39.69684013992245752, 93.46121380294496817 ) ) ;
#3728=CARTESIAN_POINT ( 'NONE',  ( 1.352400422481993658, 50.46853102219002096, 94.32058880123798872 ) ) ;
#3729=VECTOR ( 'NONE', #16359, 1000.000000000000227 ) ;
#3730=AXIS2_PLACEMENT_3D ( 'NONE', #13744, #765, #17048 ) ;
#3732=EDGE_LOOP ( 'NONE', ( #13113, #6411, #20589, #12939 ) ) ;
#3733=DIRECTION ( 'NONE',  ( 0.000000000000000000, 0.000000000000000000, 1.000000000000000000 ) ) ;
#3734=VERTEX_POINT ( 'NONE', #10256 ) ;
#3737=CARTESIAN_POINT ( 'NONE',  ( -4.524181921268124462, 40.28999182795290324, 91.03933880123798872 ) ) ;
#3738=ORIENTED_EDGE ( 'NONE', *, *, #12768, .F. ) ;
#3741=CARTESIAN_POINT ( 'NONE',  ( 35.92215374030650565, 36.96218137147968719, 92.39963826115175038 ) ) ;
#3745=EDGE_CURVE ( 'NONE', #6639, #15290, #20319, .T. ) ;
#3761=DIRECTION ( 'NONE',  ( 0.000000000000000000, -1.000000000000000000, 0.000000000000000000 ) ) ;
#3763=CARTESIAN_POINT ( 'NONE',  ( -4.500660556396669065, 42.81632233694663370, 94.00808879953098085 ) ) ;
#3764=CARTESIAN_POINT ( 'NONE',  ( 4.987494971863720927, 47.58855820898865829, 93.46121379953098085 ) ) ;
#3769=DIRECTION ( 'NONE',  ( -0.000000000000000000, -0.000000000000000000, 1.000000000000000000 ) ) ;
#3789=ORIENTED_EDGE ( 'NONE', *, *, #591, .F. ) ;
#3790=AXIS2_PLACEMENT_3D ( 'NONE', #20522, #9267, #15757 ) ;
#3791=DIRECTION ( 'NONE',  ( -3.942553354492745503E-16, 1.000000000000000000, 0.000000000000000000 ) ) ;
#3793=CARTESIAN_POINT ( 'NONE',  ( 1.352400422481993658, 50.46853102219002096, 95.72683880123798872 ) ) ;
#3803=DIRECTION ( 'NONE',  ( 1.000000000000000000, 0.000000000000000000, 0.000000000000000000 ) ) ;
#3804=CYLINDRICAL_SURFACE ( 'NONE', #940, 6.200000000000000178 ) ;
#3812=CARTESIAN_POINT ( 'NONE',  ( 6.828503391016846891, 43.33193468930419101, 91.50808880123798872 ) ) ;
#3818=DIRECTION ( 'NONE',  ( -1.000000000000000000, 9.340818716798192921E-14, 0.000000000000000000 ) ) ;
#3819=DIRECTION ( 'NONE',  ( 1.000000000000000000, -0.000000000000000000, -0.000000000000000000 ) ) ;
#3821=CARTESIAN_POINT ( 'NONE',  ( 4.613683346302097199, 40.84891852973634485, 90.69696562749766144 ) ) ;
#3822=VECTOR ( 'NONE', #20090, 1000.000000000000000 ) ;
#3823=FACE_OUTER_BOUND ( 'NONE', #17618, .T. ) ;
#3835=CARTESIAN_POINT ( 'NONE',  ( 4.987494971863720927, 47.58855820898865829, 92.52371380294498238 ) ) ;
#3839=CARTESIAN_POINT ( 'NONE',  ( 4.394343283833276992, 39.11584570990505938, 93.85183880123797451 ) ) ;
#3845=CARTESIAN_POINT ( 'NONE',  ( -0.9988176903691428077, 49.83852402762217082, 93.14871380123798872 ) ) ;
#3858=DIRECTION ( 'NONE',  ( 0.000000000000000000, 1.734723475976787531E-14, -1.000000000000000000 ) ) ;
#3869=CARTESIAN_POINT ( 'NONE',  ( 1.256812508749381774, 49.74246873332880625, 94.86746379953099506 ) ) ;
#3870=CARTESIAN_POINT ( 'NONE',  ( 4.987494971863720927, 47.58855820898865829, 94.71121379953099506 ) ) ;
#3871=VERTEX_POINT ( 'NONE', #6928 ) ;
#3879=CARTESIAN_POINT ( 'NONE',  ( -4.567115856812060670, 47.10047254335474065, 94.71121380123797451 ) ) ;
#3882=FACE_OUTER_BOUND ( 'NONE', #7075, .T. ) ;
#3884=ADVANCED_FACE ( 'NONE', ( #17898, #18636 ), #8967, .T. ) ;
#3885=CARTESIAN_POINT ( 'NONE',  ( 5.568489401881125289, 48.03437091500646261, 90.41433880123798872 ) ) ;
#3886=EDGE_CURVE ( 'NONE', #5474, #8207, #12372, .T. ) ;
#3897=CARTESIAN_POINT ( 'NONE',  ( -3.350035803220276609, 49.20851703305431357, 95.88308880123798872 ) ) ;
#3906=DIRECTION ( 'NONE',  ( -0.000000000000000000, 1.000000000000000000, -0.000000000000000000 ) ) ;
#3907=CARTESIAN_POINT ( 'NONE',  ( 11.22215374030649926, 42.96218137147968008, 77.40433879953098995 ) ) ;
#3909=CARTESIAN_POINT ( 'NONE',  ( -0.08603609158598878037, 38.30449681981696841, 92.55433879953098142 ) ) ;
#3912=CARTESIAN_POINT ( 'NONE',  ( -2.904223097202481174, 48.62752260303690122, 92.83621380294498238 ) ) ;
#3914=ORIENTED_EDGE ( 'NONE', *, *, #2067, .F. ) ;
#3915=EDGE_CURVE ( 'NONE', #6086, #19935, #5550, .T. ) ;
#3917=EDGE_CURVE ( 'NONE', #5383, #10416, #7463, .T. ) ;
#3922=CARTESIAN_POINT ( 'NONE',  ( -4.524181921268124462, 40.28999182795290324, 96.19558880123798872 ) ) ;
#3936=CARTESIAN_POINT ( 'NONE',  ( -2.077846259693550746, 39.65884927180063357, 91.97683880294496817 ) ) ;
#3941=CARTESIAN_POINT ( 'NONE',  ( 2.043125170982144745, 38.48583871533720213, 93.77371380123798872 ) ) ;
#3948=CARTESIAN_POINT ( 'NONE',  ( -0.2125050281363792815, 38.58189400963055959, 94.55496380294496817 ) ) ;
#3949=ORIENTED_EDGE ( 'NONE', *, *, #7658, .T. ) ;
#3954=LINE ( 'NONE', #15357, #17249 ) ;
#3960=EDGE_CURVE ( 'NONE', #14953, #20498, #3403, .T. ) ;
#3969=ORIENTED_EDGE ( 'NONE', *, *, #16127, .T. ) ;
#3971=CARTESIAN_POINT ( 'NONE',  ( -4.500660556396669065, 42.81632233694663370, 96.50808879953099506 ) ) ;
#3972=CARTESIAN_POINT ( 'NONE',  ( -5.058133621542618030, 44.89684013992257405, 91.42996379953099506 ) ) ;
#3973=ORIENTED_EDGE ( 'NONE', *, *, #16355, .F. ) ;
#3975=CARTESIAN_POINT ( 'NONE',  ( 3.460444912181559474, 49.25145096859824889, 93.14871380123798872 ) ) ;
#3979=CARTESIAN_POINT ( 'NONE',  ( -3.943187491250720544, 40.73580453397070755, 91.58621379953098085 ) ) ;
#3982=CARTESIAN_POINT ( 'NONE',  ( 3.460444912181559474, 49.25145096859824889, 95.64871380123798872 ) ) ;
#3986=DIRECTION ( 'NONE',  ( 1.000000000000000000, 1.402518428993831676E-16, 0.000000000000000000 ) ) ;
#3987=CARTESIAN_POINT ( 'NONE',  ( 6.198496396448986090, 45.68315280215533392, 91.58621380123798872 ) ) ;
#3990=EDGE_CURVE ( 'NONE', #16241, #20542, #15669, .T. ) ;
#3995=ORIENTED_EDGE ( 'NONE', *, *, #20174, .F. ) ;
#4000=DIRECTION ( 'NONE',  ( -0.7071067811865435759, 0.7071067811865515695, 0.000000000000000000 ) ) ;
#4001=CARTESIAN_POINT ( 'NONE',  ( -4.524181921268124462, 40.28999182795290324, 96.19558880123798872 ) ) ;
#4005=VERTEX_POINT ( 'NONE', #16081 ) ;
#4009=CARTESIAN_POINT ( 'NONE',  ( 2.263363662449282110, 49.77488197367689793, 93.03606768333816035 ) ) ;
#4014=CARTESIAN_POINT ( 'NONE',  ( 2.196363144981350768, 38.51593444236233665, 92.55433879953095300 ) ) ;
#4015=CARTESIAN_POINT ( 'NONE',  ( -3.943187491250720544, 40.73580453397070755, 94.39871380294499659 ) ) ;
#4016=CARTESIAN_POINT ( 'NONE',  ( -2.904223097202481174, 48.62752260303690122, 91.58621380294496817 ) ) ;
#4024=CARTESIAN_POINT ( 'NONE',  ( 1.352400422481993658, 50.46853102219002096, 93.22683880123798872 ) ) ;
#4031=ORIENTED_EDGE ( 'NONE', *, *, #16018, .T. ) ;
#4036=DIRECTION ( 'NONE',  ( -0.000000000000000000, -1.000000000000000000, -0.000000000000000000 ) ) ;
#4037=CARTESIAN_POINT ( 'NONE',  ( -1.219056181852248066, 49.77488197367201650, 94.56237966814981633 ) ) ;
#4044=DIRECTION ( 'NONE',  ( -1.334402673828313339E-16, -1.619179559944692391E-32, 1.000000000000000000 ) ) ;
#4046=ORIENTED_EDGE ( 'NONE', *, *, #2595, .T. ) ;
#4047=DIRECTION ( 'NONE',  ( 1.000000000000000000, 0.000000000000000000, 0.000000000000000000 ) ) ;
#4052=CARTESIAN_POINT ( 'NONE',  ( -4.500660556396669065, 42.81632233694663370, 95.57058880294496817 ) ) ;
#4061=EDGE_CURVE ( 'NONE', #16593, #18224, #20739, .T. ) ;
#4062=DIRECTION ( 'NONE',  ( 0.000000000000000000, 0.000000000000000000, 1.000000000000000000 ) ) ;
#4070=PLANE ( 'NONE',  #10591 ) ;
#4072=LINE ( 'NONE', #1206, #7069 ) ;
#4074=LINE ( 'NONE', #788, #2454 ) ;
#4081=CARTESIAN_POINT ( 'NONE',  ( -3.943187491250720544, 40.73580453397070755, 95.33621379953099506 ) ) ;
#4083=ORIENTED_EDGE ( 'NONE', *, *, #16747, .T. ) ;
#4084=CARTESIAN_POINT ( 'NONE',  ( -0.9988176903691428077, 49.83852402762217082, 93.30496380123798872 ) ) ;
#4087=CARTESIAN_POINT ( 'NONE',  ( -7.677846259693483333, 47.36218137147966445, 93.55433879953098142 ) ) ;
#4088=ORIENTED_EDGE ( 'NONE', *, *, #19493, .T. ) ;
#4090=CARTESIAN_POINT ( 'NONE',  ( 3.460444912181559474, 49.25145096859824889, 93.14871380123798872 ) ) ;
#4100=CARTESIAN_POINT ( 'NONE',  ( -4.477846259693498254, 51.36218137147968577, 53.35433879953099989 ) ) ;
#4105=CARTESIAN_POINT ( 'NONE',  ( -5.677846259693490438, 44.16218137147969003, 92.55433879953098142 ) ) ;
#4106=CARTESIAN_POINT ( 'NONE',  ( 5.146043734657006041, 40.41782908280415398, 90.30634084312077903 ) ) ;
#4109=VECTOR ( 'NONE', #7880, 1000.000000000000000 ) ;
#4117=DIRECTION ( 'NONE',  ( 0.8191520442889931308, 0.5735764363510443831, 1.093078678171161523E-16 ) ) ;
#4119=CARTESIAN_POINT ( 'NONE',  ( -5.784195910403845176, 44.99242805365518194, 92.13308880123798872 ) ) ;
#4122=CARTESIAN_POINT ( 'NONE',  ( -0.2125050281363792815, 38.58189400963055959, 93.30496380294501080 ) ) ;
#4123=EDGE_CURVE ( 'NONE', #468, #7741, #4471, .T. ) ;
#4130=FACE_BOUND ( 'NONE', #4588, .T. ) ;
#4131=LINE ( 'NONE', #18288, #9261 ) ;
#4133=CARTESIAN_POINT ( 'NONE',  ( 4.454345183533989783, 39.79502090995749342, 90.27410581162071423 ) ) ;
#4134=DIRECTION ( 'NONE',  ( -0.000000000000000000, -0.000000000000000000, -1.000000000000000000 ) ) ;
#4139=ORIENTED_EDGE ( 'NONE', *, *, #2723, .T. ) ;
#4141=VECTOR ( 'NONE', #17010, 1000.000000000000000 ) ;
#4144=LINE ( 'NONE', #5953, #1109 ) ;
#4146=CARTESIAN_POINT ( 'NONE',  ( -4.567115856812060670, 47.10047254335474065, 94.71121380123797451 ) ) ;
#4147=CARTESIAN_POINT ( 'NONE',  ( -4.898948001865909063, 44.60983979649643771, 95.05433879953105247 ) ) ;
#4149=CARTESIAN_POINT ( 'NONE',  ( 4.987494971863720927, 47.58855820898865829, 93.77371380294498238 ) ) ;
#4150=CARTESIAN_POINT ( 'NONE',  ( -0.9988176903691428077, 49.83852402762217082, 93.14871380123798872 ) ) ;
#4152=EDGE_CURVE ( 'NONE', #10420, #14607, #7990, .T. ) ;
#4154=DIRECTION ( 'NONE',  ( 1.000000000000000000, -0.000000000000000000, -0.000000000000000000 ) ) ;
#4159=ORIENTED_EDGE ( 'NONE', *, *, #3250, .F. ) ;
#4163=ORIENTED_EDGE ( 'NONE', *, *, #8621, .T. ) ;
#4165=CARTESIAN_POINT ( 'NONE',  ( -4.567115856812060670, 47.10047254335474065, 90.80496380123797451 ) ) ;
#4166=ORIENTED_EDGE ( 'NONE', *, *, #10308, .T. ) ;
#4168=CARTESIAN_POINT ( 'NONE',  ( -0.2125050281363792815, 38.58189400963056670, 94.24246379953099506 ) ) ;
#4173=ORIENTED_EDGE ( 'NONE', *, *, #20241, .F. ) ;
#4185=ORIENTED_EDGE ( 'NONE', *, *, #8470, .T. ) ;
#4186=EDGE_CURVE ( 'NONE', #8801, #4661, #4776, .T. ) ;
#4191=CARTESIAN_POINT ( 'NONE',  ( -3.943187491250720544, 40.73580453397070755, 91.58621379953098085 ) ) ;
#4193=CARTESIAN_POINT ( 'NONE',  ( 3.460444912181559474, 49.25145096859824889, 91.89871380123798872 ) ) ;
#4214=DIRECTION ( 'NONE',  ( 1.000000000000000000, 0.000000000000000000, -0.000000000000000000 ) ) ;
#4215=CARTESIAN_POINT ( 'NONE',  ( -4.524181921268124462, 40.28999182795290324, 96.03933880123798872 ) ) ;
#4225=LINE ( 'NONE', #13806, #16776 ) ;
#4229=CARTESIAN_POINT ( 'NONE',  ( -5.058133621542618030, 44.89684013992257405, 92.99246380294498238 ) ) ;
#4233=CARTESIAN_POINT ( 'NONE',  ( -3.154801521863568325, 47.83913663364971569, 92.55433879953098142 ) ) ;
#4235=CARTESIAN_POINT ( 'NONE',  ( 5.146040402138061687, 40.41782331071202350, 90.30634062920465510 ) ) ;
#4236=CARTESIAN_POINT ( 'NONE',  ( -2.416137431568557314, 39.07291177436112406, 93.77371380123797451 ) ) ;
#4242=LINE ( 'NONE', #20203, #6860 ) ;
#4248=CARTESIAN_POINT ( 'NONE',  ( 5.568489401881125289, 48.03437091500646261, 92.91433880123798872 ) ) ;
#4253=CARTESIAN_POINT ( 'NONE',  ( 11.22215374030649926, 39.96218137147969429, 80.55433879953099563 ) ) ;
#4260=CARTESIAN_POINT ( 'NONE',  ( -4.500660556396669065, 42.81632233694663370, 91.82058880294496817 ) ) ;
#4263=CARTESIAN_POINT ( 'NONE',  ( -3.943187491250720544, 40.73580453397070755, 94.08621379953100927 ) ) ;
#4265=CYLINDRICAL_SURFACE ( 'NONE', #1924, 5.199999999999999289 ) ;
#4272=CARTESIAN_POINT ( 'NONE',  ( 30.92220646078100188, 42.76218137147968434, 62.80715055817104542 ) ) ;
#4274=CARTESIAN_POINT ( 'NONE',  ( 31.07218010054375412, 42.76218137147968434, 70.80574467885102763 ) ) ;
#4276=LINE ( 'NONE', #1105, #5033 ) ;
#4278=FACE_OUTER_BOUND ( 'NONE', #10735, .T. ) ;
#4281=ORIENTED_EDGE ( 'NONE', *, *, #3886, .F. ) ;
#4283=LINE ( 'NONE', #7276, #18686 ) ;
#4284=CARTESIAN_POINT ( 'NONE',  ( 3.460444912181559474, 49.25145096859824889, 94.39871380123798872 ) ) ;
#4285=DIRECTION ( 'NONE',  ( 1.000000000000000000, -0.000000000000000000, -0.000000000000000000 ) ) ;
#4288=CARTESIAN_POINT ( 'NONE',  ( 5.611423337425062385, 41.22389019960463230, 94.08621380123797451 ) ) ;
#4297=CARTESIAN_POINT ( 'NONE',  ( -4.524181921268124462, 40.28999182795290324, 91.19558880123797451 ) ) ;
#4305=LINE ( 'NONE', #4611, #5554 ) ;
#4314=CARTESIAN_POINT ( 'NONE',  ( -2.416137431568557314, 39.07291177436112406, 96.11746380123797451 ) ) ;
#4315=ORIENTED_EDGE ( 'NONE', *, *, #10962, .F. ) ;
#4328=CARTESIAN_POINT ( 'NONE',  ( -5.784195910403845176, 44.99242805365518194, 91.03933880123798872 ) ) ;
#4332=CARTESIAN_POINT ( 'NONE',  ( 3.122153740306552905, 48.66551347115873227, 93.85183880294498238 ) ) ;
#4345=LINE ( 'NONE', #10870, #551 ) ;
#4346=LINE ( 'NONE', #15856, #1611 ) ;
#4349=LINE ( 'NONE', #7664, #6358 ) ;
#4351=FACE_BOUND ( 'NONE', #6204, .T. ) ;
#4354=CARTESIAN_POINT ( 'NONE',  ( -5.784195910403845176, 44.99242805365518194, 92.13308880123798872 ) ) ;
#4357=ORIENTED_EDGE ( 'NONE', *, *, #12972, .F. ) ;
#4362=CARTESIAN_POINT ( 'NONE',  ( 5.025485839985549319, 41.56218137147963887, 91.03933880294498238 ) ) ;
#4364=DIRECTION ( 'NONE',  ( 1.621236893436268647E-16, 2.273814620809075225E-32, -1.000000000000000000 ) ) ;
#4367=CARTESIAN_POINT ( 'NONE',  ( 0.5221537403065019678, 51.36218137147968577, 87.21440135111343750 ) ) ;
#4368=LINE ( 'NONE', #12683, #994 ) ;
#4369=CARTESIAN_POINT ( 'NONE',  ( 30.92220646078100188, 36.96218137147968008, 29.55715055817103476 ) ) ;
#4376=LINE ( 'NONE', #4272, #13159 ) ;
#4377=PLANE ( 'NONE',  #10494 ) ;
#4378=CARTESIAN_POINT ( 'NONE',  ( 1.352400422481993658, 50.46853102219002096, 95.57058880123798872 ) ) ;
#4388=CARTESIAN_POINT ( 'NONE',  ( -4.567115856812060670, 47.10047254335474065, 94.71121380123797451 ) ) ;
#4389=CARTESIAN_POINT ( 'NONE',  ( -1.219056181852248066, 49.77488197367201650, 94.56237966814981633 ) ) ;
#4390=ORIENTED_EDGE ( 'NONE', *, *, #11294, .T. ) ;
#4396=EDGE_CURVE ( 'NONE', #2580, #19160, #10342, .T. ) ;
#4405=CARTESIAN_POINT ( 'NONE',  ( 5.596449423573146120, 45.91824161709900665, 95.05433879953102405 ) ) ;
#4411=EDGE_CURVE ( 'NONE', #5376, #1084, #7331, .T. ) ;
#4412=EDGE_CURVE ( 'NONE', #12733, #13051, #20089, .T. ) ;
#4417=VECTOR ( 'NONE', #9984, 1000.000000000000000 ) ;
#4424=CARTESIAN_POINT ( 'NONE',  ( -2.416137431568557314, 39.07291177436112406, 94.86746380123797451 ) ) ;
#4425=EDGE_CURVE ( 'NONE', #15803, #5518, #11239, .T. ) ;
#4438=EDGE_LOOP ( 'NONE', ( #14208, #5596, #117, #16232, #13575, #1535, #19184, #491 ) ) ;
#4442=CARTESIAN_POINT ( 'NONE',  ( 1.352400422481993658, 50.46853102219002096, 95.57058880123798872 ) ) ;
#4445=LINE ( 'NONE', #10961, #17743 ) ;
#4446=SURFACE_STYLE_USAGE ( .BOTH. , #17331 ) ;
#4448=PLANE ( 'NONE',  #4472 ) ;
#4449=ADVANCED_FACE ( 'NONE', ( #3823 ), #5627, .T. ) ;
#4452=CARTESIAN_POINT ( 'NONE',  ( 5.722153740306817227, 44.84677435893293307, 94.60825776475003579 ) ) ;
#4463=PLANE ( 'NONE',  #13389 ) ;
#4464=VECTOR ( 'NONE', #15325, 1000.000000000000000 ) ;
#4465=ORIENTED_EDGE ( 'NONE', *, *, #10411, .T. ) ;
#4471=LINE ( 'NONE', #17663, #12266 ) ;
#4472=AXIS2_PLACEMENT_3D ( 'NONE', #7436, #6044, #10967 ) ;
#4473=CARTESIAN_POINT ( 'NONE',  ( 1.868012774839550749, 39.13936707477651566, 92.13308880294498238 ) ) ;
#4475=LINE ( 'NONE', #19550, #11682 ) ;
#4486=CARTESIAN_POINT ( 'NONE',  ( -5.154188915835984375, 42.64120994080404614, 94.71121380123797451 ) ) ;
#4496=CARTESIAN_POINT ( 'NONE',  ( 2.043125170982144745, 38.48583871533720213, 92.67996380123798872 ) ) ;
#4497=CARTESIAN_POINT ( 'NONE',  ( 10.77494014480653917, 42.96218137147968008, 58.20715055817105110 ) ) ;
#4508=CARTESIAN_POINT ( 'NONE',  ( 6.828503391016846891, 43.33193468930419101, 91.66433880123796030 ) ) ;
#4509=ORIENTED_EDGE ( 'NONE', *, *, #2570, .T. ) ;
#4511=CARTESIAN_POINT ( 'NONE',  ( 5.200945329014118990, 40.92307955209284387, 95.05433879953095300 ) ) ;
#4516=LINE ( 'NONE', #9017, #20107 ) ;
#4518=ORIENTED_EDGE ( 'NONE', *, *, #7260, .T. ) ;
#4521=ORIENTED_EDGE ( 'NONE', *, *, #9457, .F. ) ;
#4523=LINE ( 'NONE', #11040, #12978 ) ;
#4524=CARTESIAN_POINT ( 'NONE',  ( 5.611423337425062385, 41.22389019960463230, 92.83621380123797451 ) ) ;
#4537=EDGE_CURVE ( 'NONE', #13701, #1203, #463, .T. ) ;
#4538=CIRCLE ( 'NONE', #15770, 4.199999999999999289 ) ;
#4540=DIRECTION ( 'NONE',  ( -1.193617070626243484E-16, -1.000000000000000000, -0.000000000000000000 ) ) ;
#4543=CARTESIAN_POINT ( 'NONE',  ( -0.3080929418689875576, 37.85583172076933778, 93.85183880123797451 ) ) ;
#4546=CARTESIAN_POINT ( 'NONE',  ( 5.544968037009670780, 45.50804040601273925, 89.94558880294498238 ) ) ;
#4551=CARTESIAN_POINT ( 'NONE',  ( 11.22215374030649926, 42.76218137147968434, 70.80574467885102763 ) ) ;
#4553=CARTESIAN_POINT ( 'NONE',  ( 3.460444912181559474, 49.25145096859824889, 91.89871380123798872 ) ) ;
#4556=CARTESIAN_POINT ( 'NONE',  ( -4.677846259693498432, 44.16218137147969003, 92.70661078214052964 ) ) ;
#4565=ADVANCED_FACE ( 'NONE', ( #3255 ), #163, .F. ) ;
#4571=CARTESIAN_POINT ( 'NONE',  ( 3.122153740306552905, 48.66551347115873227, 93.85183880294498238 ) ) ;
#4575=CARTESIAN_POINT ( 'NONE',  ( 4.199109002476567376, 47.83913663364971569, 93.48786078214052964 ) ) ;
#4582=DIRECTION ( 'NONE',  ( -1.000000000000000000, 4.818676322157797375E-16, 0.000000000000000000 ) ) ;
#4588=EDGE_LOOP ( 'NONE', ( #2849, #15139 ) ) ;
#4590=ORIENTED_EDGE ( 'NONE', *, *, #12438, .F. ) ;
#4592=CARTESIAN_POINT ( 'NONE',  ( -4.524181921268124462, 40.28999182795290324, 92.44558880123798872 ) ) ;
#4603=CARTESIAN_POINT ( 'NONE',  ( -4.531920369308549468, 45.91945145313098209, 92.55433879953098142 ) ) ;
#4604=CARTESIAN_POINT ( 'NONE',  ( 5.146040402138061687, 40.41782331071202350, 90.30634062920465510 ) ) ;
#4606=EDGE_LOOP ( 'NONE', ( #12672, #15087, #12277, #10657 ) ) ;
#4608=CARTESIAN_POINT ( 'NONE',  ( 5.176717291127333809, 46.72077138471917834, 95.05433879953092458 ) ) ;
#4611=CARTESIAN_POINT ( 'NONE',  ( 10.77494014480653561, 42.76218137147968434, 77.40433879953098995 ) ) ;
#4614=VERTEX_POINT ( 'NONE', #6952 ) ;
#4621=LINE ( 'NONE', #1773, #17730 ) ;
#4639=CARTESIAN_POINT ( 'NONE',  ( -5.784195910403845176, 44.99242805365518194, 95.88308880123798872 ) ) ;
#4642=LINE ( 'NONE', #11583, #7899 ) ;
#4645=CIRCLE ( 'NONE', #19259, 0.9921021478795020165 ) ;
#4650=VERTEX_POINT ( 'NONE', #575 ) ;
#4652=EDGE_CURVE ( 'NONE', #17731, #9962, #9972, .T. ) ;
#4656=CARTESIAN_POINT ( 'NONE',  ( -3.981178359372548492, 46.76218137147973408, 93.85183879953099506 ) ) ;
#4661=VERTEX_POINT ( 'NONE', #16865 ) ;
#4665=ADVANCED_FACE ( 'NONE', ( #2283 ), #7928, .T. ) ;
#4672=ORIENTED_EDGE ( 'NONE', *, *, #21006, .T. ) ;
#4680=AXIS2_PLACEMENT_3D ( 'NONE', #8259, #13052, #13364 ) ;
#4682=CARTESIAN_POINT ( 'NONE',  ( -2.416137431568557314, 39.07291177436112406, 96.11746380123797451 ) ) ;
#4693=EDGE_CURVE ( 'NONE', #3176, #14996, #9171, .T. ) ;
#4694=CARTESIAN_POINT ( 'NONE',  ( -5.154188915835984375, 42.64120994080404614, 93.61746380123797451 ) ) ;
#4701=LINE ( 'NONE', #9732, #11302 ) ;
#4702=ORIENTED_EDGE ( 'NONE', *, *, #4061, .F. ) ;
#4707=CARTESIAN_POINT ( 'NONE',  ( 3.693419005614973383, 39.25792614782567114, 95.05433879953100984 ) ) ;
#4725=CARTESIAN_POINT ( 'NONE',  ( -4.524181921268124462, 40.28999182795290324, 93.69558880123798872 ) ) ;
#4729=CARTESIAN_POINT ( 'NONE',  ( 5.544968037009670780, 45.50804040601273925, 93.38308879953099506 ) ) ;
#4735=ORIENTED_EDGE ( 'NONE', *, *, #4411, .F. ) ;
#4736=LINE ( 'NONE', #11995, #217 ) ;
#4737=DIRECTION ( 'NONE',  ( 0.000000000000000000, 0.000000000000000000, 1.000000000000000000 ) ) ;
#4739=CARTESIAN_POINT ( 'NONE',  ( -4.567115856812060670, 47.10047254335474065, 90.96121380123797451 ) ) ;
#4741=CARTESIAN_POINT ( 'NONE',  ( -4.567115856812060670, 47.10047254335474065, 93.30496380123798872 ) ) ;
#4747=CARTESIAN_POINT ( 'NONE',  ( -3.154801521863568325, 47.83913663364971569, 92.86286078555453116 ) ) ;
#4764=COLOUR_RGB ( '', 0.66274510, 0.83137255, 0.94901961) ;
#4769=CARTESIAN_POINT ( 'NONE',  ( -7.677846259693478892, 49.36218137147968577, 93.55433879953098142 ) ) ;
#4771=CYLINDRICAL_SURFACE ( 'NONE', #6473, 5.199999999999999289 ) ;
#4776=LINE ( 'NONE', #11301, #2403 ) ;
#4778=ORIENTED_EDGE ( 'NONE', *, *, #11818, .F. ) ;
#4785=ORIENTED_EDGE ( 'NONE', *, *, #19357, .F. ) ;
#4791=CARTESIAN_POINT ( 'NONE',  ( -5.154188915835984375, 42.64120994080404614, 94.71121380123797451 ) ) ;
#4792=CARTESIAN_POINT ( 'NONE',  ( 4.394343283833276992, 39.11584570990505938, 92.60183880123797451 ) ) ;
#4793=CYLINDRICAL_SURFACE ( 'NONE', #21007, 4.200000000000001066 ) ;
#4796=ADVANCED_FACE ( 'NONE', ( #19355 ), #4771, .F. ) ;
#4797=VECTOR ( 'NONE', #1452, 1000.000000000000114 ) ;
#4805=CARTESIAN_POINT ( 'NONE',  ( -5.784195910403845176, 44.99242805365518194, 94.63308880123798872 ) ) ;
#4807=LINE ( 'NONE', #11327, #19796 ) ;
#4825=CARTESIAN_POINT ( 'NONE',  ( -1.677846259693499542, 44.16218137147969003, 50.15433879953098995 ) ) ;
#4835=CARTESIAN_POINT ( 'NONE',  ( -4.477846259693498254, 36.96218137147968008, 53.35433879953099989 ) ) ;
#4838=CARTESIAN_POINT ( 'NONE',  ( 2.891178777429407099, 49.58011692473793630, 94.41981103945796860 ) ) ;
#4843=CARTESIAN_POINT ( 'NONE',  ( -0.2125050281363792815, 38.58189400963055959, 95.49246379953098085 ) ) ;
#4848=VERTEX_POINT ( 'NONE', #5194 ) ;
#4860=CARTESIAN_POINT ( 'NONE',  ( 11.22215374030649926, 42.96218137147968008, 77.40433879953098995 ) ) ;
#4864=AXIS2_PLACEMENT_3D ( 'NONE', #9476, #19049, #11081 ) ;
#4875=CARTESIAN_POINT ( 'NONE',  ( 4.394343283833276992, 39.11584570990505938, 91.35183880123798872 ) ) ;
#4882=MANIFOLD_SOLID_BREP ( 'Stock-MAS-160-1', #5077 ) ;
#4895=CARTESIAN_POINT ( 'NONE',  ( -5.154188915835984375, 42.64120994080404614, 92.21121380123797451 ) ) ;
#4897=DIRECTION ( 'NONE',  ( 1.402518428993831676E-16, -1.000000000000000000, 0.000000000000000000 ) ) ;
#4901=VERTEX_POINT ( 'NONE', #5837 ) ;
#4906=CARTESIAN_POINT ( 'NONE',  ( 1.352400422481993658, 50.46853102219002096, 94.32058880123798872 ) ) ;
#4913=CARTESIAN_POINT ( 'NONE',  ( 3.873544841512767789, 48.16470079461350906, 93.50578198602111968 ) ) ;
#4916=DIRECTION ( 'NONE',  ( 0.000000000000000000, 0.000000000000000000, -1.000000000000000000 ) ) ;
#4927=VERTEX_POINT ( 'NONE', #1683 ) ;
#4934=DIRECTION ( 'NONE',  ( -1.402518428993831676E-16, 1.000000000000000000, 0.000000000000000000 ) ) ;
#4938=CARTESIAN_POINT ( 'NONE',  ( -3.416655834010613013, 49.09312775492363556, 93.38736517557353523 ) ) ;
#4944=CARTESIAN_POINT ( 'NONE',  ( 3.122153740306552905, 48.66551347115873227, 94.78933879953099506 ) ) ;
#4947=CARTESIAN_POINT ( 'NONE',  ( -3.154801521863568325, 47.83913663364971569, 83.28180655319408743 ) ) ;
#4954=CARTESIAN_POINT ( 'NONE',  ( 5.611423337425062385, 41.22389019960463230, 93.92996380123798872 ) ) ;
#4963=CARTESIAN_POINT ( 'NONE',  ( 11.22215374030650281, 42.96218137147968008, 61.40715055817103263 ) ) ;
#4969=ORIENTED_EDGE ( 'NONE', *, *, #7164, .T. ) ;
#4977=CARTESIAN_POINT ( 'NONE',  ( -1.219056181836355446, 49.77488197367695477, 93.15612966814926210 ) ) ;
#4982=CARTESIAN_POINT ( 'NONE',  ( 6.828503391016846891, 43.33193468930419101, 91.50808880123798872 ) ) ;
#4997=VERTEX_POINT ( 'NONE', #19227 ) ;
#5000=CARTESIAN_POINT ( 'NONE',  ( 3.460444912181559474, 49.25145096859824889, 90.49246380123798872 ) ) ;
#5005=VECTOR ( 'NONE', #17055, 1000.000000000000000 ) ;
#5007=ORIENTED_EDGE ( 'NONE', *, *, #591, .T. ) ;
#5010=ORIENTED_EDGE ( 'NONE', *, *, #5982, .T. ) ;
#5022=DIRECTION ( 'NONE',  ( 1.000000000000000000, 1.402518428993831676E-16, 0.000000000000000000 ) ) ;
#5026=DIRECTION ( 'NONE',  ( 0.000000000000000000, 2.891205793294680792E-16, 1.000000000000000000 ) ) ;
#5033=VECTOR ( 'NONE', #20559, 1000.000000000000000 ) ;
#5039=CARTESIAN_POINT ( 'NONE',  ( -2.500166695032101760, 48.49377146048118448, 93.72752763193321357 ) ) ;
#5041=DIRECTION ( 'NONE',  ( 0.000000000000000000, -2.168404344970984808E-15, -1.000000000000000000 ) ) ;
#5049=DIRECTION ( 'NONE',  ( 0.4999999999999984457, 0.8660254037844394848, -0.000000000000000000 ) ) ;
#5051=ORIENTED_EDGE ( 'NONE', *, *, #19143, .T. ) ;
#5061=( BOUNDED_CURVE ( )  B_SPLINE_CURVE ( 2, ( #17234, #2661, #16923, #8952, #20204, #750, #4146, #13731, #4037 ),
 .UNSPECIFIED., .F., .F. ) 
 B_SPLINE_CURVE_WITH_KNOTS ( ( 3, 2, 2, 2, 3 ),
 ( 0.2030272526279940093, 0.2083266037756280609, 0.2343674292475841914, 0.2604082547195403219, 0.2851266610854426564 ),
 .UNSPECIFIED. ) 
 CURVE ( )  GEOMETRIC_REPRESENTATION_ITEM ( )  RATIONAL_B_SPLINE_CURVE ( ( 0.9753234597498641190, 0.9845093586922131212, 1.000000000000000000, 0.9238795325112867385, 1.000000000000000000, 0.9238795325112867385, 1.000000000000000000, 0.9277451227429492908, 0.9926614284717510950 ) ) 
 REPRESENTATION_ITEM ( '' )  );
#5064=CARTESIAN_POINT ( 'NONE',  ( 31.22215374030650281, 42.76218137147968434, 74.20433879953100131 ) ) ;
#5066=EDGE_CURVE ( 'NONE', #11018, #2442, #7963, .T. ) ;
#5072=LINE ( 'NONE', #4963, #10990 ) ;
#5077=CLOSED_SHELL ( 'NONE', ( #11488, #8970, #11188, #12069, #14384, #270, #4796, #7423, #19235, #15491, #7584, #5385, #14392, #20285, #9668, #17148, #470, #15399, #16111, #16878, #6133, #17165, #7914, #17887, #13260, #16278, #1839, #4665, #16394, #18485, #13002, #16611, #7455, #9478, #11019, #9617, #18507, #9594, #3884, #16098, #10145, #2700, #15361, #12986, #12594, #18710, #15758, #2315, #7961, #11061, #5697, #18318, #16921, #2209, #17297, #3078, #18473, #4449, #20935, #13395, #7221, #12859, #20024, #12619, #8761, #18172, #18683, #1984, #7669, #14270, #4565, #8853, #7811, #3454, #11938, #11721, #7566, #10125, #12125, #15712, #7369, #16396, #3419, #6846, #6921, #5265, #16671, #20926, #2866, #7902, #1447, #7273, #10032, #14903, #16280, #5304, #15745, #15511, #15864, #12840, #18142, #18354, #10796, #14934, #18124, #18059 ) ) ;
#5078=DIRECTION ( 'NONE',  ( 1.000000000000000000, -0.000000000000000000, -0.000000000000000000 ) ) ;
#5079=ORIENTED_EDGE ( 'NONE', *, *, #7004, .F. ) ;
#5086=PLANE ( 'NONE',  #11492 ) ;
#5092=CARTESIAN_POINT ( 'NONE',  ( 5.611423337425062385, 41.22389019960463230, 93.92996380123798872 ) ) ;
#5098=VECTOR ( 'NONE', #10220, 1000.000000000000000 ) ;
#5106=DIRECTION ( 'NONE',  ( -0.000000000000000000, 0.000000000000000000, -1.000000000000000000 ) ) ;
#5111=CARTESIAN_POINT ( 'NONE',  ( 4.394343283833276992, 39.11584570990505938, 91.35183880123798872 ) ) ;
#5113=CARTESIAN_POINT ( 'NONE',  ( -4.524181921268124462, 40.28999182795290324, 94.78933880123798872 ) ) ;
#5115=EDGE_LOOP ( 'NONE', ( #7492, #1098, #2522, #11641 ) ) ;
#5117=VERTEX_POINT ( 'NONE', #8699 ) ;
#5119=CARTESIAN_POINT ( 'NONE',  ( 3.460444912181559474, 49.25145096859824889, 90.64871380123798872 ) ) ;
#5124=DIRECTION ( 'NONE',  ( -1.193617070626243484E-16, -1.000000000000000000, -0.000000000000000000 ) ) ;
#5125=CARTESIAN_POINT ( 'NONE',  ( 31.07218010054375412, 42.96218137147968008, 65.80574467885102763 ) ) ;
#5126=DIRECTION ( 'NONE',  ( -1.334402673828313339E-16, 1.592765810570777996E-32, 1.000000000000000000 ) ) ;
#5135=VECTOR ( 'NONE', #713, 1000.000000000000000 ) ;
#5140=VERTEX_POINT ( 'NONE', #493 ) ;
#5146=PLANE ( 'NONE',  #11288 ) ;
#5147=CARTESIAN_POINT ( 'NONE',  ( -4.500660556396669065, 42.81632233694663370, 92.75808879953098085 ) ) ;
#5154=CARTESIAN_POINT ( 'NONE',  ( 5.025485839985549319, 41.56218137147963887, 94.47683879953099506 ) ) ;
#5158=VERTEX_POINT ( 'NONE', #2199 ) ;
#5160=LINE ( 'NONE', #19636, #18346 ) ;
#5174=CARTESIAN_POINT ( 'NONE',  ( 4.394343283833276992, 39.11584570990505938, 94.00808880123797451 ) ) ;
#5191=CARTESIAN_POINT ( 'NONE',  ( -5.784195910403845176, 44.99242805365518194, 92.13308880123798872 ) ) ;
#5192=CARTESIAN_POINT ( 'NONE',  ( -5.784195910403845176, 44.99242805365518194, 90.88308880123798872 ) ) ;
#5194=CARTESIAN_POINT ( 'NONE',  ( 30.92220646078100188, 42.76218137147968434, 58.20715055817105110 ) ) ;
#5195=AXIS2_PLACEMENT_3D ( 'NONE', #13513, #14508, #19502 ) ;
#5202=CARTESIAN_POINT ( 'NONE',  ( -4.500660556396669065, 42.81632233694663370, 93.07058880294496817 ) ) ;
#5204=VERTEX_POINT ( 'NONE', #14417 ) ;
#5215=CARTESIAN_POINT ( 'NONE',  ( -3.943187491250720544, 40.73580453397070755, 94.39871380294496817 ) ) ;
#5217=CARTESIAN_POINT ( 'NONE',  ( -4.524181921268124462, 40.28999182795290324, 92.28933880123798872 ) ) ;
#5218=CARTESIAN_POINT ( 'NONE',  ( -5.154188915835984375, 42.64120994080404614, 91.11746380123797451 ) ) ;
#5225=CARTESIAN_POINT ( 'NONE',  ( 5.568489401881125289, 48.03437091500646261, 95.41433880123797451 ) ) ;
#5234=EDGE_LOOP ( 'NONE', ( #7443, #19106, #8522, #10518 ) ) ;
#5235=CARTESIAN_POINT ( 'NONE',  ( -3.116943990436417788, 39.65933899544464225, 92.55433879953100984 ) ) ;
#5245=CARTESIAN_POINT ( 'NONE',  ( -7.677846259693480668, 38.96218137147968008, 93.55433879953098142 ) ) ;
#5249=FACE_OUTER_BOUND ( 'NONE', #1326, .T. ) ;
#5250=CARTESIAN_POINT ( 'NONE',  ( -5.058133621542618030, 44.89684013992257405, 93.92996379953099506 ) ) ;
#5259=CARTESIAN_POINT ( 'NONE',  ( -4.524181921268124462, 40.28999182795290324, 96.19558880123798872 ) ) ;
#5260=ORIENTED_EDGE ( 'NONE', *, *, #12972, .T. ) ;
#5265=ADVANCED_FACE ( 'NONE', ( #8137 ), #6637, .T. ) ;
#5268=VERTEX_POINT ( 'NONE', #1767 ) ;
#5275=CARTESIAN_POINT ( 'NONE',  ( -4.524181921268124462, 40.28999182795290324, 93.69558880123800293 ) ) ;
#5280=DIRECTION ( 'NONE',  ( -1.000000000000000000, 1.193617070626243484E-16, 0.000000000000000000 ) ) ;
#5291=CARTESIAN_POINT ( 'NONE',  ( -4.500660556396669065, 42.81632233694663370, 95.57058880294496817 ) ) ;
#5298=DIRECTION ( 'NONE',  ( 1.000000000000000000, -0.000000000000000000, -0.000000000000000000 ) ) ;
#5300=CARTESIAN_POINT ( 'NONE',  ( 1.352400422481993658, 50.46853102219002096, 91.97683880123797451 ) ) ;
#5301=( BOUNDED_SURFACE ( )  B_SPLINE_SURFACE ( 1, 2, ( 
 ( #9726, #1631, #14606, #1847, #6826, #8331, #11531, #13332, #19804, #5225, #8012, #11742, #16626, #14810, #20966, #18216, #6401, #231, #12908, #4805, #16207, #133, #11427, #4906, #8116, #6510, #6610, #13017, #19491, #17900, #3322, #9827, #6929, #20115, #16837, #20215, #5648, #18637, #3845, #447, #15352, #18316, #7139, #8655, #2475, #13433, #547, #8866, #19904, #12157, #7249, #20001, #15137, #5328, #11841, #15242, #17050, #2048, #13845, #20325, #7030, #8544, #15031, #13529, #766, #3737, #8968, #10367, #4165, #10258, #5436, #8754, #16733, #13745, #7354, #11952, #5761, #5551, #15453 ),
 ( #2156, #10472, #4052, #12268, #10580, #18750, #18428, #869, #2255, #658, #2362, #13640, #10688, #12056, #18534, #3948, #16936, #19063, #9179, #2889, #7677, #15978, #15670, #18848, #4571, #5968, #2674, #12571, #1090, #12373, #1192, #1290, #14154, #12468, #14060, #974, #7577, #9070, #2789, #7464, #11093, #5875, #17252, #15559, #7886, #2985, #4473, #9491, #12679, #10994, #4260, #1395, #17151, #2572, #18950, #14259, #20544, #19159, #17561, #10786, #4362, #10888, #17465, #7778, #9389, #14372, #20847, #9290, #13960, #15778, #17359, #20442, #20638, #15873, #6067, #20740, #6175, #6274, #12776 ) ),
 .UNSPECIFIED., .F., .F., .F. ) 
 B_SPLINE_SURFACE_WITH_KNOTS ( ( 2, 2 ),
 ( 3, 2, 2, 2, 2, 2, 2, 2, 2, 2, 2, 2, 2, 2, 2, 2, 2, 2, 2, 2, 2, 2, 2, 2, 2, 2, 2, 2, 2, 2, 2, 2, 2, 2, 2, 2, 2, 2, 2, 3 ),
 ( 0.000000000000000000, 1.000000000000000000 ),
 ( 0.000000000000000000, 0.02500000000000000139, 0.05000000000000000278, 0.07499999999999999722, 0.1000000000000000056, 0.1250000000000000000, 0.1499999999999999944, 0.1749999999999999889, 0.2000000000000000111, 0.2250000000000000056, 0.2500000000000000000, 0.2750000000000000222, 0.2999999999999999889, 0.3250000000000000111, 0.3499999999999999778, 0.3750000000000000000, 0.4000000000000000222, 0.4249999999999999889, 0.4500000000000000111, 0.4749999999999999778, 0.5000000000000000000, 0.5250000000000000222, 0.5500000000000000444, 0.5749999999999999556, 0.5999999999999999778, 0.6250000000000000000, 0.6500000000000000222, 0.6750000000000000444, 0.6999999999999999556, 0.7249999999999999778, 0.7500000000000000000, 0.7750000000000000222, 0.8000000000000000444, 0.8249999999999999556, 0.8499999999999999778, 0.8750000000000000000, 0.9000000000000000222, 0.9250000000000000444, 0.9499999999999999556, 0.9600309957089442348 ),
 .UNSPECIFIED. ) 
 GEOMETRIC_REPRESENTATION_ITEM ( )  RATIONAL_B_SPLINE_SURFACE ( (
 ( 1.000000000000000000, 0.9238795325112867385, 1.000000000000000000, 0.9238795325112867385, 1.000000000000000000, 0.9238795325112867385, 1.000000000000000000, 0.9238795325112867385, 1.000000000000000000, 0.9238795325112867385, 1.000000000000000000, 0.9238795325112867385, 1.000000000000000000, 0.9238795325112867385, 1.000000000000000000, 0.9238795325112867385, 1.000000000000000000, 0.9238795325112867385, 1.000000000000000000, 0.9238795325112867385, 1.000000000000000000, 0.9238795325112867385, 1.000000000000000000, 0.9238795325112867385, 1.000000000000000000, 0.9238795325112867385, 1.000000000000000000, 0.9238795325112867385, 1.000000000000000000, 0.9238795325112867385, 1.000000000000000000, 0.9238795325112867385, 1.000000000000000000, 0.9238795325112867385, 1.000000000000000000, 0.9238795325112867385, 1.000000000000000000, 0.9238795325112867385, 1.000000000000000000, 0.9238795325112867385, 1.000000000000000000, 0.9238795325112867385, 1.000000000000000000, 0.9238795325112867385, 1.000000000000000000, 0.9238795325112867385, 1.000000000000000000, 0.9238795325112867385, 1.000000000000000000, 0.9238795325112867385, 1.000000000000000000, 0.9238795325112867385, 1.000000000000000000, 0.9238795325112867385, 1.000000000000000000, 0.9238795325112867385, 1.000000000000000000, 0.9238795325112867385, 1.000000000000000000, 0.9238795325112867385, 1.000000000000000000, 0.9238795325112867385, 1.000000000000000000, 0.9238795325112867385, 1.000000000000000000, 0.9238795325112867385, 1.000000000000000000, 0.9238795325112867385, 1.000000000000000000, 0.9238795325112867385, 1.000000000000000000, 0.9238795325112867385, 1.000000000000000000, 0.9238795325112867385, 1.000000000000000000, 0.9238795325112867385, 1.000000000000000000, 0.9694574366903154772, 0.9634246591005992677),
 ( 1.000000000000000000, 0.9238795325112867385, 1.000000000000000000, 0.9238795325112867385, 1.000000000000000000, 0.9238795325112867385, 1.000000000000000000, 0.9238795325112867385, 1.000000000000000000, 0.9238795325112867385, 1.000000000000000000, 0.9238795325112867385, 1.000000000000000000, 0.9238795325112867385, 1.000000000000000000, 0.9238795325112867385, 1.000000000000000000, 0.9238795325112867385, 1.000000000000000000, 0.9238795325112867385, 1.000000000000000000, 0.9238795325112867385, 1.000000000000000000, 0.9238795325112867385, 1.000000000000000000, 0.9238795325112867385, 1.000000000000000000, 0.9238795325112867385, 1.000000000000000000, 0.9238795325112867385, 1.000000000000000000, 0.9238795325112867385, 1.000000000000000000, 0.9238795325112867385, 1.000000000000000000, 0.9238795325112867385, 1.000000000000000000, 0.9238795325112867385, 1.000000000000000000, 0.9238795325112867385, 1.000000000000000000, 0.9238795325112867385, 1.000000000000000000, 0.9238795325112867385, 1.000000000000000000, 0.9238795325112867385, 1.000000000000000000, 0.9238795325112867385, 1.000000000000000000, 0.9238795325112867385, 1.000000000000000000, 0.9238795325112867385, 1.000000000000000000, 0.9238795325112867385, 1.000000000000000000, 0.9238795325112867385, 1.000000000000000000, 0.9238795325112867385, 1.000000000000000000, 0.9238795325112867385, 1.000000000000000000, 0.9238795325112867385, 1.000000000000000000, 0.9238795325112867385, 1.000000000000000000, 0.9238795325112867385, 1.000000000000000000, 0.9238795325112867385, 1.000000000000000000, 0.9238795325112867385, 1.000000000000000000, 0.9238795325112867385, 1.000000000000000000, 0.9238795325112867385, 1.000000000000000000, 0.9238795325112867385, 1.000000000000000000, 0.9694574366903154772, 0.9634246591005992677) ) ) 
 REPRESENTATION_ITEM ( '' )  SURFACE ( )  );
#5304=ADVANCED_FACE ( 'NONE', ( #2069 ), #13042, .F. ) ;
#5308=DIRECTION ( 'NONE',  ( 1.000000000000000000, 0.000000000000000000, 0.000000000000000000 ) ) ;
#5311=CARTESIAN_POINT ( 'NONE',  ( -3.567000345541168738, 47.45638922224109280, 95.05433879953099563 ) ) ;
#5313=CARTESIAN_POINT ( 'NONE',  ( -5.154188915835984375, 42.64120994080404614, 90.96121380123797451 ) ) ;
#5317=CARTESIAN_POINT ( 'NONE',  ( -5.784195910403845176, 44.99242805365518194, 94.63308880123798872 ) ) ;
#5318=UNCERTAINTY_MEASURE_WITH_UNIT (LENGTH_MEASURE( 1.000000000000000082E-05 ), #2326, 'distance_accuracy_value', 'NONE');
#5328=CARTESIAN_POINT ( 'NONE',  ( -3.350035803220276609, 49.20851703305431357, 91.97683880123797451 ) ) ;
#5330=ORIENTED_EDGE ( 'NONE', *, *, #18204, .F. ) ;
#5350=DIRECTION ( 'NONE',  ( 1.000000000000000000, 1.213411507412056509E-16, 0.000000000000000000 ) ) ;
#5354=CARTESIAN_POINT ( 'NONE',  ( -2.077846259693550746, 39.65884927180063357, 95.41433879953098085 ) ) ;
#5355=CARTESIAN_POINT ( 'NONE',  ( -5.058133621542618030, 44.89684013992257405, 92.67996379953099506 ) ) ;
#5357=DIRECTION ( 'NONE',  ( 1.000000000000000000, -0.000000000000000000, -0.000000000000000000 ) ) ;
#5361=LINE ( 'NONE', #8260, #12892 ) ;
#5364=CARTESIAN_POINT ( 'NONE',  ( 4.394343283833276992, 39.11584570990505938, 94.00808880123797451 ) ) ;
#5365=ORIENTED_EDGE ( 'NONE', *, *, #5878, .T. ) ;
#5367=LINE ( 'NONE', #18360, #4417 ) ;
#5368=CARTESIAN_POINT ( 'NONE',  ( 5.146043734657006041, 40.41782908280415398, 90.15009084312077903 ) ) ;
#5371=CARTESIAN_POINT ( 'NONE',  ( 10.77494014480653917, 42.96218137147968008, 61.80715055817104542 ) ) ;
#5376=VERTEX_POINT ( 'NONE', #2176 ) ;
#5383=VERTEX_POINT ( 'NONE', #5896 ) ;
#5385=ADVANCED_FACE ( 'NONE', ( #15263, #5788 ), #10804, .F. ) ;
#5388=CARTESIAN_POINT ( 'NONE',  ( 2.916646314870772194, 38.79555996194921619, 92.55433879953098142 ) ) ;
#5391=CARTESIAN_POINT ( 'NONE',  ( -2.416137431568557314, 39.07291177436112406, 95.02371380123797451 ) ) ;
#5395=CARTESIAN_POINT ( 'NONE',  ( -5.058133621542618030, 44.89684013992257405, 95.49246380294496817 ) ) ;
#5396=VECTOR ( 'NONE', #15725, 1000.000000000000000 ) ;
#5400=ORIENTED_EDGE ( 'NONE', *, *, #20510, .F. ) ;
#5401=CARTESIAN_POINT ( 'NONE',  ( 32.72215374030650281, 44.16218137147968292, 45.55433879953098852 ) ) ;
#5404=CARTESIAN_POINT ( 'NONE',  ( -2.416137431568557314, 39.07291177436112406, 92.52371380123797451 ) ) ;
#5405=VECTOR ( 'NONE', #16444, 1000.000000000000000 ) ;
#5406=CARTESIAN_POINT ( 'NONE',  ( 0.5221537403065020788, 52.36218137147968577, 83.03825919817350609 ) ) ;
#5419=VECTOR ( 'NONE', #15908, 1000.000000000000000 ) ;
#5421=CARTESIAN_POINT ( 'NONE',  ( 4.987494971863720927, 47.58855820898865829, 90.02371380294498238 ) ) ;
#5426=CARTESIAN_POINT ( 'NONE',  ( -4.524181921268124462, 40.28999182795290324, 96.03933880123798872 ) ) ;
#5427=AXIS2_PLACEMENT_3D ( 'NONE', #2294, #808, #13682 ) ;
#5431=LINE ( 'NONE', #13525, #3445 ) ;
#5436=CARTESIAN_POINT ( 'NONE',  ( -0.9988176903691428077, 49.83852402762217082, 90.64871380123798872 ) ) ;
#5462=ORIENTED_EDGE ( 'NONE', *, *, #19872, .F. ) ;
#5464=CARTESIAN_POINT ( 'NONE',  ( 1.256812508749381774, 49.74246873332880625, 92.36746379953098085 ) ) ;
#5465=CARTESIAN_POINT ( 'NONE',  ( -0.2125050281363792815, 38.58189400963055959, 91.74246379953099506 ) ) ;
#5467=ORIENTED_EDGE ( 'NONE', *, *, #9631, .T. ) ;
#5470=CARTESIAN_POINT ( 'NONE',  ( 11.32022995165976198, 36.96218137147968719, 93.55433879953098142 ) ) ;
#5473=CARTESIAN_POINT ( 'NONE',  ( -0.8237052942265477018, 49.18499566818285018, 92.44558879953099506 ) ) ;
#5474=VERTEX_POINT ( 'NONE', #14017 ) ;
#5476=CARTESIAN_POINT ( 'NONE',  ( 5.025485839985549319, 41.56218137147963887, 90.72683879953099506 ) ) ;
#5480=LINE ( 'NONE', #12412, #3064 ) ;
#5483=CARTESIAN_POINT ( 'NONE',  ( -3.350035803220276609, 49.20851703305431357, 90.72683880123797451 ) ) ;
#5487=CARTESIAN_POINT ( 'NONE',  ( 0.5221537403065020788, 52.36218137147968577, 48.36106904222365444 ) ) ;
#5497=LINE ( 'NONE', #17202, #5835 ) ;
#5498=CARTESIAN_POINT ( 'NONE',  ( 10.77494014480653561, 42.96218137147968008, 77.40433879953098995 ) ) ;
#5500=EDGE_LOOP ( 'NONE', ( #15221, #12806 ) ) ;
#5515=CARTESIAN_POINT ( 'NONE',  ( -3.943187491250720544, 40.73580453397070755, 93.14871380294496817 ) ) ;
#5518=VERTEX_POINT ( 'NONE', #2741 ) ;
#5520=ORIENTED_EDGE ( 'NONE', *, *, #14981, .T. ) ;
#5524=CARTESIAN_POINT ( 'NONE',  ( -5.154188915835984375, 42.64120994080404614, 93.61746380123797451 ) ) ;
#5528=CARTESIAN_POINT ( 'NONE',  ( 5.611423337425062385, 41.22389019960463230, 91.58621380123798872 ) ) ;
#5532=ORIENTED_EDGE ( 'NONE', *, *, #20293, .T. ) ;
#5536=ORIENTED_EDGE ( 'NONE', *, *, #9033, .F. ) ;
#5537=DIRECTION ( 'NONE',  ( -1.000000000000000000, -3.942553354492745503E-16, 0.000000000000000000 ) ) ;
#5540=CARTESIAN_POINT ( 'NONE',  ( 8.722153740306483272, 51.36218137147968577, 95.05433879953098142 ) ) ;
#5542=VECTOR ( 'NONE', #19953, 1000.000000000000000 ) ;
#5544=CARTESIAN_POINT ( 'NONE',  ( -5.154188915835984375, 42.64120994080404614, 93.46121380123797451 ) ) ;
#5549=EDGE_LOOP ( 'NONE', ( #1240, #3354, #13584, #9503 ) ) ;
#5550=LINE ( 'NONE', #2254, #11582 ) ;
#5551=CARTESIAN_POINT ( 'NONE',  ( 5.146041124512939824, 40.41782456190201600, 90.15009067557426192 ) ) ;
#5553=CARTESIAN_POINT ( 'NONE',  ( 2.916646314870772194, 38.79555996194921619, 92.55433879953098142 ) ) ;
#5554=VECTOR ( 'NONE', #6113, 1000.000000000000000 ) ;
#5557=CARTESIAN_POINT ( 'NONE',  ( -1.677846259693499542, 50.36218137147968577, 37.95170767603170248 ) ) ;
#5561=ORIENTED_EDGE ( 'NONE', *, *, #3507, .F. ) ;
#5563=ORIENTED_EDGE ( 'NONE', *, *, #426, .T. ) ;
#5570=ORIENTED_EDGE ( 'NONE', *, *, #7104, .F. ) ;
#5574=CARTESIAN_POINT ( 'NONE',  ( 5.544968037009670780, 45.50804040601273925, 94.63308879953099506 ) ) ;
#5575=CARTESIAN_POINT ( 'NONE',  ( 3.948530577815480225, 39.69684013992245752, 91.89871379953099506 ) ) ;
#5577=CARTESIAN_POINT ( 'NONE',  ( 6.828503391016846891, 43.33193468930419101, 94.16433880123797451 ) ) ;
#5578=CARTESIAN_POINT ( 'NONE',  ( -4.524181921268124462, 40.28999182795290324, 94.78933880123805977 ) ) ;
#5582=VERTEX_POINT ( 'NONE', #8924 ) ;
#5584=CARTESIAN_POINT ( 'NONE',  ( -4.524181921268124462, 40.28999182795290324, 94.94558880123797451 ) ) ;
#5589=DIRECTION ( 'NONE',  ( 1.000000000000000000, 0.000000000000000000, -0.000000000000000000 ) ) ;
#5596=ORIENTED_EDGE ( 'NONE', *, *, #12621, .T. ) ;
#5602=CARTESIAN_POINT ( 'NONE',  ( -5.154188915835984375, 42.64120994080404614, 96.11746380123797451 ) ) ;
#5603=EDGE_LOOP ( 'NONE', ( #12942, #7052, #13651, #12822 ) ) ;
#5610=CARTESIAN_POINT ( 'NONE',  ( 11.22215374030650281, 42.96218137147968008, 69.80574467885101342 ) ) ;
#5613=CARTESIAN_POINT ( 'NONE',  ( 6.828503391016846891, 43.33193468930419101, 94.16433880123797451 ) ) ;
#5616=DIRECTION ( 'NONE',  ( -5.595882180570345180E-16, 1.000000000000000000, 0.000000000000000000 ) ) ;
#5617=CARTESIAN_POINT ( 'NONE',  ( -3.981178359372548492, 46.76218137147973408, 94.16433880294496817 ) ) ;
#5621=VERTEX_POINT ( 'NONE', #2533 ) ;
#5622=CARTESIAN_POINT ( 'NONE',  ( 5.722153740306476166, 44.16218185472587976, 94.89411094854372664 ) ) ;
#5626=CARTESIAN_POINT ( 'NONE',  ( 5.568489401881125289, 48.03437091500646261, 95.57058880123798872 ) ) ;
#5627=PLANE ( 'NONE',  #13602 ) ;
#5631=ORIENTED_EDGE ( 'NONE', *, *, #13895, .F. ) ;
#5634=CARTESIAN_POINT ( 'NONE',  ( 11.22215374030650281, 42.96218137147968008, 66.20574467885104752 ) ) ;
#5635=LINE ( 'NONE', #18622, #16400 ) ;
#5638=CARTESIAN_POINT ( 'NONE',  ( 5.544968037009670780, 45.50804040601273925, 91.19558880294498238 ) ) ;
#5641=CARTESIAN_POINT ( 'NONE',  ( 6.198496396448986090, 45.68315280215533392, 90.33621380123798872 ) ) ;
#5648=CARTESIAN_POINT ( 'NONE',  ( -4.567115856812060670, 47.10047254335474065, 93.30496380123798872 ) ) ;
#5661=ORIENTED_EDGE ( 'NONE', *, *, #16128, .F. ) ;
#5669=ORIENTED_EDGE ( 'NONE', *, *, #12657, .F. ) ;
#5673=CARTESIAN_POINT ( 'NONE',  ( -5.058133621542618030, 44.89684013992257405, 92.67996379953099506 ) ) ;
#5675=CARTESIAN_POINT ( 'NONE',  ( 6.828503391016846891, 43.33193468930419101, 95.41433880123797451 ) ) ;
#5679=CARTESIAN_POINT ( 'NONE',  ( 3.948530577815480225, 39.69684013992245752, 91.89871379953099506 ) ) ;
#5682=CARTESIAN_POINT ( 'NONE',  ( -5.784195910403845176, 44.99242805365518194, 96.03933880123796030 ) ) ;
#5697=ADVANCED_FACE ( 'NONE', ( #1465 ), #14333, .F. ) ;
#5700=CARTESIAN_POINT ( 'NONE',  ( -5.368445182934982185, 36.96218137147968008, 80.55433879953099563 ) ) ;
#5701=CARTESIAN_POINT ( 'NONE',  ( 3.460444912181559474, 49.25145096859824889, 90.64871380123798872 ) ) ;
#5702=ORIENTED_EDGE ( 'NONE', *, *, #9013, .T. ) ;
#5711=AXIS2_PLACEMENT_3D ( 'NONE', #20999, #6434, #13151 ) ;
#5714=EDGE_CURVE ( 'NONE', #3020, #13327, #6863, .T. ) ;
#5721=CARTESIAN_POINT ( 'NONE',  ( -4.500660556396669065, 42.81632233694663370, 94.32058880294496817 ) ) ;
#5728=DIRECTION ( 'NONE',  ( -1.000000000000000000, 0.000000000000000000, 0.000000000000000000 ) ) ;
#5729=CARTESIAN_POINT ( 'NONE',  ( -5.784195910403845176, 44.99242805365518194, 96.03933880123796030 ) ) ;
#5730=DIRECTION ( 'NONE',  ( -0.000000000000000000, -0.000000000000000000, 1.000000000000000000 ) ) ;
#5742=CARTESIAN_POINT ( 'NONE',  ( -3.857995858694130753, 47.10914555767435274, 95.05433879953105247 ) ) ;
#5743=VECTOR ( 'NONE', #11956, 999.9999999999998863 ) ;
#5745=CARTESIAN_POINT ( 'NONE',  ( 3.122153740306552905, 48.66551347115873227, 92.60183880294498238 ) ) ;
#5747=CARTESIAN_POINT ( 'NONE',  ( -5.784195910403845176, 44.99242805365518194, 93.38308880123798872 ) ) ;
#5751=CARTESIAN_POINT ( 'NONE',  ( 4.167070027254266229, 47.87117560886914447, 95.05212442257573002 ) ) ;
#5752=CARTESIAN_POINT ( 'NONE',  ( -3.350035803220276609, 49.20851703305431357, 91.97683880123797451 ) ) ;
#5755=ORIENTED_EDGE ( 'NONE', *, *, #13413, .F. ) ;
#5761=CARTESIAN_POINT ( 'NONE',  ( 5.611423337425062385, 41.22389019960463230, 90.17996380123798872 ) ) ;
#5762=VERTEX_POINT ( 'NONE', #17939 ) ;
#5776=CARTESIAN_POINT ( 'NONE',  ( 11.22215374030650281, 42.96218137147968008, 57.80715055817105252 ) ) ;
#5779=VECTOR ( 'NONE', #19413, 1000.000000000000000 ) ;
#5780=DIRECTION ( 'NONE',  ( 1.000000000000000000, 1.402518428993831676E-16, 0.000000000000000000 ) ) ;
#5787=ORIENTED_EDGE ( 'NONE', *, *, #6660, .T. ) ;
#5788=FACE_OUTER_BOUND ( 'NONE', #14179, .T. ) ;
#5791=CARTESIAN_POINT ( 'NONE',  ( -3.943187491250720544, 40.73580453397070755, 92.83621379953099506 ) ) ;
#5792=VECTOR ( 'NONE', #18183, 1000.000000000000000 ) ;
#5794=CARTESIAN_POINT ( 'NONE',  ( -3.350035803220276609, 49.20851703305431357, 93.38308880123798872 ) ) ;
#5800=CARTESIAN_POINT ( 'NONE',  ( -3.350035803220276609, 49.20851703305431357, 90.88308880123797451 ) ) ;
#5801=AXIS2_PLACEMENT_3D ( 'NONE', #5406, #15216, #627 ) ;
#5812=B_SPLINE_CURVE_WITH_KNOTS ( 'NONE', 3,
 ( #14296, #7610, #11226, #12499, #9322, #14093, #14504, #9630, #20872, #16112 ),
 .UNSPECIFIED., .F., .F.,
 ( 4, 2, 2, 2, 4 ),
 ( 0.000000000000000000, 0.001160160651305680753, 0.002320321302611361072, 0.003480481953917041391, 0.004640642605222721276 ),
 .UNSPECIFIED. ) ;
#5816=CARTESIAN_POINT ( 'NONE',  ( -2.416137431568557314, 39.07291177436112406, 92.52371380123797451 ) ) ;
#5819=CARTESIAN_POINT ( 'NONE',  ( 10.77494014480653917, 42.96218137147968008, 57.80715055817105252 ) ) ;
#5829=CARTESIAN_POINT ( 'NONE',  ( 6.828503391016846891, 43.33193468930419101, 95.41433880123797451 ) ) ;
#5833=CARTESIAN_POINT ( 'NONE',  ( 1.868012774839550749, 39.13936707477651566, 90.88308880294496817 ) ) ;
#5835=VECTOR ( 'NONE', #4000, 999.9999999999998863 ) ;
#5837=CARTESIAN_POINT ( 'NONE',  ( 11.22215374030650281, 42.76218137147968434, 72.80433879953100984 ) ) ;
#5838=AXIS2_PLACEMENT_3D ( 'NONE', #9467, #11168, #12345 ) ;
#5840=ORIENTED_EDGE ( 'NONE', *, *, #16017, .F. ) ;
#5855=VECTOR ( 'NONE', #9054, 1000.000000000000000 ) ;
#5859=PLANE ( 'NONE',  #17263 ) ;
#5860=CARTESIAN_POINT ( 'NONE',  ( 1.352400422481993658, 50.46853102219002096, 93.07058880123798872 ) ) ;
#5862=CARTESIAN_POINT ( 'NONE',  ( 31.22215374030650281, 42.76218137147968434, 78.80433879953099563 ) ) ;
#5863=CARTESIAN_POINT ( 'NONE',  ( 3.122075258343615545, 38.59543968120053847, 90.05576841395854615 ) ) ;
#5865=VECTOR ( 'NONE', #17019, 1000.000000000000000 ) ;
#5867=VERTEX_POINT ( 'NONE', #17088 ) ;
#5875=CARTESIAN_POINT ( 'NONE',  ( 4.987494971863720927, 47.58855820898865829, 92.52371380294498238 ) ) ;
#5877=CARTESIAN_POINT ( 'NONE',  ( -10.17784625969349754, 51.36218137147968577, 54.55433879953098852 ) ) ;
#5878=EDGE_CURVE ( 'NONE', #4650, #13095, #8788, .T. ) ;
#5881=PLANE ( 'NONE',  #7046 ) ;
#5889=DIRECTION ( 'NONE',  ( 0.000000000000000000, 1.000000000000000000, 1.734723475976787531E-14 ) ) ;
#5890=CARTESIAN_POINT ( 'NONE',  ( -4.567115856812060670, 47.10047254335474065, 95.80496380123798872 ) ) ;
#5896=CARTESIAN_POINT ( 'NONE',  ( 1.514255888186008203, 51.36218137147968577, 52.53721119516358584 ) ) ;
#5897=VERTEX_POINT ( 'NONE', #8687 ) ;
#5901=CARTESIAN_POINT ( 'NONE',  ( -2.416137431568557314, 39.07291177436112406, 96.27371380123797451 ) ) ;
#5904=CARTESIAN_POINT ( 'NONE',  ( -5.784195910403845176, 44.99242805365518194, 93.53933880123797451 ) ) ;
#5909=DIRECTION ( 'NONE',  ( 0.000000000000000000, 0.000000000000000000, -1.000000000000000000 ) ) ;
#5921=ORIENTED_EDGE ( 'NONE', *, *, #9153, .F. ) ;
#5924=LINE ( 'NONE', #15296, #11211 ) ;
#5926=CARTESIAN_POINT ( 'NONE',  ( 6.198496396448986090, 45.68315280215533392, 90.49246380123798872 ) ) ;
#5927=ORIENTED_EDGE ( 'NONE', *, *, #13949, .T. ) ;
#5934=ORIENTED_EDGE ( 'NONE', *, *, #14197, .T. ) ;
#5937=CARTESIAN_POINT ( 'NONE',  ( -5.945795452124602143, 37.96218137147967298, 95.05433879953098142 ) ) ;
#5938=CARTESIAN_POINT ( 'NONE',  ( 3.788215052820487205, 39.19523464621513398, 90.24306233796824017 ) ) ;
#5940=EDGE_CURVE ( 'NONE', #4901, #9713, #20044, .T. ) ;
#5942=CARTESIAN_POINT ( 'NONE',  ( 1.868012774839550749, 39.13936707477651566, 94.63308880294498238 ) ) ;
#5950=ORIENTED_EDGE ( 'NONE', *, *, #3626, .F. ) ;
#5953=CARTESIAN_POINT ( 'NONE',  ( 31.22215374030650281, 42.96218137147968008, 74.20433879953100131 ) ) ;
#5968=CARTESIAN_POINT ( 'NONE',  ( 4.987494971863720927, 47.58855820898865829, 93.77371380294498238 ) ) ;
#5971=DIRECTION ( 'NONE',  ( -0.000000000000000000, -1.000000000000000000, -0.000000000000000000 ) ) ;
#5973=DIRECTION ( 'NONE',  ( -0.000000000000000000, -0.000000000000000000, 1.000000000000000000 ) ) ;
#5982=EDGE_CURVE ( 'NONE', #5158, #2806, #11487, .T. ) ;
#5990=ORIENTED_EDGE ( 'NONE', *, *, #7931, .T. ) ;
#5992=EDGE_CURVE ( 'NONE', #18376, #13415, #10823, .T. ) ;
#5993=ORIENTED_EDGE ( 'NONE', *, *, #12352, .F. ) ;
#5996=CARTESIAN_POINT ( 'NONE',  ( 5.544968037009670780, 45.50804040601273925, 90.88308879953099506 ) ) ;
#5998=ORIENTED_EDGE ( 'NONE', *, *, #7556, .F. ) ;
#6004=LINE ( 'NONE', #18987, #10892 ) ;
#6008=CARTESIAN_POINT ( 'NONE',  ( 5.295834872933118831, 46.52492710298120215, 95.05433879953093879 ) ) ;
#6020=CARTESIAN_POINT ( 'NONE',  ( -5.154188915835984375, 42.64120994080404614, 91.11746380123797451 ) ) ;
#6028=DIRECTION ( 'NONE',  ( -0.7071067811865515695, 0.7071067811865434649, 0.000000000000000000 ) ) ;
#6034=CARTESIAN_POINT ( 'NONE',  ( 3.460444912181559474, 49.25145096859824889, 95.49246380123798872 ) ) ;
#6038=VECTOR ( 'NONE', #18380, 1000.000000000000000 ) ;
#6040=SURFACE_STYLE_FILL_AREA ( #10757 ) ;
#6041=FACE_OUTER_BOUND ( 'NONE', #3732, .T. ) ;
#6044=DIRECTION ( 'NONE',  ( -0.000000000000000000, 0.000000000000000000, -1.000000000000000000 ) ) ;
#6046=CARTESIAN_POINT ( 'NONE',  ( -5.154188915835984375, 42.64120994080404614, 91.11746380123797451 ) ) ;
#6047=EDGE_CURVE ( 'NONE', #9713, #5867, #6004, .T. ) ;
#6055=DIRECTION ( 'NONE',  ( -0.000000000000000000, -0.000000000000000000, 1.000000000000000000 ) ) ;
#6060=ORIENTED_EDGE ( 'NONE', *, *, #10030, .T. ) ;
#6062=CARTESIAN_POINT ( 'NONE',  ( 11.22215374030650281, 42.76218137147968434, 65.80574467885102763 ) ) ;
#6067=CARTESIAN_POINT ( 'NONE',  ( 5.544968037009670780, 45.50804040601273925, 89.94558880294498238 ) ) ;
#6073=CARTESIAN_POINT ( 'NONE',  ( 11.22215374030650281, 42.76218137147968434, 73.80433879953100984 ) ) ;
#6078=EDGE_CURVE ( 'NONE', #2513, #1287, #20578, .T. ) ;
#6080=CARTESIAN_POINT ( 'NONE',  ( 6.198496396448986090, 45.68315280215533392, 95.33621380123798872 ) ) ;
#6081=CARTESIAN_POINT ( 'NONE',  ( -0.3080929418689875576, 37.85583172076933778, 94.94558880123797451 ) ) ;
#6086=VERTEX_POINT ( 'NONE', #16216 ) ;
#6092=CIRCLE ( 'NONE', #321, 0.9921021478795063464 ) ;
#6094=CARTESIAN_POINT ( 'NONE',  ( 6.828503391016846891, 43.33193468930419101, 92.91433880123798872 ) ) ;
#6096=ORIENTED_EDGE ( 'NONE', *, *, #2870, .F. ) ;
#6097=VECTOR ( 'NONE', #15065, 1000.000000000000000 ) ;
#6104=CARTESIAN_POINT ( 'NONE',  ( -3.566428375817382257, 47.45690933515070498, 92.55433879953095300 ) ) ;
#6106=CARTESIAN_POINT ( 'NONE',  ( 1.352400422481993658, 50.46853102219002096, 90.72683880123797451 ) ) ;
#6107=ORIENTED_EDGE ( 'NONE', *, *, #11342, .F. ) ;
#6113=DIRECTION ( 'NONE',  ( 1.000000000000000000, -0.000000000000000000, -0.000000000000000000 ) ) ;
#6118=AXIS2_PLACEMENT_3D ( 'NONE', #1814, #13188, #299 ) ;
#6120=VECTOR ( 'NONE', #15872, 1000.000000000000000 ) ;
#6125=CARTESIAN_POINT ( 'NONE',  ( -4.524181921268124462, 40.28999182795290324, 92.44558880123798872 ) ) ;
#6128=EDGE_LOOP ( 'NONE', ( #19249, #5840, #6583, #16057 ) ) ;
#6133=ADVANCED_FACE ( 'NONE', ( #13125 ), #19600, .F. ) ;
#6144=CARTESIAN_POINT ( 'NONE',  ( 3.122075258343615545, 38.59543968120053847, 90.21201841395856036 ) ) ;
#6147=DIRECTION ( 'NONE',  ( -0.000000000000000000, -2.168404344970984413E-15, -1.000000000000000000 ) ) ;
#6156=EDGE_CURVE ( 'NONE', #4005, #7893, #8339, .T. ) ;
#6158=DIRECTION ( 'NONE',  ( -0.000000000000000000, -0.000000000000000000, 1.000000000000000000 ) ) ;
#6167=VECTOR ( 'NONE', #3819, 1000.000000000000000 ) ;
#6170=CARTESIAN_POINT ( 'NONE',  ( 10.77494014480653917, 42.76218137147968434, 61.80715055817104542 ) ) ;
#6172=ORIENTED_EDGE ( 'NONE', *, *, #2896, .T. ) ;
#6175=CARTESIAN_POINT ( 'NONE',  ( 5.025485839985549319, 41.56218137147963887, 89.78933880294498238 ) ) ;
#6176=ORIENTED_EDGE ( 'NONE', *, *, #12464, .F. ) ;
#6186=CARTESIAN_POINT ( 'NONE',  ( -0.3080929418689875576, 37.85583172076933778, 93.69558880123800293 ) ) ;
#6199=CARTESIAN_POINT ( 'NONE',  ( -4.567115856812060670, 47.10047254335474065, 95.96121380123798872 ) ) ;
#6204=EDGE_LOOP ( 'NONE', ( #3344, #20450, #20888, #6267 ) ) ;
#6211=CARTESIAN_POINT ( 'NONE',  ( -4.615702297814525679, 45.70854999956944198, 92.55433879953100984 ) ) ;
#6212=CARTESIAN_POINT ( 'NONE',  ( -5.154188915835984375, 42.64120994080404614, 92.36746380123797451 ) ) ;
#6228=ORIENTED_EDGE ( 'NONE', *, *, #8018, .T. ) ;
#6229=CARTESIAN_POINT ( 'NONE',  ( -1.219056181836354558, 49.77488197367695477, 93.31237966814926210 ) ) ;
#6230=ORIENTED_EDGE ( 'NONE', *, *, #10160, .T. ) ;
#6243=CARTESIAN_POINT ( 'NONE',  ( 3.460444912181559474, 49.25145096859824889, 90.64871380123798872 ) ) ;
#6252=DIRECTION ( 'NONE',  ( -1.193617070626243484E-16, -1.000000000000000000, -0.000000000000000000 ) ) ;
#6264=PLANE ( 'NONE',  #9800 ) ;
#6267=ORIENTED_EDGE ( 'NONE', *, *, #18869, .F. ) ;
#6274=CARTESIAN_POINT ( 'NONE',  ( 4.613683985508550300, 40.84891963687440608, 89.75946567728124137 ) ) ;
#6286=DIRECTION ( 'NONE',  ( 1.000000000000000000, 0.000000000000000000, 0.000000000000000000 ) ) ;
#6296=CARTESIAN_POINT ( 'NONE',  ( 6.102441102155617969, 43.42752260303680600, 90.80496379953099506 ) ) ;
#6304=CARTESIAN_POINT ( 'NONE',  ( 4.199109002476567376, 47.83913663364971569, 93.48786078214052964 ) ) ;
#6306=CARTESIAN_POINT ( 'NONE',  ( -4.898402303810498459, 43.01822212045506433, 92.55433879953096721 ) ) ;
#6313=CARTESIAN_POINT ( 'NONE',  ( 31.07218010054375412, 42.76218137147968434, 70.80574467885102763 ) ) ;
#6321=LINE ( 'NONE', #12934, #18000 ) ;
#6328=EDGE_CURVE ( 'NONE', #16577, #16572, #8664, .T. ) ;
#6332=ORIENTED_EDGE ( 'NONE', *, *, #13276, .F. ) ;
#6341=CARTESIAN_POINT ( 'NONE',  ( -5.784195910403845176, 44.99242805365518194, 93.53933880123797451 ) ) ;
#6342=CARTESIAN_POINT ( 'NONE',  ( 5.611423337425062385, 41.22389019960463230, 92.67996380123798872 ) ) ;
#6352=CARTESIAN_POINT ( 'NONE',  ( 2.722153740306497927, 50.36218137147968577, 54.55433879953098852 ) ) ;
#6358=VECTOR ( 'NONE', #18934, 1000.000000000000000 ) ;
#6359=CARTESIAN_POINT ( 'NONE',  ( 4.199109002476567376, 47.83913663364971569, 93.80036078555450274 ) ) ;
#6363=CARTESIAN_POINT ( 'NONE',  ( 5.722153740306500147, 44.16218137147969003, 77.84651775085080772 ) ) ;
#6366=CARTESIAN_POINT ( 'NONE',  ( 32.72215374030650281, 44.16218137147968292, 93.55433879953098142 ) ) ;
#6368=FACE_OUTER_BOUND ( 'NONE', #20109, .T. ) ;
#6369=DIRECTION ( 'NONE',  ( -1.402518428993831676E-16, 1.000000000000000000, 0.000000000000000000 ) ) ;
#6371=AXIS2_PLACEMENT_3D ( 'NONE', #6754, #166, #1779 ) ;
#6373=FACE_OUTER_BOUND ( 'NONE', #16026, .T. ) ;
#6374=DIRECTION ( 'NONE',  ( 0.000000000000000000, 0.000000000000000000, 1.000000000000000000 ) ) ;
#6375=EDGE_CURVE ( 'NONE', #15717, #13055, #2684, .T. ) ;
#6383=DIRECTION ( 'NONE',  ( 1.334402673828313339E-16, 1.619179559944692391E-32, -1.000000000000000000 ) ) ;
#6386=VECTOR ( 'NONE', #17053, 1000.000000000000000 ) ;
#6389=CARTESIAN_POINT ( 'NONE',  ( -5.784195910403845176, 44.99242805365518194, 94.63308880123798872 ) ) ;
#6390=CARTESIAN_POINT ( 'NONE',  ( 1.352400422481993658, 50.46853102219002096, 94.32058880123798872 ) ) ;
#6395=ORIENTED_EDGE ( 'NONE', *, *, #20354, .F. ) ;
#6400=CARTESIAN_POINT ( 'NONE',  ( 5.146040402138061687, 40.41782331071202350, 90.30634062920465510 ) ) ;
#6401=CARTESIAN_POINT ( 'NONE',  ( -2.416137431568557314, 39.07291177436112406, 94.86746380123797451 ) ) ;
#6402=ORIENTED_EDGE ( 'NONE', *, *, #19357, .T. ) ;
#6409=CARTESIAN_POINT ( 'NONE',  ( -3.998026543861774140, 40.70229664527460045, 92.55433879953100984 ) ) ;
#6410=LINE ( 'NONE', #20877, #18121 ) ;
#6411=ORIENTED_EDGE ( 'NONE', *, *, #1305, .F. ) ;
#6413=CARTESIAN_POINT ( 'NONE',  ( 10.77494014480653917, 42.96218137147968008, 57.80715055817105252 ) ) ;
#6416=DIRECTION ( 'NONE',  ( -1.000000000000000000, 0.000000000000000000, -0.000000000000000000 ) ) ;
#6421=EDGE_LOOP ( 'NONE', ( #16668, #10947, #14862, #18947 ) ) ;
#6427=DIRECTION ( 'NONE',  ( 1.000000000000000000, 1.402518428993831676E-16, 1.334402673828313339E-16 ) ) ;
#6434=DIRECTION ( 'NONE',  ( 0.7071067811865516806, -0.7071067811865433539, 0.000000000000000000 ) ) ;
#6436=CARTESIAN_POINT ( 'NONE',  ( 3.948530577815480225, 39.69684013992245752, 95.64871379953100927 ) ) ;
#6444=LINE ( 'NONE', #8268, #20601 ) ;
#6446=CARTESIAN_POINT ( 'NONE',  ( 1.352400422481993658, 50.46853102219002096, 94.32058880123798872 ) ) ;
#6447=CARTESIAN_POINT ( 'NONE',  ( -0.3080929418689875576, 37.85583172076933778, 92.44558880123798872 ) ) ;
#6455=DIRECTION ( 'NONE',  ( 1.000000000000000000, 0.000000000000000000, 1.196361017915039239E-16 ) ) ;
#6458=DIRECTION ( 'NONE',  ( -1.193617070626243484E-16, -1.000000000000000000, -0.000000000000000000 ) ) ;
#6464=ORIENTED_EDGE ( 'NONE', *, *, #1718, .F. ) ;
#6472=CARTESIAN_POINT ( 'NONE',  ( -3.416655834652597257, 49.09312775381169303, 93.23111517561484618 ) ) ;
#6473=AXIS2_PLACEMENT_3D ( 'NONE', #11296, #8720, #8404 ) ;
#6477=CARTESIAN_POINT ( 'NONE',  ( -5.784195910403845176, 44.99242805365518194, 93.38308880123798872 ) ) ;
#6481=DIRECTION ( 'NONE',  ( 1.000000000000000000, 0.000000000000000000, -0.000000000000000000 ) ) ;
#6493=VERTEX_POINT ( 'NONE', #15883 ) ;
#6494=CARTESIAN_POINT ( 'NONE',  ( 5.568489401881125289, 48.03437091500646261, 92.91433880123798872 ) ) ;
#6509=CARTESIAN_POINT ( 'NONE',  ( -0.9988176903691428077, 49.83852402762217082, 90.80496380123797451 ) ) ;
#6510=CARTESIAN_POINT ( 'NONE',  ( 5.568489401881125289, 48.03437091500646261, 94.16433880123797451 ) ) ;
#6518=ORIENTED_EDGE ( 'NONE', *, *, #9988, .T. ) ;
#6541=DIRECTION ( 'NONE',  ( 1.000000000000000000, -0.000000000000000000, 0.000000000000000000 ) ) ;
#6543=CARTESIAN_POINT ( 'NONE',  ( 3.460444912181559474, 49.25145096859824889, 94.39871380123798872 ) ) ;
#6548=CARTESIAN_POINT ( 'NONE',  ( -4.500660556396669065, 42.81632233694663370, 92.75808879953098085 ) ) ;
#6549=EDGE_LOOP ( 'NONE', ( #16969, #9008, #20349, #10413 ) ) ;
#6553=VERTEX_POINT ( 'NONE', #1617 ) ;
#6556=CARTESIAN_POINT ( 'NONE',  ( 6.198496396448986090, 45.68315280215533392, 94.08621380123798872 ) ) ;
#6569=VECTOR ( 'NONE', #6369, 1000.000000000000000 ) ;
#6577=DIRECTION ( 'NONE',  ( -0.000000000000000000, 0.000000000000000000, -1.000000000000000000 ) ) ;
#6582=CARTESIAN_POINT ( 'NONE',  ( 6.198496396448986090, 45.68315280215533392, 90.33621380123798872 ) ) ;
#6583=ORIENTED_EDGE ( 'NONE', *, *, #1526, .F. ) ;
#6599=CARTESIAN_POINT ( 'NONE',  ( 5.544968037009670780, 45.50804040601273925, 94.94558880294498238 ) ) ;
#6605=CARTESIAN_POINT ( 'NONE',  ( -3.777846259693486974, 36.96218137147968008, 54.55433879953099563 ) ) ;
#6609=CARTESIAN_POINT ( 'NONE',  ( -4.567115856812060670, 47.10047254335474065, 92.21121380123797451 ) ) ;
#6610=CARTESIAN_POINT ( 'NONE',  ( 6.198496396448986090, 45.68315280215533392, 94.08621380123798872 ) ) ;
#6617=DIRECTION ( 'NONE',  ( -0.000000000000000000, 0.000000000000000000, -1.000000000000000000 ) ) ;
#6623=EDGE_LOOP ( 'NONE', ( #13869, #16805, #18249, #473 ) ) ;
#6637=PLANE ( 'NONE',  #17640 ) ;
#6639=VERTEX_POINT ( 'NONE', #640 ) ;
#6645=CARTESIAN_POINT ( 'NONE',  ( -4.567115856812060670, 47.10047254335474065, 95.96121380123798872 ) ) ;
#6649=LINE ( 'NONE', #16555, #1985 ) ;
#6651=EDGE_CURVE ( 'NONE', #1583, #3871, #805, .T. ) ;
#6660=EDGE_CURVE ( 'NONE', #15210, #18376, #10675, .T. ) ;
#6673=DIRECTION ( 'NONE',  ( 0.000000000000000000, 0.000000000000000000, -1.000000000000000000 ) ) ;
#6677=DIRECTION ( 'NONE',  ( 0.000000000000000000, 0.000000000000000000, -1.000000000000000000 ) ) ;
#6678=LINE ( 'NONE', #14668, #1793 ) ;
#6681=LINE ( 'NONE', #8717, #9545 ) ;
#6683=DIRECTION ( 'NONE',  ( -1.000000000000000000, 1.193617070626243484E-16, 0.000000000000000000 ) ) ;
#6684=VECTOR ( 'NONE', #13859, 1000.000000000000000 ) ;
#6685=CARTESIAN_POINT ( 'NONE',  ( 3.460444912181559474, 49.25145096859824889, 91.74246380123798872 ) ) ;
#6689=ORIENTED_EDGE ( 'NONE', *, *, #10424, .T. ) ;
#6706=CARTESIAN_POINT ( 'NONE',  ( -2.077846259693550746, 39.65884927180063357, 95.72683880294496817 ) ) ;
#6713=ORIENTED_EDGE ( 'NONE', *, *, #3990, .T. ) ;
#6714=PLANE ( 'NONE',  #15349 ) ;
#6717=CARTESIAN_POINT ( 'NONE',  ( 2.900946498003601270, 49.13729913812269245, 94.63297921192028639 ) ) ;
#6718=LINE ( 'NONE', #13225, #17310 ) ;
#6720=CARTESIAN_POINT ( 'NONE',  ( -3.154801521863568325, 47.83913663364971569, 92.86286078555453116 ) ) ;
#6724=EDGE_CURVE ( 'NONE', #10499, #11154, #2662, .T. ) ;
#6727=EDGE_LOOP ( 'NONE', ( #14299, #2919, #17596, #10470 ) ) ;
#6729=ORIENTED_EDGE ( 'NONE', *, *, #3008, .F. ) ;
#6737=EDGE_CURVE ( 'NONE', #2084, #5762, #4349, .T. ) ;
#6741=ORIENTED_EDGE ( 'NONE', *, *, #11342, .T. ) ;
#6742=DIRECTION ( 'NONE',  ( 0.8191520442889929088, -0.5735764363510447161, 1.093078678171161153E-16 ) ) ;
#6745=DIRECTION ( 'NONE',  ( -0.000000000000000000, -0.000000000000000000, 1.000000000000000000 ) ) ;
#6747=PLANE ( 'NONE',  #17395 ) ;
#6748=CARTESIAN_POINT ( 'NONE',  ( 1.256812508749381774, 49.74246873332880625, 93.61746379953098085 ) ) ;
#6754=CARTESIAN_POINT ( 'NONE',  ( 31.22215374030650281, 36.96218137147968008, 45.55433879953098852 ) ) ;
#6756=CARTESIAN_POINT ( 'NONE',  ( 5.544968037009670780, 45.50804040601273925, 95.88308879953100927 ) ) ;
#6770=LINE ( 'NONE', #11896, #18670 ) ;
#6776=EDGE_CURVE ( 'NONE', #11438, #2175, #7767, .T. ) ;
#6778=EDGE_CURVE ( 'NONE', #12733, #7497, #16910, .T. ) ;
#6780=CARTESIAN_POINT ( 'NONE',  ( -1.534364324400819823, 49.45957383111225880, 94.69516862097951559 ) ) ;
#6787=CARTESIAN_POINT ( 'NONE',  ( 11.22215374030650281, 51.36218137147968577, 56.80715055817103831 ) ) ;
#6792=CARTESIAN_POINT ( 'NONE',  ( -3.350035803220276609, 49.20851703305431357, 90.72683880123797451 ) ) ;
#6795=CARTESIAN_POINT ( 'NONE',  ( -4.524181921268124462, 40.28999182795290324, 92.28933880123798872 ) ) ;
#6796=AXIS2_PLACEMENT_3D ( 'NONE', #5487, #8695, #18577 ) ;
#6800=EDGE_CURVE ( 'NONE', #13604, #16684, #2878, .T. ) ;
#6803=CARTESIAN_POINT ( 'NONE',  ( 30.92220646078100188, 42.96218137147968008, 61.40715055817103263 ) ) ;
#6811=EDGE_LOOP ( 'NONE', ( #5462, #9361, #9978, #7732, #2167, #1569, #17608, #17755, #2986, #15332, #11481, #20563 ) ) ;
#6813=CARTESIAN_POINT ( 'NONE',  ( 33.61275266354798674, 36.96218137147968719, 45.55433879953098852 ) ) ;
#6815=CARTESIAN_POINT ( 'NONE',  ( -4.500660556396669065, 42.81632233694663370, 95.57058880294496817 ) ) ;
#6818=CARTESIAN_POINT ( 'NONE',  ( -4.567115856812060670, 47.10047254335474065, 94.55496380123798872 ) ) ;
#6822=CARTESIAN_POINT ( 'NONE',  ( -1.677846259693499542, 47.73989013547934945, 54.55433879953098852 ) ) ;
#6826=CARTESIAN_POINT ( 'NONE',  ( -4.567115856812060670, 47.10047254335474065, 95.80496380123798872 ) ) ;
#6829=CARTESIAN_POINT ( 'NONE',  ( -5.368445182934975968, 51.36218137147968577, 80.55433879953099563 ) ) ;
#6830=CARTESIAN_POINT ( 'NONE',  ( 5.763099067774896334, 42.16033556087237599, 92.55433879953102405 ) ) ;
#6846=ADVANCED_FACE ( 'NONE', ( #7979 ), #5086, .F. ) ;
#6849=PLANE ( 'NONE',  #17380 ) ;
#6852=FACE_OUTER_BOUND ( 'NONE', #8541, .T. ) ;
#6853=CARTESIAN_POINT ( 'NONE',  ( 1.868012774839550749, 39.13936707477651566, 94.32058879953099506 ) ) ;
#6859=CARTESIAN_POINT ( 'NONE',  ( 6.102441102155617969, 43.42752260303680600, 92.05496379953099506 ) ) ;
#6860=VECTOR ( 'NONE', #17136, 1000.000000000000000 ) ;
#6863=LINE ( 'NONE', #4947, #15982 ) ;
#6864=CARTESIAN_POINT ( 'NONE',  ( 6.198496396448986090, 45.68315280215533392, 94.24246380123798872 ) ) ;
#6870=VECTOR ( 'NONE', #3769, 1000.000000000000000 ) ;
#6876=VECTOR ( 'NONE', #19763, 1000.000000000000000 ) ;
#6885=ORIENTED_EDGE ( 'NONE', *, *, #13140, .F. ) ;
#6889=CARTESIAN_POINT ( 'NONE',  ( 10.77494014480653561, 42.96218137147968008, 69.80574467885101342 ) ) ;
#6895=DIRECTION ( 'NONE',  ( 0.000000000000000000, -2.891205793294680792E-16, -1.000000000000000000 ) ) ;
#6898=CARTESIAN_POINT ( 'NONE',  ( 1.352400422481993658, 50.46853102219002096, 91.82058880123801714 ) ) ;
#6899=EDGE_CURVE ( 'NONE', #2422, #6639, #15955, .T. ) ;
#6907=CARTESIAN_POINT ( 'NONE',  ( 6.828503391016846891, 43.33193468930419101, 94.16433880123797451 ) ) ;
#6911=EDGE_LOOP ( 'NONE', ( #312, #19792, #11216, #8422 ) ) ;
#6914=FACE_OUTER_BOUND ( 'NONE', #743, .T. ) ;
#6917=CARTESIAN_POINT ( 'NONE',  ( -4.616483944162940389, 41.91660719363136423, 95.05433879953096721 ) ) ;
#6920=CARTESIAN_POINT ( 'NONE',  ( -0.8237052942265477018, 49.18499566818285018, 94.00808880294498238 ) ) ;
#6921=ADVANCED_FACE ( 'NONE', ( #16274 ), #8183, .F. ) ;
#6923=CARTESIAN_POINT ( 'NONE',  ( -0.9988176903691428077, 49.83852402762217082, 90.80496380123797451 ) ) ;
#6928=CARTESIAN_POINT ( 'NONE',  ( -3.226449543290803135, 47.76606447477306716, 95.05433879953076826 ) ) ;
#6929=CARTESIAN_POINT ( 'NONE',  ( -2.416137431568557314, 39.07291177436112406, 93.61746380123797451 ) ) ;
#6935=ORIENTED_EDGE ( 'NONE', *, *, #7556, .T. ) ;
#6947=ORIENTED_EDGE ( 'NONE', *, *, #17676, .T. ) ;
#6949=CARTESIAN_POINT ( 'NONE',  ( -2.904223097202481174, 48.62752260303690122, 93.77371379953099506 ) ) ;
#6950=CARTESIAN_POINT ( 'NONE',  ( -3.943187491250720544, 40.73580453397070755, 92.83621379953099506 ) ) ;
#6951=ORIENTED_EDGE ( 'NONE', *, *, #6328, .T. ) ;
#6952=CARTESIAN_POINT ( 'NONE',  ( 31.07218010054375412, 45.56218137147968861, 64.80574467885102763 ) ) ;
#6957=CARTESIAN_POINT ( 'NONE',  ( -5.058133621542618030, 44.89684013992257405, 91.42996379953099506 ) ) ;
#6960=CARTESIAN_POINT ( 'NONE',  ( -5.154188915835984375, 42.64120994080404614, 94.86746380123797451 ) ) ;
#6963=LINE ( 'NONE', #13062, #3729 ) ;
#6967=ORIENTED_EDGE ( 'NONE', *, *, #11967, .T. ) ;
#6975=CARTESIAN_POINT ( 'NONE',  ( -4.524181921268124462, 40.28999182795290324, 94.94558880123797451 ) ) ;
#6978=CARTESIAN_POINT ( 'NONE',  ( -5.368445182934982185, 36.96218137147968008, 53.35433879953099989 ) ) ;
#6984=CARTESIAN_POINT ( 'NONE',  ( -3.350035803220276609, 49.20851703305431357, 95.88308880123798872 ) ) ;
#6989=CARTESIAN_POINT ( 'NONE',  ( 5.611423337425062385, 41.22389019960463230, 92.67996380123798872 ) ) ;
#6996=AXIS2_PLACEMENT_3D ( 'NONE', #15094, #15195, #3803 ) ;
#7001=CARTESIAN_POINT ( 'NONE',  ( -4.524181921268124462, 40.28999182795290324, 92.44558880123798872 ) ) ;
#7003=CARTESIAN_POINT ( 'NONE',  ( 31.07218010054375412, 42.76218137147968434, 70.80574467885102763 ) ) ;
#7004=EDGE_CURVE ( 'NONE', #9419, #6493, #18706, .T. ) ;
#7006=B_SPLINE_CURVE_WITH_KNOTS ( 'NONE', 3,
 ( #16059, #17751, #8281, #19546, #19751, #3073 ),
 .UNSPECIFIED., .F., .F.,
 ( 4, 2, 4 ),
 ( 0.000000000000000000, 0.001381092432504991453, 0.002762184865009982906 ),
 .UNSPECIFIED. ) ;
#7007=ORIENTED_EDGE ( 'NONE', *, *, #11446, .F. ) ;
#7014=CARTESIAN_POINT ( 'NONE',  ( -4.250200499057710246, 41.08694408590478986, 95.05433879953098142 ) ) ;
#7017=CARTESIAN_POINT ( 'NONE',  ( -3.981178359372548492, 46.76218137147973408, 90.41433880294496817 ) ) ;
#7020=CARTESIAN_POINT ( 'NONE',  ( -5.784195910403845176, 44.99242805365518194, 91.03933880123798872 ) ) ;
#7030=CARTESIAN_POINT ( 'NONE',  ( 5.611423337425062385, 41.22389019960463230, 91.42996380123798872 ) ) ;
#7031=ORIENTED_EDGE ( 'NONE', *, *, #8307, .F. ) ;
#7038=DIRECTION ( 'NONE',  ( -0.000000000000000000, -0.000000000000000000, 1.000000000000000000 ) ) ;
#7041=VECTOR ( 'NONE', #1645, 1000.000000000000000 ) ;
#7046=AXIS2_PLACEMENT_3D ( 'NONE', #7582, #1095, #14265 ) ;
#7049=ORIENTED_EDGE ( 'NONE', *, *, #848, .F. ) ;
#7051=AXIS2_PLACEMENT_3D ( 'NONE', #19054, #15966, #9480 ) ;
#7052=ORIENTED_EDGE ( 'NONE', *, *, #16128, .T. ) ;
#7054=CARTESIAN_POINT ( 'NONE',  ( 3.948530577815480225, 39.69684013992245752, 94.39871379953098085 ) ) ;
#7055=CARTESIAN_POINT ( 'NONE',  ( -4.500660556396669065, 42.81632233694663370, 94.00808879953098085 ) ) ;
#7056=ORIENTED_EDGE ( 'NONE', *, *, #12747, .T. ) ;
#7064=CARTESIAN_POINT ( 'NONE',  ( -3.350035803220276609, 49.20851703305431357, 95.88308880123798872 ) ) ;
#7066=DIRECTION ( 'NONE',  ( 0.000000000000000000, 1.000000000000000000, 0.000000000000000000 ) ) ;
#7067=LINE ( 'NONE', #12309, #14945 ) ;
#7068=CARTESIAN_POINT ( 'NONE',  ( 1.352400422481993658, 50.46853102219002096, 91.82058880123801714 ) ) ;
#7069=VECTOR ( 'NONE', #20233, 1000.000000000000000 ) ;
#7075=EDGE_LOOP ( 'NONE', ( #5563, #19257, #19837, #1962 ) ) ;
#7078=ORIENTED_EDGE ( 'NONE', *, *, #17456, .F. ) ;
#7081=DIRECTION ( 'NONE',  ( 0.000000000000000000, 0.000000000000000000, 1.000000000000000000 ) ) ;
#7086=CARTESIAN_POINT ( 'NONE',  ( -7.677846259693481556, 40.96218137147969429, 93.55433879953098142 ) ) ;
#7089=CARTESIAN_POINT ( 'NONE',  ( -0.4699484075730042676, 52.36218137147968577, 52.53721119516358584 ) ) ;
#7096=CARTESIAN_POINT ( 'NONE',  ( -0.3080929418689875576, 37.85583172076933778, 91.19558880123798872 ) ) ;
#7104=EDGE_CURVE ( 'NONE', #10809, #14970, #18915, .T. ) ;
#7105=CARTESIAN_POINT ( 'NONE',  ( 0.5221537403065020788, 52.36218137147968577, 83.03825919817350609 ) ) ;
#7107=CARTESIAN_POINT ( 'NONE',  ( 1.352400422481993658, 50.46853102219002096, 94.47683880123798872 ) ) ;
#7111=DIRECTION ( 'NONE',  ( -1.334402673828310381E-16, -2.168404344970984808E-15, 1.000000000000000000 ) ) ;
#7115=ORIENTED_EDGE ( 'NONE', *, *, #13140, .T. ) ;
#7116=VECTOR ( 'NONE', #3761, 1000.000000000000000 ) ;
#7119=CARTESIAN_POINT ( 'NONE',  ( 11.22215374030650281, 42.96218137147968008, 65.80574467885102763 ) ) ;
#7122=CARTESIAN_POINT ( 'NONE',  ( -4.755598089612432133, 42.34966066996389600, 95.05433879953096721 ) ) ;
#7126=CARTESIAN_POINT ( 'NONE',  ( 3.122153740306552905, 48.66551347115873227, 91.35183880294498238 ) ) ;
#7130=CARTESIAN_POINT ( 'NONE',  ( 5.568489401881125289, 48.03437091500646261, 92.91433880123798872 ) ) ;
#7139=CARTESIAN_POINT ( 'NONE',  ( 6.198496396448986090, 45.68315280215533392, 92.83621380123798872 ) ) ;
#7144=CARTESIAN_POINT ( 'NONE',  ( -7.677846259693480668, 36.96218137147968008, 92.55433879953098142 ) ) ;
#7164=EDGE_CURVE ( 'NONE', #7741, #19935, #11340, .T. ) ;
#7167=CARTESIAN_POINT ( 'NONE',  ( 4.987494971863720927, 47.58855820898865829, 92.21121379953100927 ) ) ;
#7168=CARTESIAN_POINT ( 'NONE',  ( 3.122153740306552905, 48.66551347115873227, 94.78933879953099506 ) ) ;
#7171=CARTESIAN_POINT ( 'NONE',  ( 6.198496396448986090, 45.68315280215533392, 95.49246380123798872 ) ) ;
#7179=ORIENTED_EDGE ( 'NONE', *, *, #18870, .T. ) ;
#7182=AXIS2_PLACEMENT_3D ( 'NONE', #7105, #20085, #17015 ) ;
#7183=CARTESIAN_POINT ( 'NONE',  ( -0.3080929418689875576, 37.85583172076933778, 91.19558880123798872 ) ) ;
#7195=CARTESIAN_POINT ( 'NONE',  ( 2.043125170982144745, 38.48583871533720213, 95.17996380123798872 ) ) ;
#7207=CARTESIAN_POINT ( 'NONE',  ( -0.9988176903691428077, 49.83852402762217082, 91.89871380123798872 ) ) ;
#7211=CARTESIAN_POINT ( 'NONE',  ( -2.077846259693550746, 39.65884927180063357, 93.22683880294496817 ) ) ;
#7214=ORIENTED_EDGE ( 'NONE', *, *, #20510, .T. ) ;
#7220=CARTESIAN_POINT ( 'NONE',  ( 2.043125170982144745, 38.48583871533720213, 93.92996380123798872 ) ) ;
#7221=ADVANCED_FACE ( 'NONE', ( #935 ), #14025, .F. ) ;
#7227=CARTESIAN_POINT ( 'NONE',  ( -2.077846259693550746, 39.65884927180063357, 93.22683880294496817 ) ) ;
#7233=DIRECTION ( 'NONE',  ( 1.000000000000000000, -0.000000000000000000, -0.000000000000000000 ) ) ;
#7237=CARTESIAN_POINT ( 'NONE',  ( 5.025485839985549319, 41.56218137147963887, 93.53933880294496817 ) ) ;
#7238=( BOUNDED_CURVE ( )  B_SPLINE_CURVE ( 2, ( #11655, #18132, #16536 ),
 .UNSPECIFIED., .F., .F. ) 
 B_SPLINE_CURVE_WITH_KNOTS ( ( 3, 3 ),
 ( 0.2577596748367579904, 0.2583811345117278391 ),
 .UNSPECIFIED. ) 
 CURVE ( )  GEOMETRIC_REPRESENTATION_ITEM ( )  RATIONAL_B_SPLINE_CURVE ( ( 0.9674132986343859653, 0.9666957150223149942, 0.9660722070828959840 ) ) 
 REPRESENTATION_ITEM ( '' )  );
#7243=CARTESIAN_POINT ( 'NONE',  ( 6.198496396448986090, 45.68315280215533392, 92.83621380123798872 ) ) ;
#7249=CARTESIAN_POINT ( 'NONE',  ( -5.154188915835984375, 42.64120994080404614, 92.21121380123797451 ) ) ;
#7253=CARTESIAN_POINT ( 'NONE',  ( 28.52215374030649997, 44.16218137147968292, 87.05433879953099563 ) ) ;
#7260=EDGE_CURVE ( 'NONE', #11839, #10593, #16582, .T. ) ;
#7261=VERTEX_POINT ( 'NONE', #14725 ) ;
#7262=CARTESIAN_POINT ( 'NONE',  ( 30.92220646078100188, 45.56218137147968861, 56.80715055817104542 ) ) ;
#7269=DIRECTION ( 'NONE',  ( -1.000000000000000000, 0.000000000000000000, -1.196361017915039239E-16 ) ) ;
#7273=ADVANCED_FACE ( 'NONE', ( #782 ), #7368, .F. ) ;
#7275=ORIENTED_EDGE ( 'NONE', *, *, #1526, .T. ) ;
#7276=CARTESIAN_POINT ( 'NONE',  ( -4.477846259693498254, 37.66218137147969713, 54.55433879953098852 ) ) ;
#7278=CARTESIAN_POINT ( 'NONE',  ( 5.025485839985549319, 41.56218137147963887, 93.22683879953099506 ) ) ;
#7281=CARTESIAN_POINT ( 'NONE',  ( 2.043125170982144745, 38.48583871533720213, 93.92996380123798872 ) ) ;
#7291=CARTESIAN_POINT ( 'NONE',  ( 6.828503391016846891, 43.33193468930419101, 94.16433880123797451 ) ) ;
#7292=ORIENTED_EDGE ( 'NONE', *, *, #15156, .F. ) ;
#7306=CARTESIAN_POINT ( 'NONE',  ( 6.198496396448986090, 45.68315280215533392, 92.99246380123798872 ) ) ;
#7311=EDGE_LOOP ( 'NONE', ( #7292, #3914, #4590, #11791 ) ) ;
#7315=CARTESIAN_POINT ( 'NONE',  ( 5.611423337425062385, 41.22389019960463230, 92.67996380123805977 ) ) ;
#7318=CARTESIAN_POINT ( 'NONE',  ( 2.043125170982144745, 38.48583871533720213, 95.17996380123798872 ) ) ;
#7321=CARTESIAN_POINT ( 'NONE',  ( 3.122153740306552905, 48.66551347115873227, 91.35183880294498238 ) ) ;
#7322=B_SPLINE_CURVE_WITH_KNOTS ( 'NONE', 3,
 ( #11644, #8335, #18122, #19393, #13022, #8229, #11535, #11331, #19496, #17803, #6830, #3227, #3433, #13336, #14816, #1532, #9832, #19809, #14717, #16110, #20971, #9730, #235, #1637, #137, #13121 ),
 .UNSPECIFIED., .F., .F.,
 ( 4, 2, 2, 2, 2, 2, 2, 2, 2, 2, 2, 2, 4 ),
 ( 0.000000000000000000, 0.001352842588461793333, 0.002029263882692689241, 0.002705685176923584932, 0.004058527765385377614, 0.004734949059616283713, 0.005411370353847190680, 0.006764212942309022827, 0.007440634236539929794, 0.008117055530770836760, 0.008793476825001741992, 0.009469898119232647224, 0.01082274070769447677 ),
 .UNSPECIFIED. ) ;
#7323=LINE ( 'NONE', #13812, #4141 ) ;
#7326=ORIENTED_EDGE ( 'NONE', *, *, #1954, .F. ) ;
#7327=CARTESIAN_POINT ( 'NONE',  ( 8.722153740306483272, 51.36218137147968577, 95.05433879953098142 ) ) ;
#7328=CARTESIAN_POINT ( 'NONE',  ( 4.134898411747151670, 47.90306806511021875, 95.05422504033560926 ) ) ;
#7330=CARTESIAN_POINT ( 'NONE',  ( -5.154188915835984375, 42.64120994080404614, 94.86746380123797451 ) ) ;
#7331=LINE ( 'NONE', #20195, #2064 ) ;
#7336=VERTEX_POINT ( 'NONE', #20017 ) ;
#7341=CARTESIAN_POINT ( 'NONE',  ( -2.931538964508604739, 39.51556981890902165, 95.05433879953095300 ) ) ;
#7343=CARTESIAN_POINT ( 'NONE',  ( 1.256812508749381774, 49.74246873332880625, 91.42996380294499659 ) ) ;
#7346=CARTESIAN_POINT ( 'NONE',  ( -0.9988176903691428077, 49.83852402762217082, 90.64871380123798872 ) ) ;
#7354=CARTESIAN_POINT ( 'NONE',  ( 6.198496396448986090, 45.68315280215533392, 90.33621380123798872 ) ) ;
#7356=FACE_OUTER_BOUND ( 'NONE', #18105, .T. ) ;
#7358=VECTOR ( 'NONE', #4540, 1000.000000000000000 ) ;
#7368=PLANE ( 'NONE',  #12846 ) ;
#7369=ADVANCED_FACE ( 'NONE', ( #10704 ), #17267, .F. ) ;
#7372=PLANE ( 'NONE',  #16264 ) ;
#7381=CARTESIAN_POINT ( 'NONE',  ( 5.544968037009670780, 45.50804040601273925, 92.13308879953099506 ) ) ;
#7384=CARTESIAN_POINT ( 'NONE',  ( 5.568489401881125289, 48.03437091500646261, 93.07058880123797451 ) ) ;
#7391=ORIENTED_EDGE ( 'NONE', *, *, #16848, .T. ) ;
#7392=DIRECTION ( 'NONE',  ( -0.000000000000000000, -0.000000000000000000, 1.000000000000000000 ) ) ;
#7394=AXIS2_PLACEMENT_3D ( 'NONE', #17625, #14907, #332 ) ;
#7395=ORIENTED_EDGE ( 'NONE', *, *, #4396, .F. ) ;
#7396=CARTESIAN_POINT ( 'NONE',  ( 11.22215374030650281, 42.96218137147968008, 65.80574467885102763 ) ) ;
#7402=AXIS2_PLACEMENT_3D ( 'NONE', #14620, #18021, #1758 ) ;
#7410=CARTESIAN_POINT ( 'NONE',  ( -5.784195910403845176, 44.99242805365518194, 92.28933880123798872 ) ) ;
#7411=ORIENTED_EDGE ( 'NONE', *, *, #20873, .T. ) ;
#7412=CARTESIAN_POINT ( 'NONE',  ( 11.22215374030649926, 42.76218137147968434, 69.40574467885102194 ) ) ;
#7418=LINE ( 'NONE', #10748, #7358 ) ;
#7421=DIRECTION ( 'NONE',  ( 0.000000000000000000, -1.000000000000000000, 0.000000000000000000 ) ) ;
#7423=ADVANCED_FACE ( 'NONE', ( #17573 ), #4377, .F. ) ;
#7427=CARTESIAN_POINT ( 'NONE',  ( -5.058133621542618030, 44.89684013992257405, 91.74246380294499659 ) ) ;
#7432=VECTOR ( 'NONE', #5971, 1000.000000000000000 ) ;
#7434=VERTEX_POINT ( 'NONE', #14168 ) ;
#7436=CARTESIAN_POINT ( 'NONE',  ( 10.77494014480653561, 42.96218137147968008, 77.80433879953099563 ) ) ;
#7437=LINE ( 'NONE', #13930, #10943 ) ;
#7443=ORIENTED_EDGE ( 'NONE', *, *, #848, .T. ) ;
#7445=CARTESIAN_POINT ( 'NONE',  ( 28.52215374030649997, 44.16218137147968292, 45.55433879953098852 ) ) ;
#7449=VECTOR ( 'NONE', #5126, 1000.000000000000000 ) ;
#7451=CARTESIAN_POINT ( 'NONE',  ( -0.2125050281363792815, 38.58189400963055959, 90.80496380294498238 ) ) ;
#7452=LINE ( 'NONE', #14049, #8112 ) ;
#7455=ADVANCED_FACE ( 'NONE', ( #14076 ), #2091, .T. ) ;
#7456=CARTESIAN_POINT ( 'NONE',  ( 1.352400422481993658, 50.46853102219002096, 90.57058880123798872 ) ) ;
#7460=DIRECTION ( 'NONE',  ( -0.000000000000000000, -0.000000000000000000, 1.000000000000000000 ) ) ;
#7463=LINE ( 'NONE', #18533, #12587 ) ;
#7464=CARTESIAN_POINT ( 'NONE',  ( 1.256812508749381774, 49.74246873332880625, 92.67996380294498238 ) ) ;
#7470=DIRECTION ( 'NONE',  ( -0.000000000000000000, -0.000000000000000000, 1.000000000000000000 ) ) ;
#7474=ORIENTED_EDGE ( 'NONE', *, *, #15156, .T. ) ;
#7481=VECTOR ( 'NONE', #17174, 1000.000000000000000 ) ;
#7482=CARTESIAN_POINT ( 'NONE',  ( 2.263363662449363822, 49.77488197367694767, 93.19231768333818877 ) ) ;
#7483=LINE ( 'NONE', #14169, #3523 ) ;
#7488=VECTOR ( 'NONE', #11445, 1000.000000000000000 ) ;
#7490=ORIENTED_EDGE ( 'NONE', *, *, #12747, .F. ) ;
#7492=ORIENTED_EDGE ( 'NONE', *, *, #2723, .F. ) ;
#7494=CARTESIAN_POINT ( 'NONE',  ( -5.784195910403845176, 44.99242805365518194, 94.78933880123798872 ) ) ;
#7497=VERTEX_POINT ( 'NONE', #20313 ) ;
#7499=CARTESIAN_POINT ( 'NONE',  ( 6.828503391016846891, 43.33193468930419101, 91.66433880123796030 ) ) ;
#7505=CARTESIAN_POINT ( 'NONE',  ( 11.22215374030649926, 42.76218137147968434, 80.55433879953099563 ) ) ;
#7506=CARTESIAN_POINT ( 'NONE',  ( 6.198496396448986090, 45.68315280215533392, 92.99246380123798872 ) ) ;
#7511=CARTESIAN_POINT ( 'NONE',  ( 1.352400422481993658, 50.46853102219002096, 90.57058880123798872 ) ) ;
#7512=EDGE_CURVE ( 'NONE', #5268, #2768, #15339, .T. ) ;
#7519=ORIENTED_EDGE ( 'NONE', *, *, #16848, .F. ) ;
#7521=CARTESIAN_POINT ( 'NONE',  ( -3.154801521863568325, 47.83913663364971569, 92.55433879953098142 ) ) ;
#7522=CARTESIAN_POINT ( 'NONE',  ( -0.3080929418689875576, 37.85583172076933778, 91.35183880123798872 ) ) ;
#7527=ORIENTED_EDGE ( 'NONE', *, *, #15477, .T. ) ;
#7535=CARTESIAN_POINT ( 'NONE',  ( -3.350035803220276609, 49.20851703305431357, 92.13308880123798872 ) ) ;
#7536=DIRECTION ( 'NONE',  ( 1.000000000000000000, -0.000000000000000000, -0.000000000000000000 ) ) ;
#7539=CARTESIAN_POINT ( 'NONE',  ( -5.058133621542618030, 44.89684013992257405, 94.24246380294498238 ) ) ;
#7542=( NAMED_UNIT ( * ) SI_UNIT ( $, .STERADIAN. ) SOLID_ANGLE_UNIT ( ) );
#7543=VECTOR ( 'NONE', #16161, 1000.000000000000000 ) ;
#7548=EDGE_CURVE ( 'NONE', #7434, #2442, #17238, .T. ) ;
#7556=EDGE_CURVE ( 'NONE', #5762, #7917, #1181, .T. ) ;
#7560=EDGE_CURVE ( 'NONE', #129, #15570, #14364, .T. ) ;
#7565=CARTESIAN_POINT ( 'NONE',  ( 4.394343283833276992, 39.11584570990505938, 92.60183880123797451 ) ) ;
#7566=ADVANCED_FACE ( 'NONE', ( #14248 ), #6264, .F. ) ;
#7569=CARTESIAN_POINT ( 'NONE',  ( -0.9988176903691428077, 49.83852402762217082, 91.89871380123798872 ) ) ;
#7572=AXIS2_PLACEMENT_3D ( 'NONE', #16473, #3684, #282 ) ;
#7575=ORIENTED_EDGE ( 'NONE', *, *, #6724, .F. ) ;
#7577=CARTESIAN_POINT ( 'NONE',  ( -3.981178359372548492, 46.76218137147973408, 92.91433880294496817 ) ) ;
#7582=CARTESIAN_POINT ( 'NONE',  ( 35.92215374030650565, 36.96218137147968719, 93.55433879953098142 ) ) ;
#7583=DIRECTION ( 'NONE',  ( -1.000000000000000000, -1.402518428993831676E-16, -1.196361017915039239E-16 ) ) ;
#7584=ADVANCED_FACE ( 'NONE', ( #20628, #7666, #4351 ), #5859, .F. ) ;
#7590=VERTEX_POINT ( 'NONE', #14144 ) ;
#7592=CARTESIAN_POINT ( 'NONE',  ( -4.524181921268124462, 40.28999182795290324, 93.53933880123797451 ) ) ;
#7595=CARTESIAN_POINT ( 'NONE',  ( 10.77494014480653561, 42.96218137147968008, 77.40433879953098995 ) ) ;
#7597=DIRECTION ( 'NONE',  ( -1.402518428993831676E-16, 1.000000000000000000, 0.000000000000000000 ) ) ;
#7603=CARTESIAN_POINT ( 'NONE',  ( 2.043125170982144745, 38.48583871533720213, 93.92996380123798872 ) ) ;
#7610=CARTESIAN_POINT ( 'NONE',  ( 2.563360104887394630, 38.63792983641098289, 95.05433879953099563 ) ) ;
#7612=CARTESIAN_POINT ( 'NONE',  ( -1.677846259693499542, 50.36218137147968577, 54.55433879953098852 ) ) ;
#7613=CARTESIAN_POINT ( 'NONE',  ( 4.394343283833276992, 39.11584570990505938, 91.50808880123798872 ) ) ;
#7622=EDGE_CURVE ( 'NONE', #10043, #16288, #11171, .T. ) ;
#7623=LINE ( 'NONE', #14003, #9269 ) ;
#7629=CARTESIAN_POINT ( 'NONE',  ( -3.350035803220276609, 49.20851703305431357, 95.72683880123798872 ) ) ;
#7643=CARTESIAN_POINT ( 'NONE',  ( 5.568489401881125289, 48.03437091500646261, 90.57058880123798872 ) ) ;
#7647=CARTESIAN_POINT ( 'NONE',  ( 1.256812508749381774, 49.74246873332880625, 92.67996380294498238 ) ) ;
#7651=CARTESIAN_POINT ( 'NONE',  ( 4.722153740306502812, 44.16218137147969003, 45.55433879953098852 ) ) ;
#7652=CARTESIAN_POINT ( 'NONE',  ( -10.17784625969349754, 51.36218137147968577, 80.55433879953099563 ) ) ;
#7653=CARTESIAN_POINT ( 'NONE',  ( 5.184346195580738836, 46.85389944054460898, 93.43362681315548457 ) ) ;
#7655=CARTESIAN_POINT ( 'NONE',  ( 6.828503391016846891, 43.33193468930419101, 91.66433880123796030 ) ) ;
#7658=EDGE_CURVE ( 'NONE', #14841, #9248, #12360, .T. ) ;
#7663=FACE_OUTER_BOUND ( 'NONE', #20251, .T. ) ;
#7664=CARTESIAN_POINT ( 'NONE',  ( 31.07218010054375412, 42.96218137147968008, 69.40574467885102194 ) ) ;
#7666=FACE_OUTER_BOUND ( 'NONE', #11935, .T. ) ;
#7669=ADVANCED_FACE ( 'NONE', ( #20838 ), #14048, .F. ) ;
#7671=CARTESIAN_POINT ( 'NONE',  ( 4.394343283833276992, 39.11584570990505938, 92.60183880123797451 ) ) ;
#7677=CARTESIAN_POINT ( 'NONE',  ( -3.981178359372548492, 46.76218137147973408, 94.16433880294496817 ) ) ;
#7680=DIRECTION ( 'NONE',  ( 1.402518428993831676E-16, -1.000000000000000000, 0.000000000000000000 ) ) ;
#7684=FACE_OUTER_BOUND ( 'NONE', #17994, .T. ) ;
#7689=ORIENTED_EDGE ( 'NONE', *, *, #2211, .F. ) ;
#7690=CARTESIAN_POINT ( 'NONE',  ( -4.567115856812060670, 47.10047254335474065, 94.55496380123798872 ) ) ;
#7691=CARTESIAN_POINT ( 'NONE',  ( 6.198496396448986090, 45.68315280215533392, 95.33621380123798872 ) ) ;
#7692=CARTESIAN_POINT ( 'NONE',  ( 30.92220646078100188, 42.96218137147968008, 61.80715055817104542 ) ) ;
#7696=ORIENTED_EDGE ( 'NONE', *, *, #4693, .F. ) ;
#7699=EDGE_CURVE ( 'NONE', #8464, #57, #3501, .T. ) ;
#7703=CARTESIAN_POINT ( 'NONE',  ( 4.394343283833276992, 39.11584570990505938, 94.00808880123797451 ) ) ;
#7708=ORIENTED_EDGE ( 'NONE', *, *, #5714, .T. ) ;
#7716=CARTESIAN_POINT ( 'NONE',  ( 6.006122683886344404, 43.48762228702367594, 95.05433879953098142 ) ) ;
#7727=CARTESIAN_POINT ( 'NONE',  ( 11.22215374030650281, 39.96218137147969429, 54.55433879953099563 ) ) ;
#7728=DIRECTION ( 'NONE',  ( 0.000000000000000000, -2.891205793294680792E-16, -1.000000000000000000 ) ) ;
#7729=CARTESIAN_POINT ( 'NONE',  ( 3.460444912181559474, 49.25145096859824889, 93.14871380123798872 ) ) ;
#7731=VERTEX_POINT ( 'NONE', #17766 ) ;
#7732=ORIENTED_EDGE ( 'NONE', *, *, #12768, .T. ) ;
#7741=VERTEX_POINT ( 'NONE', #9794 ) ;
#7745=CARTESIAN_POINT ( 'NONE',  ( -4.524181921268124462, 40.28999182795290324, 93.69558880123800293 ) ) ;
#7746=AXIS2_PLACEMENT_3D ( 'NONE', #14671, #17763, #8077 ) ;
#7751=CARTESIAN_POINT ( 'NONE',  ( 31.22215374030650281, 42.96218137147968008, 73.80433879953100984 ) ) ;
#7754=CARTESIAN_POINT ( 'NONE',  ( -12.18117835937254867, 39.56218137147966019, 95.05433879953098142 ) ) ;
#7757=VECTOR ( 'NONE', #19247, 1000.000000000000000 ) ;
#7767=LINE ( 'NONE', #19051, #15215 ) ;
#7771=AXIS2_PLACEMENT_3D ( 'NONE', #7253, #20118, #18537 ) ;
#7778=CARTESIAN_POINT ( 'NONE',  ( -0.2125050281363792815, 38.58189400963055959, 90.80496380294498238 ) ) ;
#7787=VERTEX_POINT ( 'NONE', #20932 ) ;
#7790=CARTESIAN_POINT ( 'NONE',  ( 6.198496396448986090, 45.68315280215533392, 94.08621380123798872 ) ) ;
#7798=( BOUNDED_CURVE ( )  B_SPLINE_CURVE ( 2, ( #10261, #16736, #2575, #20744, #20641, #4168, #10997, #4263, #1293, #14157, #12575 ),
 .UNSPECIFIED., .F., .F. ) 
 B_SPLINE_CURVE_WITH_KNOTS ( ( 3, 2, 2, 2, 2, 3 ),
 ( 0.3333811345117426717, 0.3499999999999999778, 0.3750000000000000000, 0.4000000000000000222, 0.4249999999999999889, 0.4333811345117426495 ),
 .UNSPECIFIED. ) 
 CURVE ( )  GEOMETRIC_REPRESENTATION_ITEM ( )  RATIONAL_B_SPLINE_CURVE ( ( 0.9660722070828662300, 0.9493985675960723292, 1.000000000000000000, 0.9238795325112867385, 1.000000000000000000, 0.9238795325112867385, 1.000000000000000000, 0.9238795325112867385, 1.000000000000000000, 0.9744809649152144093, 0.9660722070828662300 ) ) 
 REPRESENTATION_ITEM ( '' )  );
#7803=CARTESIAN_POINT ( 'NONE',  ( -2.904223097202481174, 48.62752260303690122, 91.27371379953098085 ) ) ;
#7811=ADVANCED_FACE ( 'NONE', ( #6368 ), #13085, .F. ) ;
#7816=CARTESIAN_POINT ( 'NONE',  ( -5.784195910403845176, 44.99242805365518194, 91.03933880123798872 ) ) ;
#7819=CARTESIAN_POINT ( 'NONE',  ( 4.722153740306502812, 44.16218137147969003, 54.55433879953099563 ) ) ;
#7820=CARTESIAN_POINT ( 'NONE',  ( 5.775515014206123787, 42.15321788283623761, 95.05433879953102405 ) ) ;
#7833=VERTEX_POINT ( 'NONE', #20595 ) ;
#7836=CARTESIAN_POINT ( 'NONE',  ( 11.22215374030650281, 42.96218137147968008, 69.80574467885101342 ) ) ;
#7839=ORIENTED_EDGE ( 'NONE', *, *, #3886, .T. ) ;
#7853=CARTESIAN_POINT ( 'NONE',  ( -4.677846259693495767, 44.16218127507053737, 93.01911326394946400 ) ) ;
#7855=CARTESIAN_POINT ( 'NONE',  ( 4.454354847297358866, 39.79502961122975790, 90.27410626197791998 ) ) ;
#7867=ORIENTED_EDGE ( 'NONE', *, *, #1029, .F. ) ;
#7871=CARTESIAN_POINT ( 'NONE',  ( -1.183761187420877548, 49.81017696809242068, 83.28180655319408743 ) ) ;
#7880=DIRECTION ( 'NONE',  ( 1.000000000000000000, -0.000000000000000000, -0.000000000000000000 ) ) ;
#7881=CARTESIAN_POINT ( 'NONE',  ( 0.5221537403065097394, 44.16218137147969003, 80.55433879953099563 ) ) ;
#7886=CARTESIAN_POINT ( 'NONE',  ( 5.025485839985549319, 41.56218137147963887, 92.28933880294496817 ) ) ;
#7887=ORIENTED_EDGE ( 'NONE', *, *, #1751, .F. ) ;
#7891=CARTESIAN_POINT ( 'NONE',  ( 31.07218010054375412, 45.56218137147968861, 64.80574467885102763 ) ) ;
#7893=VERTEX_POINT ( 'NONE', #19117 ) ;
#7899=VECTOR ( 'NONE', #3477, 1000.000000000000000 ) ;
#7902=ADVANCED_FACE ( 'NONE', ( #8047 ), #14535, .F. ) ;
#7905=EDGE_LOOP ( 'NONE', ( #20554, #6172, #13813, #5532, #3582, #15295, #20649, #5631, #12785, #17662, #5993, #15157 ) ) ;
#7907=CARTESIAN_POINT ( 'NONE',  ( -0.3080929418689875576, 37.85583172076933778, 95.10183880123796030 ) ) ;
#7911=DIRECTION ( 'NONE',  ( 1.334402673828313339E-16, 1.871524341742854397E-32, -1.000000000000000000 ) ) ;
#7914=ADVANCED_FACE ( 'NONE', ( #10074 ), #14745, .F. ) ;
#7917=VERTEX_POINT ( 'NONE', #9757 ) ;
#7921=VERTEX_POINT ( 'NONE', #66 ) ;
#7923=CARTESIAN_POINT ( 'NONE',  ( 4.787119196602786175, 47.27648799119742051, 95.05433879953092458 ) ) ;
#7928=( BOUNDED_SURFACE ( )  B_SPLINE_SURFACE ( 1, 2, ( 
 ( #19623, #1873, #10175, #3460, #6645, #2079, #8361, #14842, #13670, #12401, #7171, #5675, #18778, #9099, #17079, #20469, #18880, #15588, #9212, #2705, #2395, #8998, #20145, #10611, #1004, #15699, #797, #5577, #4288, #12081, #7281, #2505, #20356, #18562, #15485, #5904, #18663, #5794, #4084, #896, #3975, #7384, #1117, #10500, #13772, #10814, #17280, #692, #16965, #13874, #8897, #15384, #20245, #12186, #12299, #10720, #4193, #17179, #2603, #7499, #13987, #539, #18420, #2040, #19797, #13324, #5218, #7020, #10248, #13631, #6923, #15129, #441, #18307, #3528, #13427, #15343, #1931, #3627, #10465, #20106 ),
 ( #10033, #5426, #19895, #18109, #11632, #8855, #327, #16619, #11734, #8426, #16515, #16831, #8649, #13521, #2248, #16930, #18207, #5113, #14904, #5317, #6818, #11833, #10137, #3728, #757, #8536, #15023, #16725, #2149, #3839, #3941, #19994, #2353, #11943, #5544, #10360, #8747, #12050, #18527, #15234, #648, #7130, #7243, #19691, #20537, #7671, #15662, #2883, #1281, #14147, #2466, #4354, #17040, #5752, #7569, #14051, #2781, #9063, #9282, #10879, #15551, #9380, #19056, #13738, #20209, #968, #17352, #12260, #15772, #1183, #7346, #7456, #15867, #2668, #5641, #8961, #10987, #13953, #20434, #12151, #5863 ) ),
 .UNSPECIFIED., .F., .F., .F. ) 
 B_SPLINE_SURFACE_WITH_KNOTS ( ( 2, 2 ),
 ( 3, 2, 2, 2, 2, 2, 2, 2, 2, 2, 2, 2, 2, 2, 2, 2, 2, 2, 2, 2, 2, 2, 2, 2, 2, 2, 2, 2, 2, 2, 2, 2, 2, 2, 2, 2, 2, 2, 2, 2, 3 ),
 ( 0.000000000000000000, 1.000000000000000000 ),
 ( 0.000000000000000000, 0.02500000000000000139, 0.05000000000000000278, 0.07499999999999999722, 0.1000000000000000056, 0.1250000000000000000, 0.1499999999999999944, 0.1749999999999999889, 0.2000000000000000111, 0.2250000000000000056, 0.2500000000000000000, 0.2750000000000000222, 0.2999999999999999889, 0.3250000000000000111, 0.3499999999999999778, 0.3750000000000000000, 0.4000000000000000222, 0.4249999999999999889, 0.4500000000000000111, 0.4749999999999999778, 0.5000000000000000000, 0.5250000000000000222, 0.5500000000000000444, 0.5749999999999999556, 0.5999999999999999778, 0.6250000000000000000, 0.6500000000000000222, 0.6750000000000000444, 0.6999999999999999556, 0.7249999999999999778, 0.7500000000000000000, 0.7750000000000000222, 0.8000000000000000444, 0.8249999999999999556, 0.8499999999999999778, 0.8750000000000000000, 0.9000000000000000222, 0.9250000000000000444, 0.9499999999999999556, 0.9600309411673831894, 0.9696312505790569691 ),
 .UNSPECIFIED. ) 
 GEOMETRIC_REPRESENTATION_ITEM ( )  RATIONAL_B_SPLINE_SURFACE ( (
 ( 1.000000000000000000, 0.9238795325112867385, 1.000000000000000000, 0.9238795325112867385, 1.000000000000000000, 0.9238795325112867385, 1.000000000000000000, 0.9238795325112867385, 1.000000000000000000, 0.9238795325112867385, 1.000000000000000000, 0.9238795325112867385, 1.000000000000000000, 0.9238795325112867385, 1.000000000000000000, 0.9238795325112867385, 1.000000000000000000, 0.9238795325112867385, 1.000000000000000000, 0.9238795325112867385, 1.000000000000000000, 0.9238795325112867385, 1.000000000000000000, 0.9238795325112867385, 1.000000000000000000, 0.9238795325112867385, 1.000000000000000000, 0.9238795325112867385, 1.000000000000000000, 0.9238795325112867385, 1.000000000000000000, 0.9238795325112867385, 1.000000000000000000, 0.9238795325112867385, 1.000000000000000000, 0.9238795325112867385, 1.000000000000000000, 0.9238795325112867385, 1.000000000000000000, 0.9238795325112867385, 1.000000000000000000, 0.9238795325112867385, 1.000000000000000000, 0.9238795325112867385, 1.000000000000000000, 0.9238795325112867385, 1.000000000000000000, 0.9238795325112867385, 1.000000000000000000, 0.9238795325112867385, 1.000000000000000000, 0.9238795325112867385, 1.000000000000000000, 0.9238795325112867385, 1.000000000000000000, 0.9238795325112867385, 1.000000000000000000, 0.9238795325112867385, 1.000000000000000000, 0.9238795325112867385, 1.000000000000000000, 0.9238795325112867385, 1.000000000000000000, 0.9238795325112867385, 1.000000000000000000, 0.9238795325112867385, 1.000000000000000000, 0.9238795325112867385, 1.000000000000000000, 0.9238795325112867385, 1.000000000000000000, 0.9238795325112867385, 1.000000000000000000, 0.9238795325112867385, 1.000000000000000000, 0.9238795325112867385, 1.000000000000000000, 0.9694576027594803413, 0.9634247247054007479, 0.9634247247054007479, 0.9634247247054007479),
 ( 1.000000000000000000, 0.9238795325112867385, 1.000000000000000000, 0.9238795325112867385, 1.000000000000000000, 0.9238795325112867385, 1.000000000000000000, 0.9238795325112867385, 1.000000000000000000, 0.9238795325112867385, 1.000000000000000000, 0.9238795325112867385, 1.000000000000000000, 0.9238795325112867385, 1.000000000000000000, 0.9238795325112867385, 1.000000000000000000, 0.9238795325112867385, 1.000000000000000000, 0.9238795325112867385, 1.000000000000000000, 0.9238795325112867385, 1.000000000000000000, 0.9238795325112867385, 1.000000000000000000, 0.9238795325112867385, 1.000000000000000000, 0.9238795325112867385, 1.000000000000000000, 0.9238795325112867385, 1.000000000000000000, 0.9238795325112867385, 1.000000000000000000, 0.9238795325112867385, 1.000000000000000000, 0.9238795325112867385, 1.000000000000000000, 0.9238795325112867385, 1.000000000000000000, 0.9238795325112867385, 1.000000000000000000, 0.9238795325112867385, 1.000000000000000000, 0.9238795325112867385, 1.000000000000000000, 0.9238795325112867385, 1.000000000000000000, 0.9238795325112867385, 1.000000000000000000, 0.9238795325112867385, 1.000000000000000000, 0.9238795325112867385, 1.000000000000000000, 0.9238795325112867385, 1.000000000000000000, 0.9238795325112867385, 1.000000000000000000, 0.9238795325112867385, 1.000000000000000000, 0.9238795325112867385, 1.000000000000000000, 0.9238795325112867385, 1.000000000000000000, 0.9238795325112867385, 1.000000000000000000, 0.9238795325112867385, 1.000000000000000000, 0.9238795325112867385, 1.000000000000000000, 0.9238795325112867385, 1.000000000000000000, 0.9238795325112867385, 1.000000000000000000, 0.9238795325112867385, 1.000000000000000000, 0.9238795325112867385, 1.000000000000000000, 0.9694576027594803413, 0.9634247247054007479, 0.9634247247054007479, 0.9634247247054007479) ) ) 
 REPRESENTATION_ITEM ( '' )  SURFACE ( )  );
#7931=EDGE_CURVE ( 'NONE', #19935, #10420, #6649, .T. ) ;
#7932=VECTOR ( 'NONE', #5537, 1000.000000000000000 ) ;
#7944=ORIENTED_EDGE ( 'NONE', *, *, #18034, .F. ) ;
#7947=CARTESIAN_POINT ( 'NONE',  ( 4.987494971863720927, 47.58855820898865829, 95.96121379953099506 ) ) ;
#7953=EDGE_LOOP ( 'NONE', ( #14416, #12168, #8050, #9492 ) ) ;
#7955=FACE_OUTER_BOUND ( 'NONE', #14015, .T. ) ;
#7956=CARTESIAN_POINT ( 'NONE',  ( 3.460444912181559474, 49.25145096859824889, 93.14871380123798872 ) ) ;
#7961=ADVANCED_FACE ( 'NONE', ( #14951 ), #19834, .F. ) ;
#7963=LINE ( 'NONE', #14447, #8133 ) ;
#7973=CARTESIAN_POINT ( 'NONE',  ( 5.184346195548518388, 46.85389944066486123, 93.74612681657400515 ) ) ;
#7978=LINE ( 'NONE', #7871, #450 ) ;
#7979=FACE_OUTER_BOUND ( 'NONE', #8826, .T. ) ;
#7984=CARTESIAN_POINT ( 'NONE',  ( -7.677846259693481556, 40.96218137147969429, 45.55433879953098852 ) ) ;
#7989=ORIENTED_EDGE ( 'NONE', *, *, #3915, .T. ) ;
#7990=LINE ( 'NONE', #12570, #8524 ) ;
#7997=DIRECTION ( 'NONE',  ( 1.000000000000000000, 1.213411507412056509E-16, -0.000000000000000000 ) ) ;
#8001=CARTESIAN_POINT ( 'NONE',  ( 2.043125170982144745, 38.48583871533720213, 95.02371380123798872 ) ) ;
#8002=CARTESIAN_POINT ( 'NONE',  ( -3.350035803220276609, 49.20851703305431357, 91.97683880123797451 ) ) ;
#8003=CARTESIAN_POINT ( 'NONE',  ( 4.722153740306502812, 44.16218137147969003, 45.55433879953098852 ) ) ;
#8004=DIRECTION ( 'NONE',  ( 1.402518428993831676E-16, -1.000000000000000000, 0.000000000000000000 ) ) ;
#8007=ORIENTED_EDGE ( 'NONE', *, *, #3657, .T. ) ;
#8011=CARTESIAN_POINT ( 'NONE',  ( -4.524181921268124462, 40.28999182795290324, 91.19558880123797451 ) ) ;
#8012=CARTESIAN_POINT ( 'NONE',  ( 6.198496396448986090, 45.68315280215533392, 95.33621380123798872 ) ) ;
#8018=EDGE_CURVE ( 'NONE', #16288, #11321, #3667, .T. ) ;
#8021=CARTESIAN_POINT ( 'NONE',  ( -4.344483343973046807, 41.29210034554949971, 92.55433879953100984 ) ) ;
#8047=FACE_OUTER_BOUND ( 'NONE', #10852, .T. ) ;
#8049=CARTESIAN_POINT ( 'NONE',  ( 1.868012774839550749, 39.13936707477651566, 95.57058879953099506 ) ) ;
#8050=ORIENTED_EDGE ( 'NONE', *, *, #6651, .F. ) ;
#8054=VECTOR ( 'NONE', #432, 1000.000000000000000 ) ;
#8057=DIRECTION ( 'NONE',  ( 0.000000000000000000, 1.000000000000000000, 1.734723475976787846E-14 ) ) ;
#8059=CARTESIAN_POINT ( 'NONE',  ( 6.102441102155617969, 43.42752260303680600, 89.86746380294499659 ) ) ;
#8071=VECTOR ( 'NONE', #7536, 1000.000000000000000 ) ;
#8077=DIRECTION ( 'NONE',  ( 1.000000000000000000, 0.000000000000000000, -0.000000000000000000 ) ) ;
#8081=CARTESIAN_POINT ( 'NONE',  ( 31.07218010054375412, 42.76218137147968434, 70.80574467885102763 ) ) ;
#8083=EDGE_CURVE ( 'NONE', #18535, #2175, #13560, .T. ) ;
#8085=CARTESIAN_POINT ( 'NONE',  ( 1.352400422481993658, 50.46853102219002096, 93.07058880123798872 ) ) ;
#8086=ORIENTED_EDGE ( 'NONE', *, *, #2166, .F. ) ;
#8096=DIRECTION ( 'NONE',  ( -1.334402673828316297E-16, 2.168404344970984808E-15, 1.000000000000000000 ) ) ;
#8102=CIRCLE ( 'NONE', #7771, 4.199999999999999289 ) ;
#8104=CARTESIAN_POINT ( 'NONE',  ( 2.043125170982144745, 38.48583871533720213, 91.27371380123798872 ) ) ;
#8109=DIRECTION ( 'NONE',  ( -1.000000000000000000, -1.402518428993831676E-16, -1.196361017915039239E-16 ) ) ;
#8112=VECTOR ( 'NONE', #4154, 1000.000000000000000 ) ;
#8115=CARTESIAN_POINT ( 'NONE',  ( 5.568489401881125289, 48.03437091500646261, 90.57058880123798872 ) ) ;
#8116=CARTESIAN_POINT ( 'NONE',  ( 3.460444912181559474, 49.25145096859824889, 94.24246380123798872 ) ) ;
#8125=EDGE_LOOP ( 'NONE', ( #7391, #10201, #13777, #10916 ) ) ;
#8131=PLANE ( 'NONE',  #16445 ) ;
#8133=VECTOR ( 'NONE', #19136, 1000.000000000000000 ) ;
#8137=FACE_OUTER_BOUND ( 'NONE', #13231, .T. ) ;
#8138=EDGE_CURVE ( 'NONE', #1661, #20573, #2285, .T. ) ;
#8143=DIRECTION ( 'NONE',  ( 1.402518428993831676E-16, -1.000000000000000000, 0.000000000000000000 ) ) ;
#8144=EDGE_LOOP ( 'NONE', ( #12012, #6096, #2695, #10400 ) ) ;
#8151=CARTESIAN_POINT ( 'NONE',  ( 5.544968037009670780, 45.50804040601273925, 94.63308879953099506 ) ) ;
#8161=CARTESIAN_POINT ( 'NONE',  ( 1.256812508749381774, 49.74246873332880625, 90.17996380294496817 ) ) ;
#8162=CIRCLE ( 'NONE', #5427, 4.200000000000001066 ) ;
#8168=ORIENTED_EDGE ( 'NONE', *, *, #1045, .F. ) ;
#8176=ORIENTED_EDGE ( 'NONE', *, *, #19493, .F. ) ;
#8183=PLANE ( 'NONE',  #7746 ) ;
#8187=CARTESIAN_POINT ( 'NONE',  ( 1.352400422481993658, 50.46853102219002096, 90.57058880123798872 ) ) ;
#8191=DIRECTION ( 'NONE',  ( 1.000000000000000000, 1.402518428993831676E-16, 0.000000000000000000 ) ) ;
#8207=VERTEX_POINT ( 'NONE', #5125 ) ;
#8212=CARTESIAN_POINT ( 'NONE',  ( -3.350035803220276609, 49.20851703305431357, 90.72683880123797451 ) ) ;
#8224=B_SPLINE_CURVE_WITH_KNOTS ( 'NONE', 3,
 ( #13178, #2987, #3589, #15980, #6780, #13075 ),
 .UNSPECIFIED., .F., .F.,
 ( 4, 2, 4 ),
 ( 0.000000000000000000, 0.001391361808504449618, 0.002782723617008899235 ),
 .UNSPECIFIED. ) ;
#8228=LINE ( 'NONE', #11430, #16742 ) ;
#8229=CARTESIAN_POINT ( 'NONE',  ( 4.677786616261469632, 40.19619496325550756, 92.55433879953091036 ) ) ;
#8234=CARTESIAN_POINT ( 'NONE',  ( 11.22215374030650281, 45.56218137147968150, 72.80433879953100984 ) ) ;
#8236=ORIENTED_EDGE ( 'NONE', *, *, #17950, .T. ) ;
#8239=VECTOR ( 'NONE', #5106, 1000.000000000000000 ) ;
#8243=DIRECTION ( 'NONE',  ( 0.000000000000000000, 0.000000000000000000, -1.000000000000000000 ) ) ;
#8250=VECTOR ( 'NONE', #14609, 1000.000000000000000 ) ;
#8251=LINE ( 'NONE', #19727, #13597 ) ;
#8253=DIRECTION ( 'NONE',  ( 0.000000000000000000, 0.000000000000000000, 1.000000000000000000 ) ) ;
#8256=CARTESIAN_POINT ( 'NONE',  ( 4.394343283833276104, 39.11584570990505938, 94.00808880123798872 ) ) ;
#8258=ORIENTED_EDGE ( 'NONE', *, *, #16774, .F. ) ;
#8259=CARTESIAN_POINT ( 'NONE',  ( 4.199109002476567376, 47.83913663364971569, 83.28180655319408743 ) ) ;
#8260=CARTESIAN_POINT ( 'NONE',  ( -7.677846259693483333, 47.36218137147966445, 80.55433879953099563 ) ) ;
#8261=CARTESIAN_POINT ( 'NONE',  ( -4.500660556396669065, 42.81632233694663370, 96.50808879953099506 ) ) ;
#8268=CARTESIAN_POINT ( 'NONE',  ( -10.17784625969349754, 51.36218137147968577, 54.55433879953098852 ) ) ;
#8271=CARTESIAN_POINT ( 'NONE',  ( -4.524181921268124462, 40.28999182795290324, 93.53933880123797451 ) ) ;
#8281=CARTESIAN_POINT ( 'NONE',  ( -1.856544280600664454, 49.13739387491266086, 94.21485748750063749 ) ) ;
#8284=ORIENTED_EDGE ( 'NONE', *, *, #1633, .T. ) ;
#8286=CARTESIAN_POINT ( 'NONE',  ( 35.92215374030650565, 40.96218137147972982, 93.55433879953098142 ) ) ;
#8288=DIRECTION ( 'NONE',  ( 0.000000000000000000, 0.000000000000000000, -1.000000000000000000 ) ) ;
#8289=CARTESIAN_POINT ( 'NONE',  ( 13.32022995165973001, 36.96218137147968719, 92.39963826115175038 ) ) ;
#8291=EDGE_CURVE ( 'NONE', #15187, #15788, #7322, .T. ) ;
#8292=CARTESIAN_POINT ( 'NONE',  ( 0.5221537403065010796, 44.16218137147969003, 77.84651775085080772 ) ) ;
#8293=CYLINDRICAL_SURFACE ( 'NONE', #2516, 5.199999999999999289 ) ;
#8299=CARTESIAN_POINT ( 'NONE',  ( -5.154188915835984375, 42.64120994080404614, 92.21121380123797451 ) ) ;
#8307=EDGE_CURVE ( 'NONE', #19372, #15205, #8102, .T. ) ;
#8309=EDGE_LOOP ( 'NONE', ( #15812, #6395, #18426, #6518, #19654, #9121, #8328, #4518 ) ) ;
#8315=CARTESIAN_POINT ( 'NONE',  ( 33.61275266354798674, 51.36218137147967866, 93.55433879953098142 ) ) ;
#8317=EDGE_CURVE ( 'NONE', #899, #18234, #20329, .T. ) ;
#8321=CARTESIAN_POINT ( 'NONE',  ( 1.256812508749381774, 49.74246873332880625, 95.17996380294498238 ) ) ;
#8326=ORIENTED_EDGE ( 'NONE', *, *, #19242, .F. ) ;
#8327=FACE_OUTER_BOUND ( 'NONE', #18590, .T. ) ;
#8328=ORIENTED_EDGE ( 'NONE', *, *, #1418, .T. ) ;
#8330=CARTESIAN_POINT ( 'NONE',  ( -0.9988176903691428077, 49.83852402762217082, 92.05496380123798872 ) ) ;
#8331=CARTESIAN_POINT ( 'NONE',  ( -3.350035803220276609, 49.20851703305431357, 95.72683880123798872 ) ) ;
#8335=CARTESIAN_POINT ( 'NONE',  ( 3.321300766213236333, 39.00526535449171206, 92.55433879953098142 ) ) ;
#8339=LINE ( 'NONE', #14821, #11574 ) ;
#8358=PLANE ( 'NONE',  #13658 ) ;
#8359=CARTESIAN_POINT ( 'NONE',  ( 4.987494971863720927, 47.58855820898865829, 95.96121379953099506 ) ) ;
#8361=CARTESIAN_POINT ( 'NONE',  ( -0.9988176903691428077, 49.83852402762217082, 95.80496380123798872 ) ) ;
#8365=LINE ( 'NONE', #11674, #17326 ) ;
#8366=CARTESIAN_POINT ( 'NONE',  ( 1.868012774839550749, 39.13936707477651566, 94.32058879953099506 ) ) ;
#8368=( BOUNDED_CURVE ( )  B_SPLINE_CURVE ( 2, ( #8932, #12224, #10858, #20509, #18601, #10754, #15633, #4015, #17219, #10536, #17006 ),
 .UNSPECIFIED., .F., .F. ) 
 B_SPLINE_CURVE_WITH_KNOTS ( ( 3, 2, 2, 2, 2, 3 ),
 ( 0.1389341928972610829, 0.1562449552883616588, 0.1822857811697578267, 0.2083266070511540224, 0.2343674329325501626, 0.2430974982970244558 ),
 .UNSPECIFIED. ) 
 CURVE ( )  GEOMETRIC_REPRESENTATION_ITEM ( )  RATIONAL_B_SPLINE_CURVE ( ( 0.9660722130355270387, 0.9493985585634596713, 1.000000000000000000, 0.9238795325112867385, 1.000000000000000000, 0.9238795325112867385, 1.000000000000000000, 0.9238795325112867385, 1.000000000000000000, 0.9744809684693772622, 0.9660722094251257275 ) ) 
 REPRESENTATION_ITEM ( '' )  );
#8376=VERTEX_POINT ( 'NONE', #18754 ) ;
#8390=EDGE_CURVE ( 'NONE', #7590, #899, #13848, .T. ) ;
#8391=PLANE ( 'NONE',  #3621 ) ;
#8396=CARTESIAN_POINT ( 'NONE',  ( 6.828503391016846891, 43.33193468930419101, 94.00808880123805977 ) ) ;
#8400=CARTESIAN_POINT ( 'NONE',  ( 5.568489401881125289, 48.03437091500646261, 91.66433880123796030 ) ) ;
#8402=CARTESIAN_POINT ( 'NONE',  ( -0.9988176903691428077, 49.83852402762217082, 93.14871380123798872 ) ) ;
#8404=DIRECTION ( 'NONE',  ( 1.000000000000000000, 0.000000000000000000, 0.000000000000000000 ) ) ;
#8416=DIRECTION ( 'NONE',  ( 1.000000000000000000, 0.000000000000000000, 0.000000000000000000 ) ) ;
#8422=ORIENTED_EDGE ( 'NONE', *, *, #8730, .F. ) ;
#8423=CARTESIAN_POINT ( 'NONE',  ( -0.2125050281363792815, 38.58189400963055959, 94.55496380294496817 ) ) ;
#8426=CARTESIAN_POINT ( 'NONE',  ( 5.568489401881125289, 48.03437091500646261, 95.41433880123797451 ) ) ;
#8428=ORIENTED_EDGE ( 'NONE', *, *, #5992, .F. ) ;
#8435=CYLINDRICAL_SURFACE ( 'NONE', #2132, 0.9921021478795020165 ) ;
#8448=CARTESIAN_POINT ( 'NONE',  ( 11.22215374030649926, 42.96218137147968008, 77.80433879953099563 ) ) ;
#8450=LINE ( 'NONE', #10276, #14672 ) ;
#8459=EDGE_CURVE ( 'NONE', #11174, #14841, #7798, .T. ) ;
#8463=CARTESIAN_POINT ( 'NONE',  ( -3.981178359372548492, 46.76218137147973408, 93.85183879953099506 ) ) ;
#8464=VERTEX_POINT ( 'NONE', #19066 ) ;
#8465=DIRECTION ( 'NONE',  ( 1.000000000000000000, 0.000000000000000000, 1.196361017915039239E-16 ) ) ;
#8470=EDGE_CURVE ( 'NONE', #7731, #129, #20547, .T. ) ;
#8471=CARTESIAN_POINT ( 'NONE',  ( 4.987494971863720927, 47.58855820898865829, 92.21121379953100927 ) ) ;
#8475=VECTOR ( 'NONE', #11273, 1000.000000000000000 ) ;
#8489=PLANE ( 'NONE',  #20364 ) ;
#8498=PLANE ( 'NONE',  #792 ) ;
#8501=DIRECTION ( 'NONE',  ( -1.000000000000000000, 0.000000000000000000, 0.000000000000000000 ) ) ;
#8504=CARTESIAN_POINT ( 'NONE',  ( -3.638881865704250096, 47.35505628976589065, 94.13950776816832899 ) ) ;
#8509=CARTESIAN_POINT ( 'NONE',  ( -4.524181921268124462, 40.28999182795290324, 92.28933880123798872 ) ) ;
#8512=CARTESIAN_POINT ( 'NONE',  ( 6.828503391016846891, 43.33193468930419101, 92.75808880123800293 ) ) ;
#8518=CARTESIAN_POINT ( 'NONE',  ( 5.544968037009670780, 45.50804040601273925, 90.88308879953099506 ) ) ;
#8521=CARTESIAN_POINT ( 'NONE',  ( 5.025485839985549319, 41.56218137147963887, 93.53933880294496817 ) ) ;
#8522=ORIENTED_EDGE ( 'NONE', *, *, #20293, .F. ) ;
#8524=VECTOR ( 'NONE', #6374, 1000.000000000000000 ) ;
#8532=CARTESIAN_POINT ( 'NONE',  ( -3.981178359372548492, 46.76218137147973408, 94.16433880294496817 ) ) ;
#8534=EDGE_CURVE ( 'NONE', #3734, #16713, #2665, .T. ) ;
#8536=CARTESIAN_POINT ( 'NONE',  ( 5.568489401881125289, 48.03437091500646261, 94.16433880123797451 ) ) ;
#8538=CARTESIAN_POINT ( 'NONE',  ( 31.22215374030650281, 45.56218137147968861, 78.80433879953099563 ) ) ;
#8541=EDGE_LOOP ( 'NONE', ( #2359, #17579, #7527, #10235 ) ) ;
#8544=CARTESIAN_POINT ( 'NONE',  ( 4.394343283833276992, 39.11584570990505938, 91.35183880123798872 ) ) ;
#8560=VECTOR ( 'NONE', #8253, 1000.000000000000000 ) ;
#8568=ORIENTED_EDGE ( 'NONE', *, *, #14446, .T. ) ;
#8571=CARTESIAN_POINT ( 'NONE',  ( 6.102441102155617969, 43.42752260303680600, 95.80496379953099506 ) ) ;
#8572=CARTESIAN_POINT ( 'NONE',  ( -0.2125050281363792815, 38.58189400963055959, 95.49246379953098085 ) ) ;
#8582=CARTESIAN_POINT ( 'NONE',  ( -4.500660556396669065, 42.81632233694663370, 91.50808879953098085 ) ) ;
#8586=CARTESIAN_POINT ( 'NONE',  ( 4.613683346302097199, 40.84891852973634485, 90.69696562749766144 ) ) ;
#8591=EDGE_CURVE ( 'NONE', #972, #2580, #10594, .T. ) ;
#8607=CARTESIAN_POINT ( 'NONE',  ( -0.9988176903691428077, 49.83852402762217082, 93.30496380123798872 ) ) ;
#8621=EDGE_CURVE ( 'NONE', #17446, #3176, #20227, .T. ) ;
#8622=CARTESIAN_POINT ( 'NONE',  ( -0.9988176903691428077, 49.83852402762217082, 90.64871380123798872 ) ) ;
#8631=FACE_OUTER_BOUND ( 'NONE', #9849, .T. ) ;
#8633=CARTESIAN_POINT ( 'NONE',  ( -5.784195910403845176, 44.99242805365518194, 92.28933880123798872 ) ) ;
#8647=CARTESIAN_POINT ( 'NONE',  ( -2.077846259693550746, 39.65884927180063357, 93.22683880294496817 ) ) ;
#8649=CARTESIAN_POINT ( 'NONE',  ( 5.611423337425062385, 41.22389019960463230, 95.17996380123798872 ) ) ;
#8650=DIRECTION ( 'NONE',  ( -0.000000000000000000, 1.000000000000000000, 1.734723475976787531E-14 ) ) ;
#8654=CARTESIAN_POINT ( 'NONE',  ( -1.856544280600658459, 49.13739387491266086, 92.96485748750068012 ) ) ;
#8655=CARTESIAN_POINT ( 'NONE',  ( 6.828503391016846891, 43.33193468930419101, 92.75808880123800293 ) ) ;
#8659=LINE ( 'NONE', #20445, #5743 ) ;
#8664=LINE ( 'NONE', #10267, #14957 ) ;
#8669=CARTESIAN_POINT ( 'NONE',  ( 6.198496396448986090, 45.68315280215533392, 92.99246380123798872 ) ) ;
#8672=CARTESIAN_POINT ( 'NONE',  ( -3.154801521863568325, 47.83913663364971569, 95.05433879953098142 ) ) ;
#8675=VERTEX_POINT ( 'NONE', #8448 ) ;
#8676=LINE ( 'NONE', #1869, #7116 ) ;
#8679=CARTESIAN_POINT ( 'NONE',  ( -3.981178359372548492, 46.76218137147973408, 92.60183879953099506 ) ) ;
#8680=CARTESIAN_POINT ( 'NONE',  ( 1.868012774839550749, 39.13936707477651566, 91.82058879953099506 ) ) ;
#8683=CARTESIAN_POINT ( 'NONE',  ( -2.416137431568557314, 39.07291177436112406, 94.86746380123805977 ) ) ;
#8685=CARTESIAN_POINT ( 'NONE',  ( 13.32277635493561974, 51.36218137147968577, 80.55433879953099563 ) ) ;
#8687=CARTESIAN_POINT ( 'NONE',  ( -1.677846259693499542, 50.36218137147968577, 50.15433879953098995 ) ) ;
#8691=CARTESIAN_POINT ( 'NONE',  ( -4.524181921268124462, 40.28999182795290324, 91.03933880123798872 ) ) ;
#8694=EDGE_CURVE ( 'NONE', #13124, #12799, #4072, .T. ) ;
#8695=DIRECTION ( 'NONE',  ( 1.193617070626243484E-16, 1.000000000000000000, 0.000000000000000000 ) ) ;
#8698=EDGE_LOOP ( 'NONE', ( #9489, #14853, #17466, #9601, #581, #18904 ) ) ;
#8699=CARTESIAN_POINT ( 'NONE',  ( -0.4699484075730043786, 51.36218137147968577, 52.53721119516358584 ) ) ;
#8704=CARTESIAN_POINT ( 'NONE',  ( 6.828503391016846891, 43.33193468930419101, 94.16433880123797451 ) ) ;
#8708=CARTESIAN_POINT ( 'NONE',  ( 10.77494014480653561, 42.96218137147968008, 66.20574467885104752 ) ) ;
#8710=CARTESIAN_POINT ( 'NONE',  ( 11.22215374030650281, 45.56218137147968150, 56.80715055817104542 ) ) ;
#8717=CARTESIAN_POINT ( 'NONE',  ( -1.219056181852248066, 49.77488197367201650, 94.48425466814985896 ) ) ;
#8718=CARTESIAN_POINT ( 'NONE',  ( -5.154188915835984375, 42.64120994080404614, 90.96121380123797451 ) ) ;
#8720=DIRECTION ( 'NONE',  ( -0.000000000000000000, -0.000000000000000000, 1.000000000000000000 ) ) ;
#8724=DIRECTION ( 'NONE',  ( 1.193617070626243484E-16, 1.000000000000000000, 0.000000000000000000 ) ) ;
#8725=CARTESIAN_POINT ( 'NONE',  ( 2.043125170982144745, 38.48583871533720213, 95.17996380123798872 ) ) ;
#8726=EDGE_CURVE ( 'NONE', #2422, #13701, #12388, .T. ) ;
#8727=CARTESIAN_POINT ( 'NONE',  ( -5.677846259693490438, 44.16218137147969003, 111.0905869729573681 ) ) ;
#8729=CARTESIAN_POINT ( 'NONE',  ( 3.547567743947614538, 48.49067789217866675, 94.73725702289965511 ) ) ;
#8730=EDGE_CURVE ( 'NONE', #15997, #18224, #4276, .T. ) ;
#8737=CARTESIAN_POINT ( 'NONE',  ( -7.677846259693483333, 47.36218137147966445, 93.55433879953098142 ) ) ;
#8744=CARTESIAN_POINT ( 'NONE',  ( 1.868012774839550749, 39.13936707477651566, 93.38308880294498238 ) ) ;
#8747=CARTESIAN_POINT ( 'NONE',  ( -4.567115856812060670, 47.10047254335474065, 93.30496380123798872 ) ) ;
#8754=CARTESIAN_POINT ( 'NONE',  ( 1.352400422481993658, 50.46853102219002096, 90.57058880123798872 ) ) ;
#8761=ADVANCED_FACE ( 'NONE', ( #18966 ), #15685, .F. ) ;
#8767=CARTESIAN_POINT ( 'NONE',  ( 1.514255888186003984, 52.36218137147968577, 83.03825919817350609 ) ) ;
#8769=CARTESIAN_POINT ( 'NONE',  ( 10.77494014480653917, 42.76218137147968434, 61.40715055817103263 ) ) ;
#8778=CARTESIAN_POINT ( 'NONE',  ( 6.102441102155617969, 43.42752260303680600, 92.05496379953099506 ) ) ;
#8779=CARTESIAN_POINT ( 'NONE',  ( 3.122153740306552905, 48.66551347115873227, 92.28933879953099506 ) ) ;
#8783=LINE ( 'NONE', #1006, #15040 ) ;
#8785=DIRECTION ( 'NONE',  ( -0.000000000000000000, -0.000000000000000000, 1.000000000000000000 ) ) ;
#8788=LINE ( 'NONE', #7505, #9872 ) ;
#8789=CARTESIAN_POINT ( 'NONE',  ( -5.784195910403845176, 44.99242805365518194, 93.53933880123797451 ) ) ;
#8794=LINE ( 'NONE', #2408, #17458 ) ;
#8795=DIRECTION ( 'NONE',  ( -0.000000000000000000, -0.000000000000000000, 1.000000000000000000 ) ) ;
#8799=ORIENTED_EDGE ( 'NONE', *, *, #3605, .F. ) ;
#8801=VERTEX_POINT ( 'NONE', #7692 ) ;
#8803=PLANE ( 'NONE',  #12960 ) ;
#8804=CARTESIAN_POINT ( 'NONE',  ( 6.198496396448986090, 45.68315280215533392, 95.49246380123798872 ) ) ;
#8807=EDGE_CURVE ( 'NONE', #6493, #7731, #9306, .T. ) ;
#8815=CARTESIAN_POINT ( 'NONE',  ( 3.460444912181559474, 49.25145096859824889, 94.39871380123798872 ) ) ;
#8819=CARTESIAN_POINT ( 'NONE',  ( 3.122153740306552905, 48.66551347115873227, 92.60183880294498238 ) ) ;
#8824=PRESENTATION_STYLE_ASSIGNMENT (( #4446 ) ) ;
#8826=EDGE_LOOP ( 'NONE', ( #12983, #11592, #2797, #12368 ) ) ;
#8827=LINE ( 'NONE', #5401, #2358 ) ;
#8830=CARTESIAN_POINT ( 'NONE',  ( 3.122153740306552905, 48.66551347115873227, 91.03933879953099506 ) ) ;
#8839=ORIENTED_EDGE ( 'NONE', *, *, #4123, .T. ) ;
#8841=EDGE_CURVE ( 'NONE', #15205, #19372, #965, .T. ) ;
#8843=DIRECTION ( 'NONE',  ( -0.000000000000000000, -0.000000000000000000, 1.000000000000000000 ) ) ;
#8846=CARTESIAN_POINT ( 'NONE',  ( -1.998366399307998753, 38.86341998953714238, 95.05433879953095300 ) ) ;
#8852=CARTESIAN_POINT ( 'NONE',  ( -5.154188915835984375, 42.64120994080404614, 92.21121380123797451 ) ) ;
#8853=ADVANCED_FACE ( 'NONE', ( #13975 ), #7372, .F. ) ;
#8855=CARTESIAN_POINT ( 'NONE',  ( -3.350035803220276609, 49.20851703305431357, 95.72683880123798872 ) ) ;
#8863=VECTOR ( 'NONE', #5357, 1000.000000000000000 ) ;
#8866=CARTESIAN_POINT ( 'NONE',  ( -0.3080929418689875576, 37.85583172076933778, 92.44558880123798872 ) ) ;
#8874=ORIENTED_EDGE ( 'NONE', *, *, #17335, .F. ) ;
#8877=VERTEX_POINT ( 'NONE', #19480 ) ;
#8879=PLANE ( 'NONE',  #20936 ) ;
#8881=CARTESIAN_POINT ( 'NONE',  ( 6.828503391016846891, 43.33193468930419101, 92.91433880123800293 ) ) ;
#8886=ORIENTED_EDGE ( 'NONE', *, *, #13038, .T. ) ;
#8887=EDGE_CURVE ( 'NONE', #3265, #895, #9817, .T. ) ;
#8891=DIRECTION ( 'NONE',  ( 0.7071067811865433539, -0.7071067811865517916, 1.146387601258590612E-16 ) ) ;
#8892=CARTESIAN_POINT ( 'NONE',  ( 1.868012774839550749, 39.13936707477651566, 95.57058879953099506 ) ) ;
#8893=CARTESIAN_POINT ( 'NONE',  ( -2.904223097202481174, 48.62752260303690122, 91.27371379953098085 ) ) ;
#8896=ORIENTED_EDGE ( 'NONE', *, *, #16127, .F. ) ;
#8897=CARTESIAN_POINT ( 'NONE',  ( -5.154188915835984375, 42.64120994080404614, 92.36746380123797451 ) ) ;
#8900=DIRECTION ( 'NONE',  ( 0.8660254037844395958, -0.4999999999999985012, 0.000000000000000000 ) ) ;
#8903=CARTESIAN_POINT ( 'NONE',  ( 6.828503391016846891, 43.33193468930419101, 95.41433880123797451 ) ) ;
#8907=CARTESIAN_POINT ( 'NONE',  ( 30.92220646078100188, 42.76218137147968434, 62.80715055817104542 ) ) ;
#8908=VECTOR ( 'NONE', #946, 1000.000000000000000 ) ;
#8913=EDGE_LOOP ( 'NONE', ( #16647, #18049, #8874, #13961 ) ) ;
#8919=CARTESIAN_POINT ( 'NONE',  ( -0.9988176903691428077, 49.83852402762217082, 95.80496380123798872 ) ) ;
#8924=CARTESIAN_POINT ( 'NONE',  ( -1.183761187420877548, 49.81017696809242068, 92.55433879953098142 ) ) ;
#8925=CARTESIAN_POINT ( 'NONE',  ( 2.891178764483326002, 49.58011693221236271, 93.01356103993782654 ) ) ;
#8927=LINE ( 'NONE', #18495, #17086 ) ;
#8928=CARTESIAN_POINT ( 'NONE',  ( 5.611423337425062385, 41.22389019960463230, 94.08621380123797451 ) ) ;
#8931=CARTESIAN_POINT ( 'NONE',  ( 31.07218010054375412, 42.76218137147968434, 70.80574467885102763 ) ) ;
#8932=CARTESIAN_POINT ( 'NONE',  ( 5.722153740306476166, 44.16218185472587976, 94.89411094854372664 ) ) ;
#8933=CARTESIAN_POINT ( 'NONE',  ( 6.102441102155617969, 43.42752260303680600, 94.86746380294499659 ) ) ;
#8939=CARTESIAN_POINT ( 'NONE',  ( 6.102441102155617969, 43.42752260303680600, 90.80496379953099506 ) ) ;
#8941=CARTESIAN_POINT ( 'NONE',  ( -7.677846259693480668, 36.96218137147968008, 53.35433879953099989 ) ) ;
#8946=ORIENTED_EDGE ( 'NONE', *, *, #19352, .T. ) ;
#8949=CARTESIAN_POINT ( 'NONE',  ( 30.92220646078100188, 42.96218137147968008, 57.80715055817105252 ) ) ;
#8952=CARTESIAN_POINT ( 'NONE',  ( -4.524181921268124462, 40.28999182795290324, 94.94558880123797451 ) ) ;
#8956=CARTESIAN_POINT ( 'NONE',  ( -0.8237052942265477018, 49.18499566818285018, 91.50808880294498238 ) ) ;
#8958=VECTOR ( 'NONE', #11936, 1000.000000000000000 ) ;
#8961=CARTESIAN_POINT ( 'NONE',  ( 6.828503391016846891, 43.33193468930419101, 90.25808880123800293 ) ) ;
#8963=VERTEX_POINT ( 'NONE', #8003 ) ;
#8966=ORIENTED_EDGE ( 'NONE', *, *, #9457, .T. ) ;
#8967=PLANE ( 'NONE',  #3730 ) ;
#8968=CARTESIAN_POINT ( 'NONE',  ( -5.154188915835984375, 42.64120994080404614, 90.96121380123797451 ) ) ;
#8970=ADVANCED_FACE ( 'NONE', ( #11416 ), #4793, .F. ) ;
#8975=LINE ( 'NONE', #773, #265 ) ;
#8979=DIRECTION ( 'NONE',  ( 1.402518428993831676E-16, -1.000000000000000000, 1.677918375355662166E-32 ) ) ;
#8994=CARTESIAN_POINT ( 'NONE',  ( -0.8237052942265477018, 49.18499566818285018, 96.19558879953099506 ) ) ;
#8998=CARTESIAN_POINT ( 'NONE',  ( -3.350035803220276609, 49.20851703305431357, 94.63308880123798872 ) ) ;
#9000=CARTESIAN_POINT ( 'NONE',  ( -5.154188915835984375, 42.64120994080404614, 94.71121380123804556 ) ) ;
#9001=ORIENTED_EDGE ( 'NONE', *, *, #10962, .T. ) ;
#9007=CARTESIAN_POINT ( 'NONE',  ( 1.352400422481993658, 50.46853102219002096, 91.97683880123797451 ) ) ;
#9008=ORIENTED_EDGE ( 'NONE', *, *, #10262, .F. ) ;
#9011=EDGE_CURVE ( 'NONE', #17415, #17446, #860, .T. ) ;
#9012=CARTESIAN_POINT ( 'NONE',  ( 3.122075258343615545, 38.59543968120053847, 90.05576841395854615 ) ) ;
#9013=EDGE_CURVE ( 'NONE', #8877, #15717, #7452, .T. ) ;
#9017=CARTESIAN_POINT ( 'NONE',  ( -5.368445182934975968, 51.36218137147968577, 93.55433879953098142 ) ) ;
#9018=EDGE_LOOP ( 'NONE', ( #3459, #19599, #1967, #1299, #4735, #334, #11264, #13388, #3347, #5755, #5365, #18761 ) ) ;
#9023=CARTESIAN_POINT ( 'NONE',  ( -5.154188915835984375, 42.64120994080404614, 94.71121380123797451 ) ) ;
#9033=EDGE_CURVE ( 'NONE', #19399, #16713, #9060, .T. ) ;
#9034=CARTESIAN_POINT ( 'NONE',  ( -2.416137431568557314, 39.07291177436112406, 96.27371380123797451 ) ) ;
#9038=CARTESIAN_POINT ( 'NONE',  ( 3.948530577815480225, 39.69684013992245752, 90.96121380294498238 ) ) ;
#9043=PLANE ( 'NONE',  #5838 ) ;
#9045=LINE ( 'NONE', #13931, #15374 ) ;
#9054=DIRECTION ( 'NONE',  ( -1.193617070626243484E-16, -1.000000000000000000, -0.000000000000000000 ) ) ;
#9059=CARTESIAN_POINT ( 'NONE',  ( 4.613683985508550300, 40.84891963687440608, 89.75946567728124137 ) ) ;
#9060=LINE ( 'NONE', #15443, #15603 ) ;
#9061=AXIS2_PLACEMENT_3D ( 'NONE', #4369, #15784, #11098 ) ;
#9063=CARTESIAN_POINT ( 'NONE',  ( 5.568489401881125289, 48.03437091500646261, 91.66433880123796030 ) ) ;
#9070=CARTESIAN_POINT ( 'NONE',  ( -2.904223097202481174, 48.62752260303690122, 92.83621380294498238 ) ) ;
#9074=CARTESIAN_POINT ( 'NONE',  ( -7.677846259693484221, 36.96218137147968008, 53.35433879953099989 ) ) ;
#9088=CARTESIAN_POINT ( 'NONE',  ( 6.828503391016846891, 43.33193468930419101, 95.25808880123800293 ) ) ;
#9091=CARTESIAN_POINT ( 'NONE',  ( 31.22215374030650281, 45.56218137147968861, 72.80433879953100984 ) ) ;
#9097=CARTESIAN_POINT ( 'NONE',  ( -5.058133621542618030, 44.89684013992257405, 91.42996379953099506 ) ) ;
#9099=CARTESIAN_POINT ( 'NONE',  ( 4.394343283833276992, 39.11584570990505938, 95.25808880123800293 ) ) ;
#9106=FACE_OUTER_BOUND ( 'NONE', #14457, .T. ) ;
#9109=CARTESIAN_POINT ( 'NONE',  ( 6.198496396448986090, 45.68315280215533392, 90.49246380123798872 ) ) ;
#9111=VERTEX_POINT ( 'NONE', #2113 ) ;
#9114=CARTESIAN_POINT ( 'NONE',  ( 3.460444912181559474, 49.25145096859824889, 91.74246380123798872 ) ) ;
#9121=ORIENTED_EDGE ( 'NONE', *, *, #17025, .T. ) ;
#9127=CARTESIAN_POINT ( 'NONE',  ( -3.350035803220276609, 49.20851703305431357, 94.47683880123798872 ) ) ;
#9128=EDGE_CURVE ( 'NONE', #16684, #129, #16891, .T. ) ;
#9141=CARTESIAN_POINT ( 'NONE',  ( 30.92220646078100188, 42.76218137147968434, 62.80715055817104542 ) ) ;
#9145=CARTESIAN_POINT ( 'NONE',  ( -5.058133621542618030, 44.89684013992257405, 90.49246380294498238 ) ) ;
#9149=VECTOR ( 'NONE', #13005, 1000.000000000000000 ) ;
#9153=EDGE_CURVE ( 'NONE', #11154, #5474, #19758, .T. ) ;
#9155=CARTESIAN_POINT ( 'NONE',  ( 6.198496396448986090, 45.68315280215533392, 91.74246380123798872 ) ) ;
#9159=ORIENTED_EDGE ( 'NONE', *, *, #13892, .T. ) ;
#9168=DIRECTION ( 'NONE',  ( 1.000000000000000000, 1.402518428993831676E-16, 1.621236893436268400E-16 ) ) ;
#9171=LINE ( 'NONE', #4253, #15317 ) ;
#9178=DIRECTION ( 'NONE',  ( -0.000000000000000000, 2.168404344970984413E-15, -1.000000000000000000 ) ) ;
#9179=CARTESIAN_POINT ( 'NONE',  ( -4.500660556396669065, 42.81632233694663370, 94.32058880294496817 ) ) ;
#9195=LINE ( 'NONE', #12171, #6684 ) ;
#9196=CARTESIAN_POINT ( 'NONE',  ( -4.524181921268124462, 40.28999182795290324, 94.78933880123798872 ) ) ;
#9199=CARTESIAN_POINT ( 'NONE',  ( 4.394343283833276992, 39.11584570990505938, 95.10183880123797451 ) ) ;
#9208=CARTESIAN_POINT ( 'NONE',  ( 6.198496396448986090, 45.68315280215533392, 95.49246380123798872 ) ) ;
#9212=CARTESIAN_POINT ( 'NONE',  ( -5.154188915835984375, 42.64120994080404614, 94.86746380123797451 ) ) ;
#9217=EDGE_CURVE ( 'NONE', #5140, #6553, #13588, .T. ) ;
#9220=CARTESIAN_POINT ( 'NONE',  ( 3.460444912181559474, 49.25145096859824889, 90.64871380123798872 ) ) ;
#9228=LINE ( 'NONE', #4100, #17082 ) ;
#9235=CARTESIAN_POINT ( 'NONE',  ( 2.043125170982144745, 38.48583871533720213, 95.02371380123798872 ) ) ;
#9236=CARTESIAN_POINT ( 'NONE',  ( 31.07218010054375412, 42.76218137147968434, 70.80574467885102763 ) ) ;
#9248=VERTEX_POINT ( 'NONE', #10527 ) ;
#9252=CARTESIAN_POINT ( 'NONE',  ( -2.416137431568557314, 39.07291177436112406, 96.11746380123797451 ) ) ;
#9253=CARTESIAN_POINT ( 'NONE',  ( 31.22215374030650281, 45.56218137147968861, 78.80433879953099563 ) ) ;
#9257=CARTESIAN_POINT ( 'NONE',  ( 1.256812508749381774, 49.74246873332880625, 93.92996380294498238 ) ) ;
#9258=VECTOR ( 'NONE', #18512, 1000.000000000000000 ) ;
#9261=VECTOR ( 'NONE', #5298, 1000.000000000000000 ) ;
#9267=DIRECTION ( 'NONE',  ( 1.000000000000000000, 2.838338907332122006E-16, -0.000000000000000000 ) ) ;
#9269=VECTOR ( 'NONE', #12315, 1000.000000000000000 ) ;
#9274=VECTOR ( 'NONE', #3230, 1000.000000000000000 ) ;
#9276=DIRECTION ( 'NONE',  ( -0.6546536707079712025, 0.6546536707079816386, 0.3779644730092298621 ) ) ;
#9282=CARTESIAN_POINT ( 'NONE',  ( 6.198496396448986090, 45.68315280215533392, 91.58621380123798872 ) ) ;
#9289=DIRECTION ( 'NONE',  ( -1.000000000000000000, 0.000000000000000000, 0.000000000000000000 ) ) ;
#9290=CARTESIAN_POINT ( 'NONE',  ( -5.058133621542618030, 44.89684013992257405, 90.49246380294498238 ) ) ;
#9292=PLANE ( 'NONE',  #13021 ) ;
#9295=FACE_OUTER_BOUND ( 'NONE', #17799, .T. ) ;
#9298=ORIENTED_EDGE ( 'NONE', *, *, #9915, .T. ) ;
#9299=DIRECTION ( 'NONE',  ( -0.000000000000000000, 1.000000000000000000, -0.000000000000000000 ) ) ;
#9303=CARTESIAN_POINT ( 'NONE',  ( 4.394343283833276992, 39.11584570990505938, 95.10183880123797451 ) ) ;
#9305=CARTESIAN_POINT ( 'NONE',  ( 31.07218010054375412, 42.76218137147968434, 64.80574467885102763 ) ) ;
#9306=LINE ( 'NONE', #14170, #13888 ) ;
#9314=CARTESIAN_POINT ( 'NONE',  ( -3.777846259693486974, 36.96218137147968008, 93.55433879953098142 ) ) ;
#9315=CARTESIAN_POINT ( 'NONE',  ( -0.9988176903691428077, 49.83852402762217082, 94.55496380123798872 ) ) ;
#9322=CARTESIAN_POINT ( 'NONE',  ( 1.059694531045822563, 38.29779899706197455, 95.05433879953093879 ) ) ;
#9324=CARTESIAN_POINT ( 'NONE',  ( -4.500660556396669065, 42.81632233694663370, 92.75808879953098085 ) ) ;
#9325=CARTESIAN_POINT ( 'NONE',  ( 5.568489401881125289, 48.03437091500646261, 93.07058880123797451 ) ) ;
#9328=CARTESIAN_POINT ( 'NONE',  ( 5.988021488050563335, 43.25938002633461110, 95.05433879953098142 ) ) ;
#9330=CIRCLE ( 'NONE', #16790, 4.200000000000001066 ) ;
#9331=CARTESIAN_POINT ( 'NONE',  ( 4.199109002476567376, 47.83913663364971569, 93.80036078555450274 ) ) ;
#9340=CARTESIAN_POINT ( 'NONE',  ( -5.784195910403845176, 44.99242805365518194, 95.88308880123798872 ) ) ;
#9341=DIRECTION ( 'NONE',  ( 1.334402673828313339E-16, -1.592765810570777996E-32, -1.000000000000000000 ) ) ;
#9356=CARTESIAN_POINT ( 'NONE',  ( 6.828503391016846891, 43.33193468930419101, 92.91433880123798872 ) ) ;
#9358=LINE ( 'NONE', #7751, #11300 ) ;
#9360=CARTESIAN_POINT ( 'NONE',  ( -4.677846311233868626, 45.55551708285101142, 92.96487682030837618 ) ) ;
#9361=ORIENTED_EDGE ( 'NONE', *, *, #14734, .T. ) ;
#9364=CARTESIAN_POINT ( 'NONE',  ( -5.368445182934982185, 36.96218137147968008, 80.55433879953099563 ) ) ;
#9366=DIRECTION ( 'NONE',  ( -2.838338907332122006E-16, 1.000000000000000000, 0.000000000000000000 ) ) ;
#9374=DIRECTION ( 'NONE',  ( -0.000000000000000000, -0.000000000000000000, 1.000000000000000000 ) ) ;
#9378=DIRECTION ( 'NONE',  ( 1.196361017915039239E-16, 0.000000000000000000, -1.000000000000000000 ) ) ;
#9380=CARTESIAN_POINT ( 'NONE',  ( 4.394343283833276992, 39.11584570990505938, 91.35183880123798872 ) ) ;
#9389=CARTESIAN_POINT ( 'NONE',  ( -2.077846259693550746, 39.65884927180063357, 90.72683880294498238 ) ) ;
#9400=CARTESIAN_POINT ( 'NONE',  ( 1.352400422481993658, 50.46853102219002096, 95.57058880123798872 ) ) ;
#9401=CARTESIAN_POINT ( 'NONE',  ( -3.350035803220276609, 49.20851703305431357, 94.47683880123798872 ) ) ;
#9402=DIRECTION ( 'NONE',  ( 1.000000000000000000, 0.000000000000000000, 0.000000000000000000 ) ) ;
#9408=VECTOR ( 'NONE', #19320, 1000.000000000000000 ) ;
#9411=CARTESIAN_POINT ( 'NONE',  ( -4.567115856812060670, 47.10047254335474065, 93.46121380123797451 ) ) ;
#9412=FACE_OUTER_BOUND ( 'NONE', #5549, .T. ) ;
#9419=VERTEX_POINT ( 'NONE', #13648 ) ;
#9421=CARTESIAN_POINT ( 'NONE',  ( -4.567115856812060670, 47.10047254335474065, 90.96121380123797451 ) ) ;
#9422=EDGE_LOOP ( 'NONE', ( #14980, #368, #18355, #4163, #14532, #7474, #3091, #20741 ) ) ;
#9423=LINE ( 'NONE', #15912, #11114 ) ;
#9432=ORIENTED_EDGE ( 'NONE', *, *, #19002, .T. ) ;
#9439=CARTESIAN_POINT ( 'NONE',  ( 6.828503391016846891, 43.33193468930419101, 92.91433880123798872 ) ) ;
#9456=CARTESIAN_POINT ( 'NONE',  ( 2.043125170982144745, 38.48583871533720213, 93.92996380123798872 ) ) ;
#9457=EDGE_CURVE ( 'NONE', #1329, #4901, #13850, .T. ) ;
#9467=CARTESIAN_POINT ( 'NONE',  ( 0.5221537403065020788, 52.36218137147968577, 52.53721119516358584 ) ) ;
#9469=CARTESIAN_POINT ( 'NONE',  ( -4.524181921268124462, 40.28999182795290324, 91.19558880123797451 ) ) ;
#9471=EDGE_LOOP ( 'NONE', ( #19625, #12028, #6951, #10602 ) ) ;
#9476=CARTESIAN_POINT ( 'NONE',  ( 31.07218010054375412, 36.96218137147968008, 37.55574467885101342 ) ) ;
#9478=ADVANCED_FACE ( 'NONE', ( #18434, #20120 ), #13751, .T. ) ;
#9480=DIRECTION ( 'NONE',  ( -1.000000000000000000, 0.000000000000000000, 0.000000000000000000 ) ) ;
#9481=CARTESIAN_POINT ( 'NONE',  ( 1.514255888186003762, 51.36218137147968577, 87.21440135111343750 ) ) ;
#9485=EDGE_CURVE ( 'NONE', #3115, #4005, #3954, .T. ) ;
#9489=ORIENTED_EDGE ( 'NONE', *, *, #18857, .F. ) ;
#9491=CARTESIAN_POINT ( 'NONE',  ( -0.2125050281363792815, 38.58189400963055959, 92.05496380294498238 ) ) ;
#9492=ORIENTED_EDGE ( 'NONE', *, *, #16017, .T. ) ;
#9503=ORIENTED_EDGE ( 'NONE', *, *, #1418, .F. ) ;
#9504=EDGE_CURVE ( 'NONE', #3488, #10737, #8975, .T. ) ;
#9511=AXIS2_PLACEMENT_3D ( 'NONE', #19486, #17794, #3818 ) ;
#9515=AXIS2_PLACEMENT_3D ( 'NONE', #15476, #2275, #13664 ) ;
#9517=VECTOR ( 'NONE', #6895, 1000.000000000000000 ) ;
#9518=CARTESIAN_POINT ( 'NONE',  ( 6.198496396448986090, 45.68315280215533392, 94.24246380123798872 ) ) ;
#9522=DIRECTION ( 'NONE',  ( 0.000000000000000000, 0.000000000000000000, -1.000000000000000000 ) ) ;
#9528=CARTESIAN_POINT ( 'NONE',  ( -4.956235989166514422, 43.70076514643270116, 92.55433879953098142 ) ) ;
#9529=VECTOR ( 'NONE', #14180, 1000.000000000000000 ) ;
#9533=CARTESIAN_POINT ( 'NONE',  ( 5.505261640620147112, 46.12417297501537661, 95.05433879953093879 ) ) ;
#9545=VECTOR ( 'NONE', #3500, 1000.000000000000000 ) ;
#9552=ORIENTED_EDGE ( 'NONE', *, *, #21006, .F. ) ;
#9559=ORIENTED_EDGE ( 'NONE', *, *, #8694, .F. ) ;
#9567=CARTESIAN_POINT ( 'NONE',  ( -3.350035803220276609, 49.20851703305431357, 95.72683880123798872 ) ) ;
#9580=CARTESIAN_POINT ( 'NONE',  ( -7.677846259693480668, 36.96218137147968008, 95.05433879953098142 ) ) ;
#9582=CARTESIAN_POINT ( 'NONE',  ( 3.122153740306552905, 48.66551347115873227, 91.03933879953099506 ) ) ;
#9583=DIRECTION ( 'NONE',  ( 1.000000000000000000, 0.000000000000000000, 0.000000000000000000 ) ) ;
#9594=ADVANCED_FACE ( 'NONE', ( #9295 ), #5881, .F. ) ;
#9596=ORIENTED_EDGE ( 'NONE', *, *, #2570, .F. ) ;
#9601=ORIENTED_EDGE ( 'NONE', *, *, #11333, .F. ) ;
#9611=CARTESIAN_POINT ( 'NONE',  ( -4.567115856812060670, 47.10047254335474065, 95.80496380123798872 ) ) ;
#9612=CARTESIAN_POINT ( 'NONE',  ( -4.524181921268124462, 40.28999182795290324, 93.53933880123797451 ) ) ;
#9614=CARTESIAN_POINT ( 'NONE',  ( 30.92220646078100188, 42.76218137147968434, 62.80715055817104542 ) ) ;
#9617=ADVANCED_FACE ( 'NONE', ( #11197 ), #4265, .F. ) ;
#9628=AXIS2_PLACEMENT_3D ( 'NONE', #10691, #7680, #2791 ) ;
#9630=CARTESIAN_POINT ( 'NONE',  ( -0.8451447117293342526, 38.43386779256927355, 95.05433879953092458 ) ) ;
#9631=EDGE_CURVE ( 'NONE', #18045, #3176, #1198, .T. ) ;
#9648=VERTEX_POINT ( 'NONE', #20746 ) ;
#9653=EDGE_CURVE ( 'NONE', #9713, #11872, #14160, .T. ) ;
#9663=CARTESIAN_POINT ( 'NONE',  ( -3.943187491250720544, 40.73580453397070755, 95.33621379953099506 ) ) ;
#9668=ADVANCED_FACE ( 'NONE', ( #10999 ), #2990, .F. ) ;
#9669=AXIS2_PLACEMENT_3D ( 'NONE', #6313, #3143, #16538 ) ;
#9672=LINE ( 'NONE', #14753, #15557 ) ;
#9674=CARTESIAN_POINT ( 'NONE',  ( -0.3080929418689875576, 37.85583172076933778, 94.94558880123797451 ) ) ;
#9683=FACE_OUTER_BOUND ( 'NONE', #8144, .T. ) ;
#9698=CARTESIAN_POINT ( 'NONE',  ( 31.07218010054375412, 45.56218137147968861, 70.80574467885102763 ) ) ;
#9713=VERTEX_POINT ( 'NONE', #6073 ) ;
#9714=CARTESIAN_POINT ( 'NONE',  ( 4.454347278305088587, 39.79502279609036464, 90.11785590924256439 ) ) ;
#9726=CARTESIAN_POINT ( 'NONE',  ( -2.416137431568557314, 39.07291177436112406, 96.11746380123797451 ) ) ;
#9727=ORIENTED_EDGE ( 'NONE', *, *, #18945, .T. ) ;
#9730=CARTESIAN_POINT ( 'NONE',  ( 5.294808925291379254, 46.52673310323378075, 92.55433879953103826 ) ) ;
#9732=CARTESIAN_POINT ( 'NONE',  ( 4.199109002476567376, 47.83913663364971569, 83.28180655319408743 ) ) ;
#9733=EDGE_LOOP ( 'NONE', ( #1766, #20635, #2790, #19124, #7944 ) ) ;
#9734=CARTESIAN_POINT ( 'NONE',  ( -1.579458713458412822, 38.67424504376464967, 92.55433879953098142 ) ) ;
#9749=CARTESIAN_POINT ( 'NONE',  ( 31.22215374030650281, 42.76218137147968434, 78.80433879953099563 ) ) ;
#9754=CARTESIAN_POINT ( 'NONE',  ( 6.828503391016846891, 43.33193468930419101, 94.16433880123797451 ) ) ;
#9757=CARTESIAN_POINT ( 'NONE',  ( 31.07218010054375412, 42.76218137147968434, 69.40574467885102194 ) ) ;
#9759=CARTESIAN_POINT ( 'NONE',  ( -0.8237052942265477018, 49.18499566818285018, 96.19558879953099506 ) ) ;
#9767=CARTESIAN_POINT ( 'NONE',  ( 10.77494014480653561, 42.96218137147968008, 65.80574467885102763 ) ) ;
#9769=CARTESIAN_POINT ( 'NONE',  ( 3.460444912181559474, 49.25145096859824889, 94.24246380123798872 ) ) ;
#9782=LINE ( 'NONE', #3484, #7543 ) ;
#9792=VECTOR ( 'NONE', #13287, 1000.000000000000000 ) ;
#9794=CARTESIAN_POINT ( 'NONE',  ( -4.477846259693498254, 37.66218137147969713, 53.35433879953099989 ) ) ;
#9796=CARTESIAN_POINT ( 'NONE',  ( 2.043125170982144745, 38.48583871533720213, 92.52371380123798872 ) ) ;
#9800=AXIS2_PLACEMENT_3D ( 'NONE', #17454, #20730, #17547 ) ;
#9801=FACE_OUTER_BOUND ( 'NONE', #14399, .T. ) ;
#9816=CARTESIAN_POINT ( 'NONE',  ( -4.524181921268124462, 40.28999182795290324, 91.03933880123798872 ) ) ;
#9817=LINE ( 'NONE', #12789, #9149 ) ;
#9826=CARTESIAN_POINT ( 'NONE',  ( 2.580190882731760560, 49.45805475339454205, 94.54925044102853349 ) ) ;
#9827=CARTESIAN_POINT ( 'NONE',  ( -0.3080929418689875576, 37.85583172076933778, 93.69558880123800293 ) ) ;
#9828=EDGE_LOOP ( 'NONE', ( #11972, #12572, #172, #14626 ) ) ;
#9832=CARTESIAN_POINT ( 'NONE',  ( 5.918312273062399598, 44.84149841250357582, 92.55433879953093879 ) ) ;
#9835=VERTEX_POINT ( 'NONE', #20621 ) ;
#9836=DIRECTION ( 'NONE',  ( 1.402518428993831676E-16, -1.000000000000000000, 0.000000000000000000 ) ) ;
#9841=VECTOR ( 'NONE', #19877, 1000.000000000000000 ) ;
#9849=EDGE_LOOP ( 'NONE', ( #4390, #20760, #10558, #3414 ) ) ;
#9860=ORIENTED_EDGE ( 'NONE', *, *, #13374, .F. ) ;
#9866=CARTESIAN_POINT ( 'NONE',  ( 30.92220646078100188, 45.56218137147968861, 62.80715055817104542 ) ) ;
#9867=CARTESIAN_POINT ( 'NONE',  ( 1.256812508749381774, 49.74246873332880625, 94.86746379953099506 ) ) ;
#9868=ORIENTED_EDGE ( 'NONE', *, *, #3381, .F. ) ;
#9872=VECTOR ( 'NONE', #697, 1000.000000000000000 ) ;
#9877=CARTESIAN_POINT ( 'NONE',  ( -2.416137431568557314, 39.07291177436112406, 93.61746380123797451 ) ) ;
#9889=FACE_OUTER_BOUND ( 'NONE', #2049, .T. ) ;
#9890=CARTESIAN_POINT ( 'NONE',  ( 11.22215374030650281, 42.96218137147968008, 66.20574467885104752 ) ) ;
#9909=CARTESIAN_POINT ( 'NONE',  ( 6.198496396448986090, 45.68315280215533392, 91.58621380123798872 ) ) ;
#9915=EDGE_CURVE ( 'NONE', #8877, #895, #4345, .T. ) ;
#9924=FACE_OUTER_BOUND ( 'NONE', #9733, .T. ) ;
#9930=CARTESIAN_POINT ( 'NONE',  ( 6.198496396448986090, 45.68315280215533392, 91.58621380123798872 ) ) ;
#9932=PLANE ( 'NONE',  #20515 ) ;
#9934=CARTESIAN_POINT ( 'NONE',  ( 13.32277635493563039, 36.96218137147968008, 54.55433879953099563 ) ) ;
#9937=DIRECTION ( 'NONE',  ( 0.000000000000000000, 1.734723475976787846E-14, -1.000000000000000000 ) ) ;
#9953=ORIENTED_EDGE ( 'NONE', *, *, #3004, .T. ) ;
#9957=CYLINDRICAL_SURFACE ( 'NONE', #20373, 5.199999999999999289 ) ;
#9962=VERTEX_POINT ( 'NONE', #14770 ) ;
#9966=VECTOR ( 'NONE', #18403, 1000.000000000000000 ) ;
#9967=CARTESIAN_POINT ( 'NONE',  ( -1.219056181836354558, 49.77488197367695477, 93.31237966814926210 ) ) ;
#9970=CARTESIAN_POINT ( 'NONE',  ( -0.2125050281363792815, 38.58189400963055959, 94.24246379953099506 ) ) ;
#9972=LINE ( 'NONE', #13557, #8863 ) ;
#9974=ORIENTED_EDGE ( 'NONE', *, *, #19722, .F. ) ;
#9977=CARTESIAN_POINT ( 'NONE',  ( -3.981178359372548492, 46.76218137147973408, 92.60183879953099506 ) ) ;
#9978=ORIENTED_EDGE ( 'NONE', *, *, #1305, .T. ) ;
#9983=LINE ( 'NONE', #14544, #2972 ) ;
#9984=DIRECTION ( 'NONE',  ( 0.000000000000000000, 0.000000000000000000, -1.000000000000000000 ) ) ;
#9985=CARTESIAN_POINT ( 'NONE',  ( -4.524181921268124462, 40.28999182795290324, 94.78933880123798872 ) ) ;
#9988=EDGE_CURVE ( 'NONE', #10468, #13576, #19248, .T. ) ;
#9992=ORIENTED_EDGE ( 'NONE', *, *, #7560, .T. ) ;
#10003=CARTESIAN_POINT ( 'NONE',  ( 5.722153675945192752, 44.84677459913377362, 93.67075777718372365 ) ) ;
#10006=PLANE ( 'NONE',  #90 ) ;
#10008=CARTESIAN_POINT ( 'NONE',  ( 4.394343283833276104, 39.11584570990505938, 93.85183880123807398 ) ) ;
#10011=CARTESIAN_POINT ( 'NONE',  ( -5.784195910403845176, 44.99242805365518194, 90.88308880123798872 ) ) ;
#10012=CARTESIAN_POINT ( 'NONE',  ( -2.416137431568557314, 39.07291177436112406, 93.61746380123797451 ) ) ;
#10029=CARTESIAN_POINT ( 'NONE',  ( -5.784195910403845176, 44.99242805365518194, 90.88308880123798872 ) ) ;
#10030=EDGE_CURVE ( 'NONE', #16818, #20921, #16627, .T. ) ;
#10032=ADVANCED_FACE ( 'NONE', ( #1902 ), #8391, .F. ) ;
#10033=CARTESIAN_POINT ( 'NONE',  ( -2.416137431568557314, 39.07291177436112406, 96.11746380123797451 ) ) ;
#10040=CARTESIAN_POINT ( 'NONE',  ( -1.535769738210056357, 49.45816841730323432, 93.04858131124048271 ) ) ;
#10043=VERTEX_POINT ( 'NONE', #7089 ) ;
#10051=CARTESIAN_POINT ( 'NONE',  ( -2.393324858630934138, 39.09930439799452984, 92.55433879953105247 ) ) ;
#10052=VERTEX_POINT ( 'NONE', #8710 ) ;
#10065=ORIENTED_EDGE ( 'NONE', *, *, #18098, .T. ) ;
#10066=FACE_OUTER_BOUND ( 'NONE', #6623, .T. ) ;
#10067=CARTESIAN_POINT ( 'NONE',  ( 2.568262918966977004, 49.46998271715920481, 92.90703276401609401 ) ) ;
#10068=CARTESIAN_POINT ( 'NONE',  ( -0.2125050281363792815, 38.58189400963055959, 92.99246379953098085 ) ) ;
#10074=FACE_OUTER_BOUND ( 'NONE', #7905, .T. ) ;
#10081=CARTESIAN_POINT ( 'NONE',  ( -0.9988176903691428077, 49.83852402762217082, 94.39871380123798872 ) ) ;
#10093=FACE_OUTER_BOUND ( 'NONE', #12871, .T. ) ;
#10095=EDGE_LOOP ( 'NONE', ( #20040, #4785, #822, #4088 ) ) ;
#10097=FACE_OUTER_BOUND ( 'NONE', #10095, .T. ) ;
#10108=CARTESIAN_POINT ( 'NONE',  ( -3.943187491250720544, 40.73580453397070755, 95.64871380294496817 ) ) ;
#10109=VECTOR ( 'NONE', #15255, 1000.000000000000000 ) ;
#10110=CARTESIAN_POINT ( 'NONE',  ( 3.460444912181559474, 49.25145096859824889, 90.49246380123798872 ) ) ;
#10113=( BOUNDED_SURFACE ( )  B_SPLINE_SURFACE ( 1, 2, ( 
 ( #15793, #18965, #19170, #11106, #5890, #18865, #17574, #4378, #20558, #10904, #7691, #9088, #17268, #9199, #20651, #6081, #12588, #19077, #4486, #11007, #17479, #9401, #17788, #6390, #20079, #11206, #1908, #18281, #3502, #2221, #17680, #11709, #3109, #9612, #16094, #15202, #14488, #16591, #2011, #616, #10221, #19870, #301, #16699, #6989, #4792, #20956, #3699, #15104, #8509, #11917, #5191, #1517, #8002, #16488, #6898, #12894, #8400, #512, #3812, #2122, #19376, #19968, #7096, #11314, #14879, #8718, #10011, #413, #6792, #8622, #13299, #11805, #19770, #18184, #13494, #3601, #14994, #13401 ),
 ( #13601, #10108, #5291, #5395, #18391, #10331, #16803, #18709, #17328, #13921, #12439, #8933, #10755, #18917, #5942, #2323, #20289, #2646, #5721, #7539, #5617, #12026, #14127, #9257, #4332, #939, #18500, #1161, #10859, #2541, #12122, #4122, #7211, #5515, #15525, #4229, #20403, #3912, #2754, #7647, #8819, #15744, #10537, #10438, #15316, #16901, #836, #15421, #728, #13712, #20187, #7427, #18603, #4016, #17007, #2437, #7321, #13811, #12226, #10652, #17118, #9038, #5833, #15635, #12339, #18819, #17220, #9145, #1055, #14030, #20511, #8161, #19224, #20912, #4546, #8059, #1365, #12848, #3173 ) ),
 .UNSPECIFIED., .F., .F., .F. ) 
 B_SPLINE_SURFACE_WITH_KNOTS ( ( 2, 2 ),
 ( 3, 2, 2, 2, 2, 2, 2, 2, 2, 2, 2, 2, 2, 2, 2, 2, 2, 2, 2, 2, 2, 2, 2, 2, 2, 2, 2, 2, 2, 2, 2, 2, 2, 2, 2, 2, 2, 2, 2, 3 ),
 ( 0.000000000000000000, 1.000000000000000000 ),
 ( 0.000000000000000000, 0.02500000000000000139, 0.05000000000000000278, 0.07499999999999999722, 0.1000000000000000056, 0.1250000000000000000, 0.1499999999999999944, 0.1749999999999999889, 0.2000000000000000111, 0.2250000000000000056, 0.2500000000000000000, 0.2750000000000000222, 0.2999999999999999889, 0.3250000000000000111, 0.3499999999999999778, 0.3750000000000000000, 0.4000000000000000222, 0.4249999999999999889, 0.4500000000000000111, 0.4749999999999999778, 0.5000000000000000000, 0.5250000000000000222, 0.5500000000000000444, 0.5749999999999999556, 0.5999999999999999778, 0.6250000000000000000, 0.6500000000000000222, 0.6750000000000000444, 0.6999999999999999556, 0.7249999999999999778, 0.7500000000000000000, 0.7750000000000000222, 0.8000000000000000444, 0.8249999999999999556, 0.8499999999999999778, 0.8750000000000000000, 0.9000000000000000222, 0.9250000000000000444, 0.9499999999999999556, 0.9600309957089442348 ),
 .UNSPECIFIED. ) 
 GEOMETRIC_REPRESENTATION_ITEM ( )  RATIONAL_B_SPLINE_SURFACE ( (
 ( 1.000000000000000000, 0.9238795325112867385, 1.000000000000000000, 0.9238795325112867385, 1.000000000000000000, 0.9238795325112867385, 1.000000000000000000, 0.9238795325112867385, 1.000000000000000000, 0.9238795325112867385, 1.000000000000000000, 0.9238795325112867385, 1.000000000000000000, 0.9238795325112867385, 1.000000000000000000, 0.9238795325112867385, 1.000000000000000000, 0.9238795325112867385, 1.000000000000000000, 0.9238795325112867385, 1.000000000000000000, 0.9238795325112867385, 1.000000000000000000, 0.9238795325112867385, 1.000000000000000000, 0.9238795325112867385, 1.000000000000000000, 0.9238795325112867385, 1.000000000000000000, 0.9238795325112867385, 1.000000000000000000, 0.9238795325112867385, 1.000000000000000000, 0.9238795325112867385, 1.000000000000000000, 0.9238795325112867385, 1.000000000000000000, 0.9238795325112867385, 1.000000000000000000, 0.9238795325112867385, 1.000000000000000000, 0.9238795325112867385, 1.000000000000000000, 0.9238795325112867385, 1.000000000000000000, 0.9238795325112867385, 1.000000000000000000, 0.9238795325112867385, 1.000000000000000000, 0.9238795325112867385, 1.000000000000000000, 0.9238795325112867385, 1.000000000000000000, 0.9238795325112867385, 1.000000000000000000, 0.9238795325112867385, 1.000000000000000000, 0.9238795325112867385, 1.000000000000000000, 0.9238795325112867385, 1.000000000000000000, 0.9238795325112867385, 1.000000000000000000, 0.9238795325112867385, 1.000000000000000000, 0.9238795325112867385, 1.000000000000000000, 0.9238795325112867385, 1.000000000000000000, 0.9238795325112867385, 1.000000000000000000, 0.9238795325112867385, 1.000000000000000000, 0.9238795325112867385, 1.000000000000000000, 0.9238795325112867385, 1.000000000000000000, 0.9694574366903154772, 0.9634246591005992677),
 ( 1.000000000000000000, 0.9238795325112867385, 1.000000000000000000, 0.9238795325112867385, 1.000000000000000000, 0.9238795325112867385, 1.000000000000000000, 0.9238795325112867385, 1.000000000000000000, 0.9238795325112867385, 1.000000000000000000, 0.9238795325112867385, 1.000000000000000000, 0.9238795325112867385, 1.000000000000000000, 0.9238795325112867385, 1.000000000000000000, 0.9238795325112867385, 1.000000000000000000, 0.9238795325112867385, 1.000000000000000000, 0.9238795325112867385, 1.000000000000000000, 0.9238795325112867385, 1.000000000000000000, 0.9238795325112867385, 1.000000000000000000, 0.9238795325112867385, 1.000000000000000000, 0.9238795325112867385, 1.000000000000000000, 0.9238795325112867385, 1.000000000000000000, 0.9238795325112867385, 1.000000000000000000, 0.9238795325112867385, 1.000000000000000000, 0.9238795325112867385, 1.000000000000000000, 0.9238795325112867385, 1.000000000000000000, 0.9238795325112867385, 1.000000000000000000, 0.9238795325112867385, 1.000000000000000000, 0.9238795325112867385, 1.000000000000000000, 0.9238795325112867385, 1.000000000000000000, 0.9238795325112867385, 1.000000000000000000, 0.9238795325112867385, 1.000000000000000000, 0.9238795325112867385, 1.000000000000000000, 0.9238795325112867385, 1.000000000000000000, 0.9238795325112867385, 1.000000000000000000, 0.9238795325112867385, 1.000000000000000000, 0.9238795325112867385, 1.000000000000000000, 0.9238795325112867385, 1.000000000000000000, 0.9238795325112867385, 1.000000000000000000, 0.9238795325112867385, 1.000000000000000000, 0.9238795325112867385, 1.000000000000000000, 0.9238795325112867385, 1.000000000000000000, 0.9238795325112867385, 1.000000000000000000, 0.9238795325112867385, 1.000000000000000000, 0.9694574366903154772, 0.9634246591005992677) ) ) 
 REPRESENTATION_ITEM ( '' )  SURFACE ( )  );
#10115=PLANE ( 'NONE',  #14660 ) ;
#10117=CARTESIAN_POINT ( 'NONE',  ( -4.567115856812060670, 47.10047254335474065, 93.46121380123797451 ) ) ;
#10125=ADVANCED_FACE ( 'NONE', ( #721 ), #403, .F. ) ;
#10129=VERTEX_POINT ( 'NONE', #5610 ) ;
#10133=CARTESIAN_POINT ( 'NONE',  ( 3.460444912181559474, 49.25145096859824889, 91.74246380123798872 ) ) ;
#10137=CARTESIAN_POINT ( 'NONE',  ( -0.9988176903691428077, 49.83852402762217082, 94.39871380123798872 ) ) ;
#10139=B_SPLINE_CURVE_WITH_KNOTS ( 'NONE', 3,
 ( #14099, #20582, #7923, #4608, #6008, #9533, #4405, #10928, #3136, #2824, #19100, #7716, #9328, #11128, #7820, #14196, #20880, #4511, #20674, #17500, #11029, #4707, #11235, #2924 ),
 .UNSPECIFIED., .F., .F.,
 ( 4, 2, 2, 2, 2, 2, 2, 2, 2, 2, 2, 4 ),
 ( 1.161628372437217770E-05, 0.001362246422599150235, 0.002037561492036547590, 0.002712876561473944945, 0.004063506700348720573, 0.004738821769786108820, 0.005414136839223496200, 0.006764766978098251879, 0.007440082047535629718, 0.008115397116973009292, 0.009466027255847764971, 0.01081665739472252065 ),
 .UNSPECIFIED. ) ;
#10145=ADVANCED_FACE ( 'NONE', ( #11702 ), #16894, .F. ) ;
#10151=VECTOR ( 'NONE', #1665, 1000.000000000000000 ) ;
#10160=EDGE_CURVE ( 'NONE', #15424, #15187, #15138, .T. ) ;
#10161=DIRECTION ( 'NONE',  ( -1.000000000000000000, 0.000000000000000000, 0.000000000000000000 ) ) ;
#10172=CARTESIAN_POINT ( 'NONE',  ( -3.943187491250720544, 40.73580453397070755, 96.58621379953099506 ) ) ;
#10173=CARTESIAN_POINT ( 'NONE',  ( -3.943187491250720544, 40.73580453397070755, 94.08621379953100927 ) ) ;
#10175=CARTESIAN_POINT ( 'NONE',  ( -5.154188915835984375, 42.64120994080404614, 96.11746380123797451 ) ) ;
#10179=DIRECTION ( 'NONE',  ( 4.818676322157797375E-16, 1.000000000000000000, -0.000000000000000000 ) ) ;
#10184=CARTESIAN_POINT ( 'NONE',  ( -2.416137431568557314, 39.07291177436112406, 93.77371380123797451 ) ) ;
#10194=CARTESIAN_POINT ( 'NONE',  ( 11.22215374030649926, 42.96218137147968008, 77.40433879953098995 ) ) ;
#10201=ORIENTED_EDGE ( 'NONE', *, *, #3112, .F. ) ;
#10210=VERTEX_POINT ( 'NONE', #12432 ) ;
#10215=FACE_OUTER_BOUND ( 'NONE', #2622, .T. ) ;
#10220=DIRECTION ( 'NONE',  ( -1.000000000000000000, -1.402518428993831676E-16, -1.196361017915039239E-16 ) ) ;
#10221=CARTESIAN_POINT ( 'NONE',  ( 3.460444912181559474, 49.25145096859824889, 92.99246380123798872 ) ) ;
#10223=CARTESIAN_POINT ( 'NONE',  ( 2.722153740306499703, 47.73989013547934945, 54.55433879953099563 ) ) ;
#10230=CARTESIAN_POINT ( 'NONE',  ( -2.416137431568557314, 39.07291177436112406, 93.77371380123797451 ) ) ;
#10233=CARTESIAN_POINT ( 'NONE',  ( 13.72215374030650104, 51.36218137147968577, 95.05433879953098142 ) ) ;
#10235=ORIENTED_EDGE ( 'NONE', *, *, #13895, .T. ) ;
#10239=CARTESIAN_POINT ( 'NONE',  ( 13.32277635493562329, 51.36218137147968577, 54.55433879953099563 ) ) ;
#10241=EDGE_LOOP ( 'NONE', ( #17937, #20226, #4031, #11862 ) ) ;
#10243=CARTESIAN_POINT ( 'NONE',  ( -4.813079231556614879, 45.05781033453988016, 95.05433879953105247 ) ) ;
#10245=CARTESIAN_POINT ( 'NONE',  ( -5.058133621542618030, 44.89684013992257405, 91.74246380294499659 ) ) ;
#10248=CARTESIAN_POINT ( 'NONE',  ( -4.567115856812060670, 47.10047254335474065, 90.96121380123797451 ) ) ;
#10251=LINE ( 'NONE', #13740, #15340 ) ;
#10255=AXIS2_PLACEMENT_3D ( 'NONE', #18311, #3733, #11526 ) ;
#10256=CARTESIAN_POINT ( 'NONE',  ( -0.4699484075729999377, 51.36218137147968577, 87.21440135111343750 ) ) ;
#10257=VECTOR ( 'NONE', #17042, 1000.000000000000000 ) ;
#10258=CARTESIAN_POINT ( 'NONE',  ( -3.350035803220276609, 49.20851703305431357, 90.72683880123797451 ) ) ;
#10261=CARTESIAN_POINT ( 'NONE',  ( 5.722153740306498371, 44.16218137147968292, 94.58161078214052964 ) ) ;
#10262=EDGE_CURVE ( 'NONE', #20901, #3734, #7418, .T. ) ;
#10267=CARTESIAN_POINT ( 'NONE',  ( 31.07218010054375412, 42.76218137147968434, 64.80574467885102763 ) ) ;
#10276=CARTESIAN_POINT ( 'NONE',  ( 33.61275266354798674, 36.96218137147968719, 93.55433879953098142 ) ) ;
#10281=DIRECTION ( 'NONE',  ( 0.000000000000000000, -2.168404344970984808E-15, -1.000000000000000000 ) ) ;
#10282=CARTESIAN_POINT ( 'NONE',  ( -0.8237052942265477018, 49.18499566818285018, 93.69558879953099506 ) ) ;
#10283=CARTESIAN_POINT ( 'NONE',  ( -2.077846259693550746, 39.65884927180063357, 95.41433879953098085 ) ) ;
#10287=DIRECTION ( 'NONE',  ( -0.000000000000000000, 1.000000000000000000, -0.000000000000000000 ) ) ;
#10295=CARTESIAN_POINT ( 'NONE',  ( -0.9988176903691428077, 49.83852402762217082, 95.80496380123798872 ) ) ;
#10297=CARTESIAN_POINT ( 'NONE',  ( -3.777846259693487863, 51.36218137147968577, 53.35433879953099989 ) ) ;
#10299=CARTESIAN_POINT ( 'NONE',  ( -5.784195910403845176, 44.99242805365518194, 90.88308880123798872 ) ) ;
#10308=EDGE_CURVE ( 'NONE', #14607, #11193, #6444, .T. ) ;
#10314=CARTESIAN_POINT ( 'NONE',  ( -0.9988176903691428077, 49.83852402762217082, 94.55496380123798872 ) ) ;
#10326=CARTESIAN_POINT ( 'NONE',  ( 3.460444912181559474, 49.25145096859824889, 95.64871380123798872 ) ) ;
#10328=CARTESIAN_POINT ( 'NONE',  ( -0.8448747701364694995, 38.43386606678133433, 92.55433879953096721 ) ) ;
#10331=CARTESIAN_POINT ( 'NONE',  ( -2.904223097202481174, 48.62752260303690122, 95.33621380294498238 ) ) ;
#10335=AXIS2_PLACEMENT_3D ( 'NONE', #2117, #4117, #20283 ) ;
#10338=DIRECTION ( 'NONE',  ( -1.193617070626243484E-16, -1.000000000000000000, 0.000000000000000000 ) ) ;
#10341=CARTESIAN_POINT ( 'NONE',  ( -3.350035803220276609, 49.20851703305431357, 95.88308880123798872 ) ) ;
#10342=LINE ( 'NONE', #13612, #20404 ) ;
#10357=CARTESIAN_POINT ( 'NONE',  ( 4.001626195812781006, 40.29782224849783745, 89.72723091094957226 ) ) ;
#10360=CARTESIAN_POINT ( 'NONE',  ( -5.784195910403845176, 44.99242805365518194, 93.38308880123798872 ) ) ;
#10367=CARTESIAN_POINT ( 'NONE',  ( -5.784195910403845176, 44.99242805365518194, 90.88308880123798872 ) ) ;
#10375=ORIENTED_EDGE ( 'NONE', *, *, #7512, .F. ) ;
#10377=EDGE_CURVE ( 'NONE', #14607, #6086, #20812, .T. ) ;
#10382=CARTESIAN_POINT ( 'NONE',  ( 0.2012661975153932636, 37.99231409082479161, 92.61876351041186695 ) ) ;
#10391=CARTESIAN_POINT ( 'NONE',  ( -2.904223097202481174, 48.62752260303690122, 95.02371379953099506 ) ) ;
#10392=CARTESIAN_POINT ( 'NONE',  ( 6.102441102155617969, 43.42752260303680600, 94.55496379953098085 ) ) ;
#10400=ORIENTED_EDGE ( 'NONE', *, *, #10656, .T. ) ;
#10402=CARTESIAN_POINT ( 'NONE',  ( -5.784195910403845176, 44.99242805365518194, 94.78933880123798872 ) ) ;
#10404=ORIENTED_EDGE ( 'NONE', *, *, #18450, .T. ) ;
#10407=CARTESIAN_POINT ( 'NONE',  ( 6.198496396448986090, 45.68315280215533392, 90.33621380123798872 ) ) ;
#10411=EDGE_CURVE ( 'NONE', #4997, #3547, #16047, .T. ) ;
#10413=ORIENTED_EDGE ( 'NONE', *, *, #2870, .T. ) ;
#10415=EDGE_CURVE ( 'NONE', #14613, #6086, #4736, .T. ) ;
#10416=VERTEX_POINT ( 'NONE', #11679 ) ;
#10419=CARTESIAN_POINT ( 'NONE',  ( 6.828503391016846891, 43.33193468930419101, 95.41433880123797451 ) ) ;
#10420=VERTEX_POINT ( 'NONE', #10297 ) ;
#10422=ORIENTED_EDGE ( 'NONE', *, *, #3250, .T. ) ;
#10423=CARTESIAN_POINT ( 'NONE',  ( 11.22215374030649926, 42.76218137147968434, 80.55433879953099563 ) ) ;
#10424=EDGE_CURVE ( 'NONE', #1387, #10593, #2088, .T. ) ;
#10431=CARTESIAN_POINT ( 'NONE',  ( -5.784195910403845176, 44.99242805365518194, 94.78933880123798872 ) ) ;
#10434=CARTESIAN_POINT ( 'NONE',  ( -3.350035803220276609, 49.20851703305431357, 91.97683880123797451 ) ) ;
#10435=CARTESIAN_POINT ( 'NONE',  ( 1.064787648071129134, 38.29826807256112176, 92.55433879953091036 ) ) ;
#10438=CARTESIAN_POINT ( 'NONE',  ( 6.102441102155617969, 43.42752260303680600, 92.36746380294498238 ) ) ;
#10446=CARTESIAN_POINT ( 'NONE',  ( -5.154188915835984375, 42.64120994080404614, 96.11746380123797451 ) ) ;
#10448=LINE ( 'NONE', #7003, #5865 ) ;
#10458=CARTESIAN_POINT ( 'NONE',  ( -3.430302262420787063, 39.98804081939900357, 95.05433879953099563 ) ) ;
#10465=CARTESIAN_POINT ( 'NONE',  ( 3.788215052820487205, 39.19523464621513398, 90.24306233796824017 ) ) ;
#10468=VERTEX_POINT ( 'NONE', #7819 ) ;
#10470=ORIENTED_EDGE ( 'NONE', *, *, #19762, .F. ) ;
#10472=CARTESIAN_POINT ( 'NONE',  ( -3.943187491250720544, 40.73580453397070755, 95.64871380294496817 ) ) ;
#10475=CARTESIAN_POINT ( 'NONE',  ( 11.22215374030649926, 45.56218137147968861, 80.55433879953099563 ) ) ;
#10494=AXIS2_PLACEMENT_3D ( 'NONE', #19075, #4582, #1407 ) ;
#10497=CARTESIAN_POINT ( 'NONE',  ( 4.987494971863720927, 47.58855820898865829, 94.71121379953099506 ) ) ;
#10498=CARTESIAN_POINT ( 'NONE',  ( -3.943187491250720544, 40.73580453397070755, 91.58621379953098085 ) ) ;
#10499=VERTEX_POINT ( 'NONE', #7396 ) ;
#10500=CARTESIAN_POINT ( 'NONE',  ( 6.828503391016846891, 43.33193468930419101, 92.91433880123798872 ) ) ;
#10504=CARTESIAN_POINT ( 'NONE',  ( 5.544968037009670780, 45.50804040601273925, 92.13308879953099506 ) ) ;
#10518=ORIENTED_EDGE ( 'NONE', *, *, #17456, .T. ) ;
#10526=EDGE_LOOP ( 'NONE', ( #8086, #17013, #1782, #14582 ) ) ;
#10527=CARTESIAN_POINT ( 'NONE',  ( -4.677846259693496656, 44.16218127507082158, 94.26911326394257173 ) ) ;
#10529=EDGE_CURVE ( 'NONE', #12799, #531, #9423, .T. ) ;
#10530=CARTESIAN_POINT ( 'NONE',  ( 3.460444912181559474, 49.25145096859824889, 92.99246380123805977 ) ) ;
#10536=CARTESIAN_POINT ( 'NONE',  ( -4.677846234370045764, 43.47758828951683796, 94.29575777171292827 ) ) ;
#10537=CARTESIAN_POINT ( 'NONE',  ( 5.544968037009670780, 45.50804040601273925, 92.44558880294498238 ) ) ;
#10544=MECHANICAL_DESIGN_GEOMETRIC_PRESENTATION_REPRESENTATION('',(#15668),#12889);
#10548=CARTESIAN_POINT ( 'NONE',  ( 11.22215374030650281, 48.36218137147968577, 54.55433879953099563 ) ) ;
#10550=CARTESIAN_POINT ( 'NONE',  ( 5.568489401881125289, 48.03437091500646261, 93.07058880123797451 ) ) ;
#10558=ORIENTED_EDGE ( 'NONE', *, *, #30, .F. ) ;
#10561=DIRECTION ( 'NONE',  ( -0.000000000000000000, 1.000000000000000000, 1.734723475976787531E-14 ) ) ;
#10567=CARTESIAN_POINT ( 'NONE',  ( 5.025485839985549319, 41.56218137147963887, 91.03933880294498238 ) ) ;
#10580=CARTESIAN_POINT ( 'NONE',  ( -3.981178359372548492, 46.76218137147973408, 95.41433880294498238 ) ) ;
#10585=CARTESIAN_POINT ( 'NONE',  ( 11.22215374030649926, 51.36218137147968577, 70.80574467885102763 ) ) ;
#10591=AXIS2_PLACEMENT_3D ( 'NONE', #17064, #20341, #5780 ) ;
#10593=VERTEX_POINT ( 'NONE', #2168 ) ;
#10594=LINE ( 'NONE', #7262, #285 ) ;
#10597=LINE ( 'NONE', #4274, #681 ) ;
#10602=ORIENTED_EDGE ( 'NONE', *, *, #14917, .F. ) ;
#10607=EDGE_CURVE ( 'NONE', #2282, #5117, #15148, .T. ) ;
#10608=CARTESIAN_POINT ( 'NONE',  ( 6.102441102155617969, 43.42752260303680600, 94.55496379953098085 ) ) ;
#10611=CARTESIAN_POINT ( 'NONE',  ( 1.352400422481993658, 50.46853102219002096, 94.47683880123798872 ) ) ;
#10615=DIRECTION ( 'NONE',  ( 2.409338161078896715E-16, -1.000000000000000000, 0.000000000000000000 ) ) ;
#10623=AXIS2_PLACEMENT_3D ( 'NONE', #1688, #6458, #18064 ) ;
#10624=DIRECTION ( 'NONE',  ( 0.000000000000000000, 0.000000000000000000, 1.000000000000000000 ) ) ;
#10628=DIRECTION ( 'NONE',  ( -0.000000000000000000, 1.000000000000000000, -0.000000000000000000 ) ) ;
#10635=CARTESIAN_POINT ( 'NONE',  ( 10.77494014480653561, 42.96218137147968008, 73.80433879953100984 ) ) ;
#10636=CARTESIAN_POINT ( 'NONE',  ( 3.788215052820487205, 39.19523464621513398, 90.24306233796824017 ) ) ;
#10652=CARTESIAN_POINT ( 'NONE',  ( 6.102441102155617969, 43.42752260303680600, 91.11746380294498238 ) ) ;
#10653=VECTOR ( 'NONE', #2318, 999.9999999999998863 ) ;
#10656=EDGE_CURVE ( 'NONE', #15803, #14953, #20128, .T. ) ;
#10657=ORIENTED_EDGE ( 'NONE', *, *, #18870, .F. ) ;
#10658=B_SPLINE_CURVE_WITH_KNOTS ( 'NONE', 3,
 ( #17899, #9826, #6717, #8729, #11530, #3427 ),
 .UNSPECIFIED., .F., .F.,
 ( 4, 2, 4 ),
 ( 0.000000000000000000, 0.001381175314065558610, 0.002762350628131117220 ),
 .UNSPECIFIED. ) ;
#10663=CARTESIAN_POINT ( 'NONE',  ( -7.677846259693485109, 51.36218137147968577, 93.55433879953098142 ) ) ;
#10664=VECTOR ( 'NONE', #15033, 1000.000000000000114 ) ;
#10675=LINE ( 'NONE', #18301, #19616 ) ;
#10677=CARTESIAN_POINT ( 'NONE',  ( 5.544968037009670780, 45.50804040601273925, 89.94558880294498238 ) ) ;
#10679=VECTOR ( 'NONE', #7233, 1000.000000000000000 ) ;
#10688=CARTESIAN_POINT ( 'NONE',  ( 5.025485839985549319, 41.56218137147963887, 94.78933880294496817 ) ) ;
#10691=CARTESIAN_POINT ( 'NONE',  ( 31.07218010054375412, 42.76218137147968434, 70.80574467885102763 ) ) ;
#10704=FACE_OUTER_BOUND ( 'NONE', #10526, .T. ) ;
#10705=CARTESIAN_POINT ( 'NONE',  ( -1.579458713458412822, 38.67424504376464967, 92.55433879953098142 ) ) ;
#10707=DIRECTION ( 'NONE',  ( -0.4999999999999984457, -0.8660254037844394848, -0.000000000000000000 ) ) ;
#10717=CARTESIAN_POINT ( 'NONE',  ( -3.981178359372548492, 46.76218137147973408, 96.35183879953099506 ) ) ;
#10720=CARTESIAN_POINT ( 'NONE',  ( 1.352400422481993658, 50.46853102219002096, 91.97683880123797451 ) ) ;
#10735=EDGE_LOOP ( 'NONE', ( #19799, #4521, #16780, #19857 ) ) ;
#10737=VERTEX_POINT ( 'NONE', #15682 ) ;
#10740=CARTESIAN_POINT ( 'NONE',  ( -4.567115856812060670, 47.10047254335474065, 94.55496380123798872 ) ) ;
#10748=CARTESIAN_POINT ( 'NONE',  ( -0.4699484075729998267, 52.36218137147968577, 87.21440135111343750 ) ) ;
#10754=CARTESIAN_POINT ( 'NONE',  ( -0.2125050281363792815, 38.58189400963056670, 94.55496380294496817 ) ) ;
#10755=CARTESIAN_POINT ( 'NONE',  ( 5.025485839985549319, 41.56218137147963887, 94.78933880294496817 ) ) ;
#10757=FILL_AREA_STYLE ('',( #18821 ) ) ;
#10761=CARTESIAN_POINT ( 'NONE',  ( 6.828503391016846891, 43.33193468930419101, 90.41433880123798872 ) ) ;
#10768=CARTESIAN_POINT ( 'NONE',  ( -3.664877280008365101, 47.31003091142736849, 92.57889353644220876 ) ) ;
#10780=VERTEX_POINT ( 'NONE', #6366 ) ;
#10784=EDGE_CURVE ( 'NONE', #4848, #16560, #4376, .T. ) ;
#10786=CARTESIAN_POINT ( 'NONE',  ( 6.102441102155617969, 43.42752260303680600, 91.11746380294498238 ) ) ;
#10791=DIRECTION ( 'NONE',  ( -0.000000000000000000, -0.000000000000000000, 1.000000000000000000 ) ) ;
#10796=ADVANCED_FACE ( 'NONE', ( #12866 ), #8879, .F. ) ;
#10798=DIRECTION ( 'NONE',  ( -0.000000000000000000, -0.000000000000000000, 1.000000000000000000 ) ) ;
#10804=PLANE ( 'NONE',  #9515 ) ;
#10805=EDGE_CURVE ( 'NONE', #7893, #17463, #9195, .T. ) ;
#10806=( BOUNDED_CURVE ( )  B_SPLINE_CURVE ( 2, ( #4556, #18833, #17542, #10768, #1068 ),
 .UNSPECIFIED., .F., .T. ) 
 B_SPLINE_CURVE_WITH_KNOTS ( ( 3, 2, 3 ),
 ( 0.6333811345117427161, 0.6500000000000000222, 0.6577596748367573465 ),
 .UNSPECIFIED. ) 
 CURVE ( )  GEOMETRIC_REPRESENTATION_ITEM ( )  RATIONAL_B_SPLINE_CURVE ( ( 0.9660722070828660080, 0.9493985675960723292, 1.000000000000000000, 0.9763731969546250999, 0.9674132986343875196 ) ) 
 REPRESENTATION_ITEM ( '' )  );
#10809=VERTEX_POINT ( 'NONE', #5776 ) ;
#10811=CARTESIAN_POINT ( 'NONE',  ( -3.350035803220276609, 49.20851703305431357, 93.38308880123798872 ) ) ;
#10813=ORIENTED_EDGE ( 'NONE', *, *, #17950, .F. ) ;
#10814=CARTESIAN_POINT ( 'NONE',  ( 4.394343283833276992, 39.11584570990505938, 92.75808880123797451 ) ) ;
#10816=DIRECTION ( 'NONE',  ( 0.8660254037844395958, -0.4999999999999985012, 0.000000000000000000 ) ) ;
#10823=LINE ( 'NONE', #7612, #5419 ) ;
#10824=CARTESIAN_POINT ( 'NONE',  ( 4.394343283833276992, 39.11584570990505938, 92.75808880123797451 ) ) ;
#10827=DIRECTION ( 'NONE',  ( 1.000000000000000000, -0.000000000000000000, -0.000000000000000000 ) ) ;
#10841=CARTESIAN_POINT ( 'NONE',  ( 1.352400422481993658, 50.46853102219002096, 91.97683880123797451 ) ) ;
#10852=EDGE_LOOP ( 'NONE', ( #19839, #415, #17725, #1406 ) ) ;
#10854=LINE ( 'NONE', #1362, #14516 ) ;
#10856=CARTESIAN_POINT ( 'NONE',  ( -4.567115856812060670, 47.10047254335474065, 95.80496380123798872 ) ) ;
#10858=CARTESIAN_POINT ( 'NONE',  ( 5.025485839985549319, 41.56218137147963887, 94.78933880294496817 ) ) ;
#10859=CARTESIAN_POINT ( 'NONE',  ( 5.025485839985549319, 41.56218137147963887, 93.53933880294496817 ) ) ;
#10866=CARTESIAN_POINT ( 'NONE',  ( -0.3080929418689875576, 37.85583172076933778, 91.35183880123798872 ) ) ;
#10869=ORIENTED_EDGE ( 'NONE', *, *, #6737, .F. ) ;
#10870=CARTESIAN_POINT ( 'NONE',  ( 11.22215374030650281, 42.76218137147968434, 78.80433879953099563 ) ) ;
#10872=DIRECTION ( 'NONE',  ( -1.193617070626243484E-16, -1.000000000000000000, -0.000000000000000000 ) ) ;
#10879=CARTESIAN_POINT ( 'NONE',  ( 6.828503391016846891, 43.33193468930419101, 91.50808880123798872 ) ) ;
#10888=CARTESIAN_POINT ( 'NONE',  ( 3.948530577815480225, 39.69684013992245752, 90.96121380294498238 ) ) ;
#10891=DIRECTION ( 'NONE',  ( -1.000000000000000000, 0.000000000000000000, 0.000000000000000000 ) ) ;
#10892=VECTOR ( 'NONE', #1327, 1000.000000000000000 ) ;
#10901=CARTESIAN_POINT ( 'NONE',  ( 6.828503391016846891, 43.33193468930419101, 95.25808880123800293 ) ) ;
#10904=CARTESIAN_POINT ( 'NONE',  ( 5.568489401881125289, 48.03437091500646261, 95.41433880123797451 ) ) ;
#10905=DIRECTION ( 'NONE',  ( 0.000000000000000000, -1.000000000000000000, -2.168404344970984808E-15 ) ) ;
#10906=CARTESIAN_POINT ( 'NONE',  ( 0.5221537403065010796, 44.16218137147969003, 50.15433879953098995 ) ) ;
#10914=CARTESIAN_POINT ( 'NONE',  ( -3.350035803220276609, 49.20851703305431357, 94.63308880123798872 ) ) ;
#10916=ORIENTED_EDGE ( 'NONE', *, *, #18204, .T. ) ;
#10928=CARTESIAN_POINT ( 'NONE',  ( 5.829886354652526137, 45.28396961230274087, 95.05433879953102405 ) ) ;
#10931=( BOUNDED_CURVE ( )  B_SPLINE_CURVE ( 2, ( #15445, #5751, #11658 ),
 .UNSPECIFIED., .F., .F. ) 
 B_SPLINE_CURVE_WITH_KNOTS ( ( 3, 3 ),
 ( 0.1123202270280673071, 0.1128933701044576160 ),
 .UNSPECIFIED. ) 
 CURVE ( )  GEOMETRIC_REPRESENTATION_ITEM ( )  RATIONAL_B_SPLINE_CURVE ( ( 0.9672500519790907525, 0.9666242557201361052, 0.9660722070857192811 ) ) 
 REPRESENTATION_ITEM ( '' )  );
#10937=CARTESIAN_POINT ( 'NONE',  ( 31.22215374030650281, 45.56218137147968861, 78.80433879953099563 ) ) ;
#10939=CARTESIAN_POINT ( 'NONE',  ( 2.043125170982144745, 38.48583871533720213, 92.67996380123798872 ) ) ;
#10942=ORIENTED_EDGE ( 'NONE', *, *, #18320, .F. ) ;
#10943=VECTOR ( 'NONE', #20411, 1000.000000000000000 ) ;
#10947=ORIENTED_EDGE ( 'NONE', *, *, #19232, .T. ) ;
#10955=CARTESIAN_POINT ( 'NONE',  ( 1.352400422481993658, 50.46853102219002096, 90.72683880123797451 ) ) ;
#10960=VECTOR ( 'NONE', #12072, 1000.000000000000000 ) ;
#10961=CARTESIAN_POINT ( 'NONE',  ( 35.92215374030650565, 51.36218137147967866, 45.55433879953098852 ) ) ;
#10962=EDGE_CURVE ( 'NONE', #4614, #7590, #20550, .T. ) ;
#10964=AXIS2_PLACEMENT_3D ( 'NONE', #5498, #7081, #13283 ) ;
#10967=DIRECTION ( 'NONE',  ( -1.000000000000000000, 0.000000000000000000, 0.000000000000000000 ) ) ;
#10972=CARTESIAN_POINT ( 'NONE',  ( 5.722153740306498371, 44.16218137147968292, 94.58161078214052964 ) ) ;
#10976=VECTOR ( 'NONE', #10628, 1000.000000000000000 ) ;
#10987=CARTESIAN_POINT ( 'NONE',  ( 5.611423337425062385, 41.22389019960463230, 90.17996380123798872 ) ) ;
#10990=VECTOR ( 'NONE', #17959, 1000.000000000000000 ) ;
#10991=CARTESIAN_POINT ( 'NONE',  ( 10.77494014480653561, 42.96218137147968008, 69.40574467885102194 ) ) ;
#10994=CARTESIAN_POINT ( 'NONE',  ( -3.943187491250720544, 40.73580453397070755, 91.89871380294498238 ) ) ;
#10997=CARTESIAN_POINT ( 'NONE',  ( -2.077846259693550746, 39.65884927180063357, 94.16433879953098085 ) ) ;
#10999=FACE_OUTER_BOUND ( 'NONE', #6811, .T. ) ;
#11002=ORIENTED_EDGE ( 'NONE', *, *, #1771, .T. ) ;
#11006=CARTESIAN_POINT ( 'NONE',  ( -5.784195910403845176, 44.99242805365518194, 93.38308880123798872 ) ) ;
#11007=CARTESIAN_POINT ( 'NONE',  ( -5.784195910403845176, 44.99242805365518194, 94.63308880123798872 ) ) ;
#11008=DIRECTION ( 'NONE',  ( -0.000000000000000000, -0.000000000000000000, 1.000000000000000000 ) ) ;
#11012=CARTESIAN_POINT ( 'NONE',  ( 2.263363662449209279, 49.77488197367684819, 94.28606768333811772 ) ) ;
#11016=CARTESIAN_POINT ( 'NONE',  ( 4.987494971863720927, 47.58855820898865829, 90.96121379953099506 ) ) ;
#11018=VERTEX_POINT ( 'NONE', #18956 ) ;
#11019=ADVANCED_FACE ( 'NONE', ( #1199, #7684 ), #15011, .T. ) ;
#11021=FACE_OUTER_BOUND ( 'NONE', #5115, .T. ) ;
#11026=CARTESIAN_POINT ( 'NONE',  ( 5.568489401881125289, 48.03437091500646261, 90.57058880123798872 ) ) ;
#11029=CARTESIAN_POINT ( 'NONE',  ( 4.374958955798271099, 39.84603773934203019, 95.05433879953099563 ) ) ;
#11040=CARTESIAN_POINT ( 'NONE',  ( 30.92220646078100188, 45.56218137147968861, 62.80715055817104542 ) ) ;
#11041=CARTESIAN_POINT ( 'NONE',  ( -2.416137431568557314, 39.07291177436112406, 91.27371380123798872 ) ) ;
#11045=EDGE_CURVE ( 'NONE', #1084, #17463, #16607, .T. ) ;
#11048=DIRECTION ( 'NONE',  ( 0.000000000000000000, -1.000000000000000000, 2.168404344970984413E-15 ) ) ;
#11051=CARTESIAN_POINT ( 'NONE',  ( -3.154801521863568325, 47.83913663364971569, 83.28180655319408743 ) ) ;
#11053=EDGE_LOOP ( 'NONE', ( #13460, #11202, #15495, #7989 ) ) ;
#11057=CARTESIAN_POINT ( 'NONE',  ( -4.567115856812060670, 47.10047254335474065, 92.21121380123797451 ) ) ;
#11061=ADVANCED_FACE ( 'NONE', ( #6914 ), #14691, .F. ) ;
#11068=EDGE_CURVE ( 'NONE', #20901, #19399, #4645, .T. ) ;
#11070=CARTESIAN_POINT ( 'NONE',  ( -5.784195910403845176, 44.99242805365518194, 91.03933880123798872 ) ) ;
#11078=EDGE_CURVE ( 'NONE', #15788, #15252, #16188, .T. ) ;
#11080=CARTESIAN_POINT ( 'NONE',  ( 1.256812508749381774, 49.74246873332880625, 91.11746379953096664 ) ) ;
#11081=DIRECTION ( 'NONE',  ( 0.000000000000000000, 0.000000000000000000, -1.000000000000000000 ) ) ;
#11093=CARTESIAN_POINT ( 'NONE',  ( 3.122153740306552905, 48.66551347115873227, 92.60183880294498238 ) ) ;
#11098=DIRECTION ( 'NONE',  ( 0.000000000000000000, 0.000000000000000000, -1.000000000000000000 ) ) ;
#11101=CARTESIAN_POINT ( 'NONE',  ( 35.92215374030650565, 36.96218137147968719, 45.55433879953098852 ) ) ;
#11106=CARTESIAN_POINT ( 'NONE',  ( -5.784195910403845176, 44.99242805365518194, 95.88308880123798872 ) ) ;
#11114=VECTOR ( 'NONE', #10827, 1000.000000000000000 ) ;
#11116=CARTESIAN_POINT ( 'NONE',  ( -0.3080929418689875576, 37.85583172076933778, 93.85183880123797451 ) ) ;
#11124=CARTESIAN_POINT ( 'NONE',  ( -4.826915440150258974, 45.06110468568228100, 92.55433879953100984 ) ) ;
#11125=CARTESIAN_POINT ( 'NONE',  ( -0.9988176903691428077, 49.83852402762217082, 92.05496380123798872 ) ) ;
#11128=CARTESIAN_POINT ( 'NONE',  ( 5.892585134170466254, 42.58711300521386534, 95.05433879953099563 ) ) ;
#11144=CARTESIAN_POINT ( 'NONE',  ( -5.784195910403845176, 44.99242805365518194, 93.53933880123797451 ) ) ;
#11154=VERTEX_POINT ( 'NONE', #5634 ) ;
#11156=DIRECTION ( 'NONE',  ( 1.334402673828313339E-16, 1.871524341742854397E-32, -1.000000000000000000 ) ) ;
#11158=CARTESIAN_POINT ( 'NONE',  ( -2.416137431568557314, 39.07291177436112406, 93.77371380123797451 ) ) ;
#11160=EDGE_CURVE ( 'NONE', #14970, #19160, #13940, .T. ) ;
#11166=ORIENTED_EDGE ( 'NONE', *, *, #8459, .F. ) ;
#11168=DIRECTION ( 'NONE',  ( 1.193617070626243484E-16, 1.000000000000000000, 0.000000000000000000 ) ) ;
#11171=CIRCLE ( 'NONE', #7051, 0.9921021478795063464 ) ;
#11174=VERTEX_POINT ( 'NONE', #16716 ) ;
#11178=CARTESIAN_POINT ( 'NONE',  ( -4.677846259693498432, 44.16218137147969003, 93.95661078214054385 ) ) ;
#11188=ADVANCED_FACE ( 'NONE', ( #959 ), #3718, .F. ) ;
#11190=ORIENTED_EDGE ( 'NONE', *, *, #13078, .F. ) ;
#11193=VERTEX_POINT ( 'NONE', #10239 ) ;
#11197=FACE_OUTER_BOUND ( 'NONE', #16409, .T. ) ;
#11199=ORIENTED_EDGE ( 'NONE', *, *, #14580, .F. ) ;
#11202=ORIENTED_EDGE ( 'NONE', *, *, #11859, .T. ) ;
#11203=CARTESIAN_POINT ( 'NONE',  ( -5.154188915835984375, 42.64120994080404614, 95.96121380123798872 ) ) ;
#11205=VECTOR ( 'NONE', #17241, 1000.000000000000000 ) ;
#11206=CARTESIAN_POINT ( 'NONE',  ( 5.568489401881125289, 48.03437091500646261, 94.16433880123797451 ) ) ;
#11211=VECTOR ( 'NONE', #12320, 1000.000000000000000 ) ;
#11216=ORIENTED_EDGE ( 'NONE', *, *, #12621, .F. ) ;
#11220=CARTESIAN_POINT ( 'NONE',  ( 5.611423337425062385, 41.22389019960463230, 95.33621380123798872 ) ) ;
#11226=CARTESIAN_POINT ( 'NONE',  ( 2.196093689222912371, 38.51591816243362842, 95.05433879953096721 ) ) ;
#11235=CARTESIAN_POINT ( 'NONE',  ( 3.321299285246416488, 39.00526458700550592, 95.05433879953096721 ) ) ;
#11239=CIRCLE ( 'NONE', #5801, 0.9921021478795020165 ) ;
#11241=CARTESIAN_POINT ( 'NONE',  ( 11.22215374030649926, 45.56218137147968861, 70.80574467885102763 ) ) ;
#11250=FACE_OUTER_BOUND ( 'NONE', #2036, .T. ) ;
#11253=ORIENTED_EDGE ( 'NONE', *, *, #14917, .T. ) ;
#11264=ORIENTED_EDGE ( 'NONE', *, *, #9217, .T. ) ;
#11265=DIRECTION ( 'NONE',  ( 1.000000000000000000, 1.402518428993831676E-16, 1.621236893436268400E-16 ) ) ;
#11268=CARTESIAN_POINT ( 'NONE',  ( -0.9988176903691428077, 49.83852402762217082, 92.05496380123798872 ) ) ;
#11273=DIRECTION ( 'NONE',  ( -0.000000000000000000, -0.000000000000000000, 1.000000000000000000 ) ) ;
#11283=DIRECTION ( 'NONE',  ( -1.621236893436268647E-16, -2.273814620809075225E-32, 1.000000000000000000 ) ) ;
#11288=AXIS2_PLACEMENT_3D ( 'NONE', #3349, #17822, #5041 ) ;
#11294=EDGE_CURVE ( 'NONE', #16713, #14953, #4346, .T. ) ;
#11296=CARTESIAN_POINT ( 'NONE',  ( 0.5221537403065010796, 44.16218137147969003, 77.84651775085080772 ) ) ;
#11300=VECTOR ( 'NONE', #6147, 1000.000000000000000 ) ;
#11301=CARTESIAN_POINT ( 'NONE',  ( 30.92220646078100188, 42.96218137147968008, 61.40715055817103263 ) ) ;
#11302=VECTOR ( 'NONE', #7038, 1000.000000000000000 ) ;
#11308=DIRECTION ( 'NONE',  ( 1.193617070626243484E-16, 1.000000000000000000, 0.000000000000000000 ) ) ;
#11310=ORIENTED_EDGE ( 'NONE', *, *, #18857, .T. ) ;
#11313=CARTESIAN_POINT ( 'NONE',  ( 5.611423337425062385, 41.22389019960463230, 93.92996380123798872 ) ) ;
#11314=CARTESIAN_POINT ( 'NONE',  ( -2.416137431568557314, 39.07291177436112406, 91.11746380123798872 ) ) ;
#11316=AXIS2_PLACEMENT_3D ( 'NONE', #3016, #10816, #9522 ) ;
#11321=VERTEX_POINT ( 'NONE', #3080 ) ;
#11324=DIRECTION ( 'NONE',  ( 0.000000000000000000, 0.000000000000000000, 1.000000000000000000 ) ) ;
#11327=CARTESIAN_POINT ( 'NONE',  ( -7.677846259693481556, 40.96218137147969429, 93.55433879953098142 ) ) ;
#11331=CARTESIAN_POINT ( 'NONE',  ( 5.214985644788185937, 40.92083184153662501, 92.55433879953100984 ) ) ;
#11333=EDGE_CURVE ( 'NONE', #2806, #2513, #10806, .T. ) ;
#11335=ORIENTED_EDGE ( 'NONE', *, *, #20892, .T. ) ;
#11340=LINE ( 'NONE', #3236, #16231 ) ;
#11342=EDGE_CURVE ( 'NONE', #15997, #5268, #1489, .T. ) ;
#11347=CARTESIAN_POINT ( 'NONE',  ( -1.183761187420877548, 49.81017696809242068, 92.55433879953098142 ) ) ;
#11354=DIRECTION ( 'NONE',  ( 1.000000000000000000, -1.193617070626243484E-16, 0.000000000000000000 ) ) ;
#11355=PLANE ( 'NONE',  #18413 ) ;
#11362=CARTESIAN_POINT ( 'NONE',  ( -0.2125050281363792815, 38.58189400963055959, 94.24246379953099506 ) ) ;
#11371=PLANE ( 'NONE',  #245 ) ;
#11391=DIRECTION ( 'NONE',  ( -1.000000000000000000, -5.084437235940625660E-16, -0.000000000000000000 ) ) ;
#11393=CARTESIAN_POINT ( 'NONE',  ( 10.77494014480653917, 42.96218137147968008, 61.80715055817104542 ) ) ;
#11397=CARTESIAN_POINT ( 'NONE',  ( -2.416137431568557314, 39.07291177436112406, 91.11746380123798872 ) ) ;
#11398=ORIENTED_EDGE ( 'NONE', *, *, #20230, .F. ) ;
#11415=CARTESIAN_POINT ( 'NONE',  ( 6.828503391016846891, 43.33193468930419101, 92.75808880123800293 ) ) ;
#11416=FACE_OUTER_BOUND ( 'NONE', #16309, .T. ) ;
#11427=CARTESIAN_POINT ( 'NONE',  ( -0.9988176903691428077, 49.83852402762217082, 94.39871380123798872 ) ) ;
#11430=CARTESIAN_POINT ( 'NONE',  ( -5.945795452124602143, 37.96218137147967298, 45.55433879953098852 ) ) ;
#11434=LINE ( 'NONE', #12709, #9274 ) ;
#11438=VERTEX_POINT ( 'NONE', #8289 ) ;
#11445=DIRECTION ( 'NONE',  ( 0.000000000000000000, -1.000000000000000000, 0.000000000000000000 ) ) ;
#11446=EDGE_CURVE ( 'NONE', #15205, #15934, #19341, .T. ) ;
#11447=LINE ( 'NONE', #11347, #749 ) ;
#11456=FACE_BOUND ( 'NONE', #9018, .T. ) ;
#11466=CARTESIAN_POINT ( 'NONE',  ( 3.948530577815480225, 39.69684013992245752, 93.14871379953099506 ) ) ;
#11470=ORIENTED_EDGE ( 'NONE', *, *, #4537, .F. ) ;
#11481=ORIENTED_EDGE ( 'NONE', *, *, #14396, .F. ) ;
#11487=( BOUNDED_CURVE ( )  B_SPLINE_CURVE ( 2, ( #2713, #17496, #15704, #12609, #1125, #19095, #12917, #12502, #9324, #2920, #2820 ),
 .UNSPECIFIED., .F., .T. ) 
 B_SPLINE_CURVE_WITH_KNOTS ( ( 3, 2, 2, 2, 2, 3 ),
 ( 0.5333811345117427383, 0.5500000000000000444, 0.5749999999999999556, 0.5999999999999999778, 0.6250000000000000000, 0.6333811345117427161 ),
 .UNSPECIFIED. ) 
 CURVE ( )  GEOMETRIC_REPRESENTATION_ITEM ( )  RATIONAL_B_SPLINE_CURVE ( ( 0.9660722070828660080, 0.9493985675960723292, 1.000000000000000000, 0.9238795325112867385, 1.000000000000000000, 0.9238795325112867385, 1.000000000000000000, 0.9238795325112867385, 1.000000000000000000, 0.9744809649152141873, 0.9660722070828660080 ) ) 
 REPRESENTATION_ITEM ( '' )  );
#11488=ADVANCED_FACE ( 'NONE', ( #19959 ), #3804, .F. ) ;
#11490=FACE_OUTER_BOUND ( 'NONE', #13727, .T. ) ;
#11492=AXIS2_PLACEMENT_3D ( 'NONE', #11393, #6577, #17647 ) ;
#11493=CARTESIAN_POINT ( 'NONE',  ( 5.544968037009670780, 45.50804040601273925, 93.69558880294498238 ) ) ;
#11496=CARTESIAN_POINT ( 'NONE',  ( -3.981178359372548492, 46.76218137147973408, 94.16433880294496817 ) ) ;
#11498=VECTOR ( 'NONE', #718, 1000.000000000000000 ) ;
#11502=CARTESIAN_POINT ( 'NONE',  ( 1.352400422481993658, 50.46853102219002096, 94.32058880123798872 ) ) ;
#11505=VECTOR ( 'NONE', #199, 1000.000000000000000 ) ;
#11511=ORIENTED_EDGE ( 'NONE', *, *, #11701, .F. ) ;
#11514=DIRECTION ( 'NONE',  ( -0.7071067811865434649, 0.7071067811865515695, 0.000000000000000000 ) ) ;
#11519=ORIENTED_EDGE ( 'NONE', *, *, #20241, .T. ) ;
#11520=CARTESIAN_POINT ( 'NONE',  ( 4.987494971863720927, 47.58855820898865829, 95.02371380294496817 ) ) ;
#11526=DIRECTION ( 'NONE',  ( 1.000000000000000000, 0.000000000000000000, 0.000000000000000000 ) ) ;
#11527=VECTOR ( 'NONE', #9341, 1000.000000000000000 ) ;
#11530=CARTESIAN_POINT ( 'NONE',  ( 3.873544841512769121, 48.16470079461351617, 94.75578198602110547 ) ) ;
#11531=CARTESIAN_POINT ( 'NONE',  ( -0.9988176903691428077, 49.83852402762217082, 95.64871380123798872 ) ) ;
#11535=CARTESIAN_POINT ( 'NONE',  ( 4.819906901611561878, 40.37133391887874012, 92.55433879953100984 ) ) ;
#11538=ORIENTED_EDGE ( 'NONE', *, *, #1121, .F. ) ;
#11545=VECTOR ( 'NONE', #17437, 1000.000000000000000 ) ;
#11546=DIRECTION ( 'NONE',  ( 1.000000000000000000, 0.000000000000000000, 0.000000000000000000 ) ) ;
#11556=DIRECTION ( 'NONE',  ( 0.5000000000000061062, 1.204669080539463149E-16, 0.8660254037844351549 ) ) ;
#11557=FACE_OUTER_BOUND ( 'NONE', #12100, .T. ) ;
#11567=DIRECTION ( 'NONE',  ( 0.7071067811865433539, 0.7071067811865516806, -0.000000000000000000 ) ) ;
#11569=CARTESIAN_POINT ( 'NONE',  ( 4.987494971863720927, 47.58855820898865829, 94.71121379953099506 ) ) ;
#11574=VECTOR ( 'NONE', #8979, 1000.000000000000000 ) ;
#11582=VECTOR ( 'NONE', #973, 1000.000000000000000 ) ;
#11583=CARTESIAN_POINT ( 'NONE',  ( -7.677846259693485109, 51.36218137147968577, 80.55433879953099563 ) ) ;
#11587=ORIENTED_EDGE ( 'NONE', *, *, #8291, .T. ) ;
#11589=DIRECTION ( 'NONE',  ( 1.000000000000000000, 0.000000000000000000, -0.000000000000000000 ) ) ;
#11590=CYLINDRICAL_SURFACE ( 'NONE', #7572, 6.200000000000000178 ) ;
#11592=ORIENTED_EDGE ( 'NONE', *, *, #11045, .T. ) ;
#11593=EDGE_LOOP ( 'NONE', ( #19174, #15090, #16838, #14205 ) ) ;
#11605=CARTESIAN_POINT ( 'NONE',  ( 31.07218010054375412, 45.56218137147968861, 70.80574467885102763 ) ) ;
#11608=EDGE_CURVE ( 'NONE', #15667, #3488, #10854, .T. ) ;
#11609=CARTESIAN_POINT ( 'NONE',  ( -2.416137431568557314, 39.07291177436112406, 92.36746380123797451 ) ) ;
#11619=ORIENTED_EDGE ( 'NONE', *, *, #8726, .T. ) ;
#11625=ORIENTED_EDGE ( 'NONE', *, *, #8459, .T. ) ;
#11629=CARTESIAN_POINT ( 'NONE',  ( 5.568489401881125289, 48.03437091500646261, 90.41433880123798872 ) ) ;
#11632=CARTESIAN_POINT ( 'NONE',  ( -4.567115856812060670, 47.10047254335474065, 95.80496380123798872 ) ) ;
#11635=VERTEX_POINT ( 'NONE', #12532 ) ;
#11639=CARTESIAN_POINT ( 'NONE',  ( 31.22215374030650281, 42.96218137147968008, 77.80433879953099563 ) ) ;
#11641=ORIENTED_EDGE ( 'NONE', *, *, #1633, .F. ) ;
#11644=CARTESIAN_POINT ( 'NONE',  ( 2.916646314870772194, 38.79555996194921619, 92.55433879953098142 ) ) ;
#11655=CARTESIAN_POINT ( 'NONE',  ( -3.226449543290803135, 47.76606447477306716, 95.05433879953076826 ) ) ;
#11658=CARTESIAN_POINT ( 'NONE',  ( 4.199109002476567376, 47.83913663364971569, 95.05036078555451695 ) ) ;
#11665=DIRECTION ( 'NONE',  ( 0.000000000000000000, -1.000000000000000000, -2.168404344970984413E-15 ) ) ;
#11667=CARTESIAN_POINT ( 'NONE',  ( -3.981178359372548492, 46.76218137147973408, 96.35183879953099506 ) ) ;
#11674=CARTESIAN_POINT ( 'NONE',  ( 11.22215374030649926, 45.56218137147968861, 80.55433879953099563 ) ) ;
#11675=CARTESIAN_POINT ( 'NONE',  ( 6.102441102155617969, 43.42752260303680600, 93.30496379953098085 ) ) ;
#11679=CARTESIAN_POINT ( 'NONE',  ( 1.514255888186008203, 51.36218137147968577, 48.36106904222365444 ) ) ;
#11680=CARTESIAN_POINT ( 'NONE',  ( 4.199109002476567376, 47.83913663364971569, 93.80036078555450274 ) ) ;
#11681=CARTESIAN_POINT ( 'NONE',  ( -3.350035803220276609, 49.20851703305431357, 94.47683880123798872 ) ) ;
#11682=VECTOR ( 'NONE', #5078, 1000.000000000000000 ) ;
#11683=LINE ( 'NONE', #5371, #18694 ) ;
#11694=CARTESIAN_POINT ( 'NONE',  ( -0.3080929418689875576, 37.85583172076933778, 93.85183880123797451 ) ) ;
#11699=ORIENTED_EDGE ( 'NONE', *, *, #2758, .F. ) ;
#11701=EDGE_CURVE ( 'NONE', #12731, #15579, #9672, .T. ) ;
#11702=FACE_OUTER_BOUND ( 'NONE', #8309, .T. ) ;
#11703=LINE ( 'NONE', #17966, #15044 ) ;
#11704=DIRECTION ( 'NONE',  ( 1.000000000000000000, 1.402518428993831676E-16, 0.000000000000000000 ) ) ;
#11709=CARTESIAN_POINT ( 'NONE',  ( -0.3080929418689875576, 37.85583172076933778, 93.69558880123800293 ) ) ;
#11710=CARTESIAN_POINT ( 'NONE',  ( 5.568489401881125289, 48.03437091500646261, 94.16433880123797451 ) ) ;
#11720=CARTESIAN_POINT ( 'NONE',  ( 0.5221537403065097394, 44.16218137147969003, 92.55433879953098142 ) ) ;
#11721=ADVANCED_FACE ( 'NONE', ( #19739 ), #11371, .F. ) ;
#11725=CARTESIAN_POINT ( 'NONE',  ( 4.199109002476567376, 47.83913663364971569, 92.55433879953098142 ) ) ;
#11727=ORIENTED_EDGE ( 'NONE', *, *, #15969, .F. ) ;
#11732=CARTESIAN_POINT ( 'NONE',  ( 3.460444912181559474, 49.25145096859824889, 92.99246380123798872 ) ) ;
#11734=CARTESIAN_POINT ( 'NONE',  ( 3.460444912181559474, 49.25145096859824889, 95.49246380123798872 ) ) ;
#11738=CARTESIAN_POINT ( 'NONE',  ( 10.77494014480653917, 42.76218137147968434, 57.80715055817105252 ) ) ;
#11741=EDGE_CURVE ( 'NONE', #5518, #20901, #9983, .T. ) ;
#11742=CARTESIAN_POINT ( 'NONE',  ( 6.828503391016846891, 43.33193468930419101, 95.25808880123800293 ) ) ;
#11747=LINE ( 'NONE', #16633, #12542 ) ;
#11766=CARTESIAN_POINT ( 'NONE',  ( -5.058133621542618030, 44.89684013992257405, 95.17996379953099506 ) ) ;
#11775=CARTESIAN_POINT ( 'NONE',  ( 3.460444912181559474, 49.25145096859824889, 94.39871380123798872 ) ) ;
#11790=CARTESIAN_POINT ( 'NONE',  ( -5.154188915835984375, 42.64120994080404614, 93.61746380123797451 ) ) ;
#11791=ORIENTED_EDGE ( 'NONE', *, *, #1603, .F. ) ;
#11793=AXIS2_PLACEMENT_3D ( 'NONE', #19680, #1614, #8416 ) ;
#11801=CARTESIAN_POINT ( 'NONE',  ( 0.5221537403065010796, 44.16218137147969003, 77.84651775085080772 ) ) ;
#11805=CARTESIAN_POINT ( 'NONE',  ( 3.460444912181559474, 49.25145096859824889, 90.49246380123798872 ) ) ;
#11812=PLANE ( 'NONE',  #16719 ) ;
#11814=CARTESIAN_POINT ( 'NONE',  ( 4.987494971863720927, 47.58855820898865829, 90.96121379953099506 ) ) ;
#11818=EDGE_CURVE ( 'NONE', #13327, #3871, #15203, .T. ) ;
#11829=CARTESIAN_POINT ( 'NONE',  ( -3.981178359372548492, 46.76218137147973408, 92.91433880294496817 ) ) ;
#11832=EDGE_CURVE ( 'NONE', #4650, #19160, #16421, .T. ) ;
#11833=CARTESIAN_POINT ( 'NONE',  ( -3.350035803220276609, 49.20851703305431357, 94.47683880123798872 ) ) ;
#11839=VERTEX_POINT ( 'NONE', #6822 ) ;
#11841=CARTESIAN_POINT ( 'NONE',  ( -0.9988176903691428077, 49.83852402762217082, 91.89871380123798872 ) ) ;
#11845=DIRECTION ( 'NONE',  ( -1.334402673828313832E-16, 2.891205793294680792E-16, 1.000000000000000000 ) ) ;
#11859=EDGE_CURVE ( 'NONE', #7741, #14613, #5431, .T. ) ;
#11862=ORIENTED_EDGE ( 'NONE', *, *, #14396, .T. ) ;
#11866=CARTESIAN_POINT ( 'NONE',  ( -3.154801521863568325, 47.83913663364971569, 93.80036078214054385 ) ) ;
#11867=CARTESIAN_POINT ( 'NONE',  ( 1.256812508749381774, 49.74246873332880625, 93.61746379953098085 ) ) ;
#11868=CARTESIAN_POINT ( 'NONE',  ( 1.256812508749381774, 49.74246873332880625, 92.36746379953098085 ) ) ;
#11872=VERTEX_POINT ( 'NONE', #16730 ) ;
#11877=VECTOR ( 'NONE', #6617, 1000.000000000000000 ) ;
#11878=CARTESIAN_POINT ( 'NONE',  ( 5.568489401881125289, 48.03437091500646261, 94.32058880123798872 ) ) ;
#11882=CARTESIAN_POINT ( 'NONE',  ( 10.77494014480653917, 42.96218137147968008, 57.80715055817105252 ) ) ;
#11883=AXIS2_PLACEMENT_3D ( 'NONE', #19922, #6742, #13247 ) ;
#11894=VECTOR ( 'NONE', #3683, 1000.000000000000000 ) ;
#11896=CARTESIAN_POINT ( 'NONE',  ( 11.22215374030649926, 51.36218137147968577, 80.55433879953099563 ) ) ;
#11904=ORIENTED_EDGE ( 'NONE', *, *, #19154, .T. ) ;
#11909=LINE ( 'NONE', #3694, #16068 ) ;
#11910=CARTESIAN_POINT ( 'NONE',  ( 1.352400422481993658, 50.46853102219002096, 94.47683880123798872 ) ) ;
#11917=CARTESIAN_POINT ( 'NONE',  ( -5.154188915835984375, 42.64120994080404614, 92.21121380123797451 ) ) ;
#11925=CARTESIAN_POINT ( 'NONE',  ( -0.9988176903691428077, 49.83852402762217082, 92.05496380123798872 ) ) ;
#11935=EDGE_LOOP ( 'NONE', ( #19461, #18154, #61, #4166, #17261, #13633, #1463, #14923, #20496, #4465, #15348, #9159 ) ) ;
#11936=DIRECTION ( 'NONE',  ( 0.000000000000000000, -1.000000000000000000, 0.000000000000000000 ) ) ;
#11937=CARTESIAN_POINT ( 'NONE',  ( -4.335999953777515792, 46.33399087051191145, 95.05433879953096721 ) ) ;
#11938=ADVANCED_FACE ( 'NONE', ( #8327 ), #6714, .F. ) ;
#11940=CARTESIAN_POINT ( 'NONE',  ( 6.102441102155617969, 43.42752260303680600, 92.36746380294498238 ) ) ;
#11941=CARTESIAN_POINT ( 'NONE',  ( 3.460444912181559474, 49.25145096859824889, 94.24246380123798872 ) ) ;
#11943=CARTESIAN_POINT ( 'NONE',  ( -4.524181921268124462, 40.28999182795290324, 93.53933880123797451 ) ) ;
#11948=EDGE_LOOP ( 'NONE', ( #3686, #6885, #15707, #20093 ) ) ;
#11952=CARTESIAN_POINT ( 'NONE',  ( 6.828503391016846891, 43.33193468930419101, 90.25808880123800293 ) ) ;
#11956=DIRECTION ( 'NONE',  ( -0.7071067811865435759, -0.7071067811865515695, -0.000000000000000000 ) ) ;
#11964=CARTESIAN_POINT ( 'NONE',  ( -0.4699484075730043786, 51.36218137147968577, 52.53721119516358584 ) ) ;
#11966=CARTESIAN_POINT ( 'NONE',  ( 4.394343283833276104, 39.11584570990505938, 92.75808880123797451 ) ) ;
#11967=EDGE_CURVE ( 'NONE', #1387, #8963, #13637, .T. ) ;
#11972=ORIENTED_EDGE ( 'NONE', *, *, #8470, .F. ) ;
#11978=CARTESIAN_POINT ( 'NONE',  ( -2.904223097202481174, 48.62752260303690122, 96.27371379953099506 ) ) ;
#11979=CARTESIAN_POINT ( 'NONE',  ( 5.025485839985549319, 41.56218137147963887, 95.72683879953099506 ) ) ;
#11989=CARTESIAN_POINT ( 'NONE',  ( -3.981178359372548492, 46.76218137147973408, 91.35183879953098085 ) ) ;
#11994=ORIENTED_EDGE ( 'NONE', *, *, #18363, .F. ) ;
#11995=CARTESIAN_POINT ( 'NONE',  ( -4.477846259693498254, 36.96218137147968008, 54.55433879953098852 ) ) ;
#11998=CARTESIAN_POINT ( 'NONE',  ( -0.9988176903691428077, 49.83852402762217082, 90.64871380123798872 ) ) ;
#12012=ORIENTED_EDGE ( 'NONE', *, *, #3960, .T. ) ;
#12022=CARTESIAN_POINT ( 'NONE',  ( -4.567115856812060670, 47.10047254335474065, 94.71121380123797451 ) ) ;
#12026=CARTESIAN_POINT ( 'NONE',  ( -2.904223097202481174, 48.62752260303690122, 94.08621380294496817 ) ) ;
#12028=ORIENTED_EDGE ( 'NONE', *, *, #416, .F. ) ;
#12030=AXIS2_PLACEMENT_3D ( 'NONE', #11882, #10624, #5589 ) ;
#12035=CARTESIAN_POINT ( 'NONE',  ( 6.198496396448986090, 45.68315280215533392, 92.99246380123798872 ) ) ;
#12042=DIRECTION ( 'NONE',  ( -0.8660254037844397068, -0.4999999999999981126, -0.000000000000000000 ) ) ;
#12045=CARTESIAN_POINT ( 'NONE',  ( -3.105421771460856295, 39.66752508378051090, 95.05433879953098142 ) ) ;
#12049=CARTESIAN_POINT ( 'NONE',  ( 11.22215374030650281, 42.76218137147968434, 69.80574467885101342 ) ) ;
#12050=CARTESIAN_POINT ( 'NONE',  ( -3.350035803220276609, 49.20851703305431357, 93.22683880123798872 ) ) ;
#12056=CARTESIAN_POINT ( 'NONE',  ( 3.948530577815480225, 39.69684013992245752, 94.71121380294496817 ) ) ;
#12058=CARTESIAN_POINT ( 'NONE',  ( 2.722153740306497927, 50.36218137147968577, 50.15433879953098995 ) ) ;
#12060=DIRECTION ( 'NONE',  ( 1.000000000000000000, -0.000000000000000000, -0.000000000000000000 ) ) ;
#12065=ORIENTED_EDGE ( 'NONE', *, *, #19875, .T. ) ;
#12068=DIRECTION ( 'NONE',  ( 0.8660254037844399289, 0.4999999999999977796, 0.000000000000000000 ) ) ;
#12069=ADVANCED_FACE ( 'NONE', ( #2472 ), #18946, .F. ) ;
#12072=DIRECTION ( 'NONE',  ( 4.818676322157797375E-16, 1.000000000000000000, -0.000000000000000000 ) ) ;
#12078=CARTESIAN_POINT ( 'NONE',  ( 5.025485839985549319, 41.56218137147963887, 94.47683879953099506 ) ) ;
#12079=CARTESIAN_POINT ( 'NONE',  ( -3.943187491250720544, 40.73580453397070755, 96.58621379953099506 ) ) ;
#12081=CARTESIAN_POINT ( 'NONE',  ( 4.394343283833276992, 39.11584570990505938, 94.00808880123797451 ) ) ;
#12082=CARTESIAN_POINT ( 'NONE',  ( -5.784195910403845176, 44.99242805365518194, 94.63308880123808819 ) ) ;
#12085=CARTESIAN_POINT ( 'NONE',  ( 1.256812508749381774, 49.74246873332880625, 92.36746379953098085 ) ) ;
#12089=CARTESIAN_POINT ( 'NONE',  ( -3.350035803220276609, 49.20851703305431357, 94.63308880123798872 ) ) ;
#12094=PLANE ( 'NONE',  #12030 ) ;
#12100=EDGE_LOOP ( 'NONE', ( #10813, #20953, #19649, #15178 ) ) ;
#12107=CARTESIAN_POINT ( 'NONE',  ( -4.567115856812060670, 47.10047254335474065, 94.71121380123797451 ) ) ;
#12109=LINE ( 'NONE', #15409, #5542 ) ;
#12116=FACE_OUTER_BOUND ( 'NONE', #2963, .T. ) ;
#12119=DIRECTION ( 'NONE',  ( -0.000000000000000000, -0.000000000000000000, -1.000000000000000000 ) ) ;
#12122=CARTESIAN_POINT ( 'NONE',  ( 1.868012774839550749, 39.13936707477651566, 93.38308880294498238 ) ) ;
#12123=CARTESIAN_POINT ( 'NONE',  ( 11.22215374030650281, 42.96218137147968008, 58.20715055817105110 ) ) ;
#12125=ADVANCED_FACE ( 'NONE', ( #6373 ), #12773, .F. ) ;
#12126=EDGE_CURVE ( 'NONE', #13051, #15145, #16417, .T. ) ;
#12128=VECTOR ( 'NONE', #18155, 1000.000000000000000 ) ;
#12133=CARTESIAN_POINT ( 'NONE',  ( 6.828503391016846891, 43.33193468930419101, 95.41433880123797451 ) ) ;
#12136=CARTESIAN_POINT ( 'NONE',  ( -0.4699484075730042676, 52.36218137147968577, 52.53721119516358584 ) ) ;
#12147=CARTESIAN_POINT ( 'NONE',  ( -3.943187491250720544, 40.73580453397070755, 90.64871380294496817 ) ) ;
#12151=CARTESIAN_POINT ( 'NONE',  ( 3.788215052820487205, 39.19523464621513398, 90.08681233796825438 ) ) ;
#12152=ORIENTED_EDGE ( 'NONE', *, *, #19002, .F. ) ;
#12157=CARTESIAN_POINT ( 'NONE',  ( -4.524181921268124462, 40.28999182795290324, 92.28933880123798872 ) ) ;
#12165=ORIENTED_EDGE ( 'NONE', *, *, #8390, .T. ) ;
#12168=ORIENTED_EDGE ( 'NONE', *, *, #16420, .F. ) ;
#12171=CARTESIAN_POINT ( 'NONE',  ( 11.22215374030649926, 42.76218137147968434, 80.55433879953099563 ) ) ;
#12173=CARTESIAN_POINT ( 'NONE',  ( -3.777846259693486974, 36.96218137147968008, 53.35433879953099989 ) ) ;
#12180=AXIS2_PLACEMENT_3D ( 'NONE', #9698, #14675, #12980 ) ;
#12183=CARTESIAN_POINT ( 'NONE',  ( 3.122153740306552905, 48.66551347115873227, 96.03933879953099506 ) ) ;
#12186=CARTESIAN_POINT ( 'NONE',  ( -3.350035803220276609, 49.20851703305431357, 92.13308880123798872 ) ) ;
#12192=CARTESIAN_POINT ( 'NONE',  ( -0.9988176903691428077, 49.83852402762217082, 93.30496380123798872 ) ) ;
#12197=VECTOR ( 'NONE', #11008, 1000.000000000000000 ) ;
#12208=CARTESIAN_POINT ( 'NONE',  ( 5.611423337425062385, 41.22389019960463230, 90.33621380123798872 ) ) ;
#12220=LINE ( 'NONE', #9141, #15072 ) ;
#12223=LINE ( 'NONE', #14514, #17654 ) ;
#12224=CARTESIAN_POINT ( 'NONE',  ( 5.722153871292735339, 42.76884579771262906, 94.83987682607160252 ) ) ;
#12226=CARTESIAN_POINT ( 'NONE',  ( 5.544968037009670780, 45.50804040601273925, 91.19558880294498238 ) ) ;
#12228=CARTESIAN_POINT ( 'NONE',  ( 2.263363662449358493, 49.77488197367694767, 94.44231768333818877 ) ) ;
#12236=CARTESIAN_POINT ( 'NONE',  ( 6.198496396448986090, 45.68315280215533392, 94.24246380123798872 ) ) ;
#12246=VECTOR ( 'NONE', #17820, 1000.000000000000000 ) ;
#12252=EDGE_CURVE ( 'NONE', #10416, #2282, #18442, .T. ) ;
#12257=CARTESIAN_POINT ( 'NONE',  ( 5.544968037009670780, 45.50804040601273925, 93.69558880294498238 ) ) ;
#12260=CARTESIAN_POINT ( 'NONE',  ( -5.784195910403845176, 44.99242805365518194, 90.88308880123798872 ) ) ;
#12266=VECTOR ( 'NONE', #20543, 1000.000000000000000 ) ;
#12268=CARTESIAN_POINT ( 'NONE',  ( -5.058133621542618030, 44.89684013992257405, 95.49246380294496817 ) ) ;
#12277=ORIENTED_EDGE ( 'NONE', *, *, #10030, .F. ) ;
#12281=ORIENTED_EDGE ( 'NONE', *, *, #1014, .F. ) ;
#12293=( BOUNDED_CURVE ( )  B_SPLINE_CURVE ( 2, ( #17636, #7653, #2762, #15531, #20615 ),
 .UNSPECIFIED., .F., .T. ) 
 B_SPLINE_CURVE_WITH_KNOTS ( ( 3, 2, 3 ),
 ( 0.5083811345117428271, 0.5250000000000000222, 0.5333811345117427383 ),
 .UNSPECIFIED. ) 
 CURVE ( )  GEOMETRIC_REPRESENTATION_ITEM ( )  RATIONAL_B_SPLINE_CURVE ( ( 0.9660722070828657859, 0.9493985675960727733, 1.000000000000000000, 0.9744809649152141873, 0.9660722070828660080 ) ) 
 REPRESENTATION_ITEM ( '' )  );
#12296=CARTESIAN_POINT ( 'NONE',  ( -0.2125050281363792815, 38.58189400963055959, 91.74246379953099506 ) ) ;
#12299=CARTESIAN_POINT ( 'NONE',  ( -0.9988176903691428077, 49.83852402762217082, 92.05496380123798872 ) ) ;
#12300=CARTESIAN_POINT ( 'NONE',  ( -0.3080929418689875576, 37.85583172076932357, 94.94558880123805977 ) ) ;
#12302=DIRECTION ( 'NONE',  ( -0.000000000000000000, -0.000000000000000000, 1.000000000000000000 ) ) ;
#12309=CARTESIAN_POINT ( 'NONE',  ( 10.77494014480653917, 42.76218137147968434, 58.20715055817105110 ) ) ;
#12315=DIRECTION ( 'NONE',  ( -0.000000000000000000, 2.168404344970984413E-15, -1.000000000000000000 ) ) ;
#12319=VECTOR ( 'NONE', #18282, 1000.000000000000000 ) ;
#12320=DIRECTION ( 'NONE',  ( -0.000000000000000000, -0.000000000000000000, 1.000000000000000000 ) ) ;
#12321=FACE_OUTER_BOUND ( 'NONE', #14766, .T. ) ;
#12322=CARTESIAN_POINT ( 'NONE',  ( -0.9988176903691428077, 49.83852402762217082, 90.80496380123797451 ) ) ;
#12325=DIRECTION ( 'NONE',  ( 0.000000000000000000, -2.168404344970984413E-15, -1.000000000000000000 ) ) ;
#12326=ORIENTED_EDGE ( 'NONE', *, *, #1693, .F. ) ;
#12339=CARTESIAN_POINT ( 'NONE',  ( -2.077846259693550746, 39.65884927180063357, 90.72683880294498238 ) ) ;
#12345=DIRECTION ( 'NONE',  ( -1.000000000000000000, 1.193617070626243484E-16, 0.000000000000000000 ) ) ;
#12347=CARTESIAN_POINT ( 'NONE',  ( 5.568489401881125289, 48.03437091500646261, 91.82058880123797451 ) ) ;
#12349=CARTESIAN_POINT ( 'NONE',  ( -0.3080929418689875576, 37.85583172076932357, 93.85183880123800293 ) ) ;
#12352=EDGE_CURVE ( 'NONE', #18958, #7336, #7437, .T. ) ;
#12360=LINE ( 'NONE', #18838, #608 ) ;
#12368=ORIENTED_EDGE ( 'NONE', *, *, #19872, .T. ) ;
#12372=LINE ( 'NONE', #20000, #16985 ) ;
#12373=CARTESIAN_POINT ( 'NONE',  ( 3.948530577815480225, 39.69684013992245752, 93.46121380294496817 ) ) ;
#12378=DIRECTION ( 'NONE',  ( 1.000000000000000000, -9.149887137874721638E-17, -0.000000000000000000 ) ) ;
#12384=ORIENTED_EDGE ( 'NONE', *, *, #14662, .F. ) ;
#12387=CARTESIAN_POINT ( 'NONE',  ( 13.32277635493562684, 36.96218137147968008, 80.55433879953099563 ) ) ;
#12388=LINE ( 'NONE', #17066, #12197 ) ;
#12398=CARTESIAN_POINT ( 'NONE',  ( 1.352400422481993658, 50.46853102219002096, 95.72683880123798872 ) ) ;
#12401=CARTESIAN_POINT ( 'NONE',  ( 5.568489401881125289, 48.03437091500646261, 95.57058880123798872 ) ) ;
#12403=ORIENTED_EDGE ( 'NONE', *, *, #7560, .F. ) ;
#12407=ORIENTED_EDGE ( 'NONE', *, *, #2758, .T. ) ;
#12409=CARTESIAN_POINT ( 'NONE',  ( 2.043125170982144745, 38.48583871533720213, 92.67996380123798872 ) ) ;
#12410=EDGE_LOOP ( 'NONE', ( #20807, #12441, #850, #11470 ) ) ;
#12412=CARTESIAN_POINT ( 'NONE',  ( 31.22215374030650281, 45.56218137147968861, 78.80433879953099563 ) ) ;
#12417=CARTESIAN_POINT ( 'NONE',  ( 30.92220646078100188, 45.56218137147968861, 62.80715055817104542 ) ) ;
#12423=CARTESIAN_POINT ( 'NONE',  ( -0.3080929418689875576, 37.85583172076933778, 92.60183880123797451 ) ) ;
#12426=CARTESIAN_POINT ( 'NONE',  ( 0.5221537403065020788, 52.36218137147968577, 52.53721119516358584 ) ) ;
#12432=CARTESIAN_POINT ( 'NONE',  ( -7.677846259693483333, 47.36218137147966445, 95.05433879953098142 ) ) ;
#12434=DIRECTION ( 'NONE',  ( 0.4999999999999977240, -0.8660254037844398178, 0.000000000000000000 ) ) ;
#12435=CARTESIAN_POINT ( 'NONE',  ( 6.198496396448986090, 45.68315280215533392, 92.99246380123798872 ) ) ;
#12438=EDGE_CURVE ( 'NONE', #1479, #14315, #1801, .T. ) ;
#12439=CARTESIAN_POINT ( 'NONE',  ( 5.544968037009670780, 45.50804040601273925, 94.94558880294498238 ) ) ;
#12441=ORIENTED_EDGE ( 'NONE', *, *, #6899, .T. ) ;
#12442=CARTESIAN_POINT ( 'NONE',  ( 5.544968037009670780, 45.50804040601273925, 94.94558880294498238 ) ) ;
#12445=CARTESIAN_POINT ( 'NONE',  ( 5.568489401881125289, 48.03437091500646261, 90.57058880123798872 ) ) ;
#12456=CARTESIAN_POINT ( 'NONE',  ( -5.945795452124602143, 37.96218137147967298, 53.35433879953099989 ) ) ;
#12464=EDGE_CURVE ( 'NONE', #11154, #3488, #185, .T. ) ;
#12468=CARTESIAN_POINT ( 'NONE',  ( -3.943187491250720544, 40.73580453397070755, 93.14871380294496817 ) ) ;
#12485=DIRECTION ( 'NONE',  ( -0.000000000000000000, -0.000000000000000000, 1.000000000000000000 ) ) ;
#12486=VECTOR ( 'NONE', #13430, 1000.000000000000000 ) ;
#12490=CARTESIAN_POINT ( 'NONE',  ( -0.8237052942265477018, 49.18499566818285018, 91.19558879953099506 ) ) ;
#12497=VECTOR ( 'NONE', #15657, 1000.000000000000000 ) ;
#12499=CARTESIAN_POINT ( 'NONE',  ( 1.445335398664440607, 38.34581663015914188, 95.05433879953095300 ) ) ;
#12502=CARTESIAN_POINT ( 'NONE',  ( -3.943187491250720544, 40.73580453397070755, 92.83621379953099506 ) ) ;
#12520=CARTESIAN_POINT ( 'NONE',  ( 6.198496396448986090, 45.68315280215533392, 95.33621380123798872 ) ) ;
#12525=ORIENTED_EDGE ( 'NONE', *, *, #11446, .T. ) ;
#12532=CARTESIAN_POINT ( 'NONE',  ( -7.677846259693483333, 47.36218137147966445, 80.55433879953099563 ) ) ;
#12535=CARTESIAN_POINT ( 'NONE',  ( 5.568489401881125289, 48.03437091500646261, 95.41433880123797451 ) ) ;
#12537=( BOUNDED_CURVE ( )  B_SPLINE_CURVE ( 2, ( #742, #2024, #8521, #2340, #19983, #15006, #7227, #2451, #5202, #15433, #428 ),
 .UNSPECIFIED., .F., .F. ) 
 B_SPLINE_CURVE_WITH_KNOTS ( ( 3, 2, 2, 2, 2, 3 ),
 ( 0.3472607999482700269, 0.3645715623395309746, 0.3906123882209271425, 0.4166532141023233660, 0.4426940399837194784, 0.4514241053481902743 ),
 .UNSPECIFIED. ) 
 CURVE ( )  GEOMETRIC_REPRESENTATION_ITEM ( )  RATIONAL_B_SPLINE_CURVE ( ( 0.9660722130358361248, 0.9493985585629908242, 1.000000000000000000, 0.9238795325112867385, 1.000000000000000000, 0.9238795325112867385, 1.000000000000000000, 0.9238795325112867385, 1.000000000000000000, 0.9744809684693873653, 0.9660722094251321668 ) ) 
 REPRESENTATION_ITEM ( '' )  );
#12538=CARTESIAN_POINT ( 'NONE',  ( 2.722153740306501479, 44.16218137147969003, 50.15433879953098995 ) ) ;
#12542=VECTOR ( 'NONE', #2054, 1000.000000000000000 ) ;
#12544=CARTESIAN_POINT ( 'NONE',  ( 5.722153675948534080, 44.84677459912131070, 94.92075777718328311 ) ) ;
#12570=CARTESIAN_POINT ( 'NONE',  ( -3.777846259693486974, 51.36218137147968577, 93.55433879953098142 ) ) ;
#12571=CARTESIAN_POINT ( 'NONE',  ( 6.102441102155617969, 43.42752260303680600, 93.61746380294498238 ) ) ;
#12572=ORIENTED_EDGE ( 'NONE', *, *, #19242, .T. ) ;
#12574=EDGE_CURVE ( 'NONE', #5140, #5376, #5072, .T. ) ;
#12575=CARTESIAN_POINT ( 'NONE',  ( -4.677846259693498432, 44.16218137147969003, 93.95661078214054385 ) ) ;
#12585=CARTESIAN_POINT ( 'NONE',  ( -5.154188915835984375, 42.64120994080404614, 93.46121380123797451 ) ) ;
#12587=VECTOR ( 'NONE', #13959, 1000.000000000000000 ) ;
#12588=CARTESIAN_POINT ( 'NONE',  ( -2.416137431568557314, 39.07291177436112406, 94.86746380123797451 ) ) ;
#12594=ADVANCED_FACE ( 'NONE', ( #18265 ), #11590, .F. ) ;
#12597=ORIENTED_EDGE ( 'NONE', *, *, #7622, .T. ) ;
#12599=CARTESIAN_POINT ( 'NONE',  ( 4.394343283833276992, 39.11584570990505938, 92.75808880123797451 ) ) ;
#12609=CARTESIAN_POINT ( 'NONE',  ( 3.948530577815479337, 39.69684013992245752, 93.14871379953099506 ) ) ;
#12619=ADVANCED_FACE ( 'NONE', ( #12321 ), #8803, .F. ) ;
#12621=EDGE_CURVE ( 'NONE', #18224, #3380, #15406, .T. ) ;
#12626=EDGE_CURVE ( 'NONE', #16572, #7590, #599, .T. ) ;
#12628=CARTESIAN_POINT ( 'NONE',  ( 4.454354847297358866, 39.79502961122975790, 90.27410626197791998 ) ) ;
#12629=CARTESIAN_POINT ( 'NONE',  ( 31.07218010054375412, 42.96218137147968008, 69.80574467885101342 ) ) ;
#12631=ORIENTED_EDGE ( 'NONE', *, *, #18724, .T. ) ;
#12642=ORIENTED_EDGE ( 'NONE', *, *, #4412, .F. ) ;
#12646=CARTESIAN_POINT ( 'NONE',  ( 3.460444912181559474, 49.25145096859824889, 91.89871380123798872 ) ) ;
#12647=DIRECTION ( 'NONE',  ( 0.000000000000000000, 0.000000000000000000, 1.000000000000000000 ) ) ;
#12649=VECTOR ( 'NONE', #7111, 1000.000000000000000 ) ;
#12656=CARTESIAN_POINT ( 'NONE',  ( 11.22215374030650281, 42.76218137147968434, 78.80433879953099563 ) ) ;
#12657=EDGE_CURVE ( 'NONE', #18041, #16139, #5497, .T. ) ;
#12670=CARTESIAN_POINT ( 'NONE',  ( 35.92215374030650565, 51.36218137147967866, 93.55433879953098142 ) ) ;
#12672=ORIENTED_EDGE ( 'NONE', *, *, #18192, .T. ) ;
#12679=CARTESIAN_POINT ( 'NONE',  ( -2.077846259693550746, 39.65884927180063357, 91.97683880294496817 ) ) ;
#12680=ORIENTED_EDGE ( 'NONE', *, *, #2166, .T. ) ;
#12683=CARTESIAN_POINT ( 'NONE',  ( -4.477846259693498254, 36.96218137147968008, 53.35433879953099989 ) ) ;
#12691=CARTESIAN_POINT ( 'NONE',  ( -0.9988176903691428077, 49.83852402762217082, 93.14871380123798872 ) ) ;
#12701=CARTESIAN_POINT ( 'NONE',  ( -2.416137431568557314, 39.07291177436112406, 93.77371380123797451 ) ) ;
#12703=ORIENTED_EDGE ( 'NONE', *, *, #3550, .F. ) ;
#12709=CARTESIAN_POINT ( 'NONE',  ( -0.4699484075729999932, 51.36218137147968577, 83.03825919817350609 ) ) ;
#12710=EDGE_LOOP ( 'NONE', ( #1802, #18478, #11699, #16034 ) ) ;
#12711=CARTESIAN_POINT ( 'NONE',  ( -4.225735884248155827, 46.53332982581555655, 92.55433879953098142 ) ) ;
#12712=CARTESIAN_POINT ( 'NONE',  ( 3.460444912181559474, 49.25145096859824889, 91.89871380123798872 ) ) ;
#12726=CARTESIAN_POINT ( 'NONE',  ( -7.677846259693485109, 51.36218137147968577, 95.05433879953098142 ) ) ;
#12731=VERTEX_POINT ( 'NONE', #18689 ) ;
#12733=VERTEX_POINT ( 'NONE', #4105 ) ;
#12742=ORIENTED_EDGE ( 'NONE', *, *, #12252, .F. ) ;
#12746=CARTESIAN_POINT ( 'NONE',  ( 5.611423337425062385, 41.22389019960463230, 92.83621380123797451 ) ) ;
#12747=EDGE_CURVE ( 'NONE', #5582, #18174, #1032, .T. ) ;
#12768=EDGE_CURVE ( 'NONE', #3115, #972, #4523, .T. ) ;
#12773=PLANE ( 'NONE',  #15688 ) ;
#12775=CARTESIAN_POINT ( 'NONE',  ( 23.29010293273768539, 19.08282756897896704, 45.55433879953098852 ) ) ;
#12776=CARTESIAN_POINT ( 'NONE',  ( 4.001626195812781006, 40.29782224849783745, 89.72723091094957226 ) ) ;
#12785=ORIENTED_EDGE ( 'NONE', *, *, #19352, .F. ) ;
#12788=FACE_OUTER_BOUND ( 'NONE', #17491, .T. ) ;
#12789=CARTESIAN_POINT ( 'NONE',  ( 31.22215374030650281, 42.76218137147968434, 78.80433879953099563 ) ) ;
#12793=CARTESIAN_POINT ( 'NONE',  ( 34.76745320192723199, 38.96218137147968719, 93.55433879953098142 ) ) ;
#12797=CARTESIAN_POINT ( 'NONE',  ( 6.828503391016846891, 43.33193468930419101, 94.16433880123797451 ) ) ;
#12799=VERTEX_POINT ( 'NONE', #19204 ) ;
#12806=ORIENTED_EDGE ( 'NONE', *, *, #14446, .F. ) ;
#12807=CARTESIAN_POINT ( 'NONE',  ( -4.630511887643872448, 41.91479704223051783, 92.55433879953096721 ) ) ;
#12808=CARTESIAN_POINT ( 'NONE',  ( 31.22215374030650281, 45.56218137147968861, 72.80433879953100984 ) ) ;
#12814=VECTOR ( 'NONE', #11514, 1000.000000000000114 ) ;
#12816=DIRECTION ( 'NONE',  ( 0.000000000000000000, -2.891205793294680792E-16, -1.000000000000000000 ) ) ;
#12822=ORIENTED_EDGE ( 'NONE', *, *, #16270, .F. ) ;
#12833=CARTESIAN_POINT ( 'NONE',  ( -5.058133621542618030, 44.89684013992257405, 93.92996379953099506 ) ) ;
#12840=ADVANCED_FACE ( 'NONE', ( #19414 ), #6747, .F. ) ;
#12845=CARTESIAN_POINT ( 'NONE',  ( -4.524181921268124462, 40.28999182795290324, 91.19558880123797451 ) ) ;
#12846=AXIS2_PLACEMENT_3D ( 'NONE', #15149, #12068, #15572 ) ;
#12847=( NAMED_UNIT ( * ) PLANE_ANGLE_UNIT ( ) SI_UNIT ( $, .RADIAN. ) );
#12848=CARTESIAN_POINT ( 'NONE',  ( 4.613683985508550300, 40.84891963687440608, 89.75946567728124137 ) ) ;
#12852=ORIENTED_EDGE ( 'NONE', *, *, #4123, .F. ) ;
#12857=VECTOR ( 'NONE', #10615, 1000.000000000000000 ) ;
#12858=VERTEX_POINT ( 'NONE', #19620 ) ;
#12859=ADVANCED_FACE ( 'NONE', ( #6852 ), #5146, .F. ) ;
#12862=CARTESIAN_POINT ( 'NONE',  ( -1.183761187420877548, 49.81017696809242068, 95.05433879953098142 ) ) ;
#12866=FACE_OUTER_BOUND ( 'NONE', #6549, .T. ) ;
#12870=AXIS2_PLACEMENT_3D ( 'NONE', #7595, #10905, #20652 ) ;
#12871=EDGE_LOOP ( 'NONE', ( #7519, #13211, #15303, #2241 ) ) ;
#12877=DIRECTION ( 'NONE',  ( -1.000000000000000000, -1.402518428993831676E-16, -0.000000000000000000 ) ) ;
#12886=DIRECTION ( 'NONE',  ( -0.4472135954999562069, 0.7745966692414842925, -0.4472135954999583718 ) ) ;
#12889=( GEOMETRIC_REPRESENTATION_CONTEXT ( 3 ) GLOBAL_UNCERTAINTY_ASSIGNED_CONTEXT ( ( #5318 ) ) GLOBAL_UNIT_ASSIGNED_CONTEXT ( ( #2326, #2440, #7542 ) ) REPRESENTATION_CONTEXT ( 'NONE', 'WORKASPACE' ) );
#12891=CARTESIAN_POINT ( 'NONE',  ( -0.9988176903691428077, 49.83852402762217082, 94.39871380123798872 ) ) ;
#12892=VECTOR ( 'NONE', #5049, 1000.000000000000000 ) ;
#12894=CARTESIAN_POINT ( 'NONE',  ( 3.460444912181559474, 49.25145096859824889, 91.74246380123798872 ) ) ;
#12908=CARTESIAN_POINT ( 'NONE',  ( -5.154188915835984375, 42.64120994080404614, 94.71121380123797451 ) ) ;
#12914=CARTESIAN_POINT ( 'NONE',  ( 2.580190882731753010, 49.45805475339454205, 93.29925044102854770 ) ) ;
#12917=CARTESIAN_POINT ( 'NONE',  ( -2.077846259693550746, 39.65884927180063357, 92.91433879953098085 ) ) ;
#12934=CARTESIAN_POINT ( 'NONE',  ( 6.722153740306509917, 44.16218137147969003, 111.0905869729573681 ) ) ;
#12939=ORIENTED_EDGE ( 'NONE', *, *, #6156, .F. ) ;
#12942=ORIENTED_EDGE ( 'NONE', *, *, #7658, .F. ) ;
#12960=AXIS2_PLACEMENT_3D ( 'NONE', #10635, #18801, #4214 ) ;
#12961=CARTESIAN_POINT ( 'NONE',  ( -0.4699484075729998822, 52.36218137147968577, 83.03825919817350609 ) ) ;
#12967=VERTEX_POINT ( 'NONE', #16342 ) ;
#12972=EDGE_CURVE ( 'NONE', #15788, #15424, #2760, .T. ) ;
#12978=VECTOR ( 'NONE', #7728, 1000.000000000000000 ) ;
#12980=DIRECTION ( 'NONE',  ( 0.000000000000000000, 2.891205793294680792E-16, 1.000000000000000000 ) ) ;
#12982=CARTESIAN_POINT ( 'NONE',  ( -0.9988176903691428077, 49.83852402762217082, 91.89871380123798872 ) ) ;
#12983=ORIENTED_EDGE ( 'NONE', *, *, #652, .F. ) ;
#12985=EDGE_LOOP ( 'NONE', ( #916, #5536, #17931, #20684 ) ) ;
#12986=ADVANCED_FACE ( 'NONE', ( #19828, #11456, #14632, #5249 ), #8358, .F. ) ;
#12998=EDGE_CURVE ( 'NONE', #9835, #19503, #16234, .T. ) ;
#13002=ADVANCED_FACE ( 'NONE', ( #1969 ), #588, .T. ) ;
#13003=ORIENTED_EDGE ( 'NONE', *, *, #17509, .T. ) ;
#13004=CARTESIAN_POINT ( 'NONE',  ( -0.8237052942265477018, 49.18499566818285018, 95.25808880294498238 ) ) ;
#13005=DIRECTION ( 'NONE',  ( -1.000000000000000000, -1.402518428993831676E-16, -1.196361017915039239E-16 ) ) ;
#13006=AXIS2_PLACEMENT_3D ( 'NONE', #8292, #194, #3496 ) ;
#13013=DIRECTION ( 'NONE',  ( -0.000000000000000000, -0.000000000000000000, 1.000000000000000000 ) ) ;
#13016=CARTESIAN_POINT ( 'NONE',  ( -5.784195910403845176, 44.99242805365518194, 92.28933880123798872 ) ) ;
#13017=CARTESIAN_POINT ( 'NONE',  ( 6.828503391016846891, 43.33193468930419101, 94.00808880123798872 ) ) ;
#13020=DIRECTION ( 'NONE',  ( -1.000000000000000000, -1.402518428993831676E-16, -0.000000000000000000 ) ) ;
#13021=AXIS2_PLACEMENT_3D ( 'NONE', #5877, #4364, #871 ) ;
#13022=CARTESIAN_POINT ( 'NONE',  ( 4.372497882239381184, 39.86211998552705893, 92.55433879953093879 ) ) ;
#13023=DIRECTION ( 'NONE',  ( 1.000000000000000000, -0.000000000000000000, -0.000000000000000000 ) ) ;
#13027=CARTESIAN_POINT ( 'NONE',  ( 0.5221537403065097394, 44.16218137147969003, 80.55433879953099563 ) ) ;
#13038=EDGE_CURVE ( 'NONE', #13701, #1661, #10658, .T. ) ;
#13042=PLANE ( 'NONE',  #11883 ) ;
#13049=CARTESIAN_POINT ( 'NONE',  ( 6.198496396448986090, 45.68315280215533392, 94.24246380123798872 ) ) ;
#13050=CARTESIAN_POINT ( 'NONE',  ( -3.777846259693487418, 51.36218137147968577, 54.55433879953099563 ) ) ;
#13051=VERTEX_POINT ( 'NONE', #18115 ) ;
#13052=DIRECTION ( 'NONE',  ( 0.7071067811865515695, 0.7071067811865434649, 0.000000000000000000 ) ) ;
#13054=CARTESIAN_POINT ( 'NONE',  ( -5.058133621542618030, 44.89684013992257405, 96.42996379953098085 ) ) ;
#13055=VERTEX_POINT ( 'NONE', #11639 ) ;
#13062=CARTESIAN_POINT ( 'NONE',  ( -1.174478664588463728, 57.66640723084523046, 80.55433879953099563 ) ) ;
#13063=CARTESIAN_POINT ( 'NONE',  ( 6.828503391016846891, 43.33193468930419101, 94.00808880123798872 ) ) ;
#13075=CARTESIAN_POINT ( 'NONE',  ( -1.219056181852248066, 49.77488197367201650, 94.56237966814981633 ) ) ;
#13078=EDGE_CURVE ( 'NONE', #17279, #10129, #15218, .T. ) ;
#13085=PLANE ( 'NONE',  #12180 ) ;
#13086=CARTESIAN_POINT ( 'NONE',  ( 5.722153740306476166, 44.16218185472587976, 94.89411094854372664 ) ) ;
#13087=CARTESIAN_POINT ( 'NONE',  ( 6.828503391016846891, 43.33193468930419101, 90.25808880123800293 ) ) ;
#13095=VERTEX_POINT ( 'NONE', #20091 ) ;
#13101=DIRECTION ( 'NONE',  ( -1.000000000000000000, -5.084437235940625660E-16, 0.000000000000000000 ) ) ;
#13107=CARTESIAN_POINT ( 'NONE',  ( -2.416137431568557314, 39.07291177436112406, 91.11746380123798872 ) ) ;
#13113=ORIENTED_EDGE ( 'NONE', *, *, #9485, .F. ) ;
#13116=CARTESIAN_POINT ( 'NONE',  ( 4.394343283833276992, 39.11584570990505938, 91.50808880123798872 ) ) ;
#13121=CARTESIAN_POINT ( 'NONE',  ( 4.135038682601217097, 47.90320695352507130, 92.55433879953098142 ) ) ;
#13124=VERTEX_POINT ( 'NONE', #16913 ) ;
#13125=FACE_OUTER_BOUND ( 'NONE', #434, .T. ) ;
#13127=ORIENTED_EDGE ( 'NONE', *, *, #15477, .F. ) ;
#13135=VECTOR ( 'NONE', #14646, 1000.000000000000114 ) ;
#13140=EDGE_CURVE ( 'NONE', #10043, #5117, #2657, .T. ) ;
#13142=ORIENTED_EDGE ( 'NONE', *, *, #5940, .T. ) ;
#13146=FACE_OUTER_BOUND ( 'NONE', #11053, .T. ) ;
#13150=ORIENTED_EDGE ( 'NONE', *, *, #7699, .T. ) ;
#13151=DIRECTION ( 'NONE',  ( 0.000000000000000000, 0.000000000000000000, 1.000000000000000000 ) ) ;
#13154=CARTESIAN_POINT ( 'NONE',  ( -3.981178359372548492, 46.76218137147973408, 96.35183879953099506 ) ) ;
#13159=VECTOR ( 'NONE', #10798, 1000.000000000000000 ) ;
#13163=CARTESIAN_POINT ( 'NONE',  ( -2.416137431568557314, 39.07291177436112406, 94.86746380123797451 ) ) ;
#13172=CARTESIAN_POINT ( 'NONE',  ( 28.52215374030649997, 44.16218137147968292, 87.05433879953099563 ) ) ;
#13178=CARTESIAN_POINT ( 'NONE',  ( -3.154801521863568325, 47.83913663364971569, 95.05036078214054385 ) ) ;
#13184=FACE_OUTER_BOUND ( 'NONE', #19390, .T. ) ;
#13186=CARTESIAN_POINT ( 'NONE',  ( -2.416137431568557314, 39.07291177436112406, 93.61746380123804556 ) ) ;
#13188=DIRECTION ( 'NONE',  ( -6.067057537060281311E-17, 0.4999999999999999445, -0.8660254037844387076 ) ) ;
#13191=CARTESIAN_POINT ( 'NONE',  ( 6.198496396448986090, 45.68315280215533392, 92.83621380123798872 ) ) ;
#13207=APPLICATION_CONTEXT ( 'automotive_design' ) ;
#13211=ORIENTED_EDGE ( 'NONE', *, *, #18363, .T. ) ;
#13212=CARTESIAN_POINT ( 'NONE',  ( -3.350035803220276609, 49.20851703305431357, 91.97683880123797451 ) ) ;
#13219=CARTESIAN_POINT ( 'NONE',  ( 10.77494014480653561, 42.96218137147968008, 66.20574467885104752 ) ) ;
#13220=AXIS2_PLACEMENT_3D ( 'NONE', #1423, #33, #11324 ) ;
#13225=CARTESIAN_POINT ( 'NONE',  ( -0.4699484075730042676, 52.36218137147968577, 48.36106904222365444 ) ) ;
#13231=EDGE_LOOP ( 'NONE', ( #9596, #18238, #15450, #12065, #8168, #10375 ) ) ;
#13236=VECTOR ( 'NONE', #497, 1000.000000000000000 ) ;
#13247=DIRECTION ( 'NONE',  ( -1.334402673828313339E-16, 1.592765810570777996E-32, 1.000000000000000000 ) ) ;
#13250=DIRECTION ( 'NONE',  ( 0.000000000000000000, 2.168404344970984413E-15, -1.000000000000000000 ) ) ;
#13252=CARTESIAN_POINT ( 'NONE',  ( 3.502103686363649881, 48.53614194976264429, 92.63161059727374891 ) ) ;
#13253=CARTESIAN_POINT ( 'NONE',  ( 5.544968037009670780, 45.50804040601273925, 93.38308879953099506 ) ) ;
#13254=AXIS2_PLACEMENT_3D ( 'NONE', #14438, #3268, #8057 ) ;
#13260=ADVANCED_FACE ( 'NONE', ( #14040 ), #20619, .F. ) ;
#13263=CARTESIAN_POINT ( 'NONE',  ( -2.077846259693550746, 39.65884927180063357, 95.41433879953098085 ) ) ;
#13276=EDGE_CURVE ( 'NONE', #20542, #11018, #8450, .T. ) ;
#13279=ORIENTED_EDGE ( 'NONE', *, *, #8621, .F. ) ;
#13283=DIRECTION ( 'NONE',  ( 1.000000000000000000, 0.000000000000000000, -0.000000000000000000 ) ) ;
#13287=DIRECTION ( 'NONE',  ( 0.000000000000000000, 0.000000000000000000, 1.000000000000000000 ) ) ;
#13292=CARTESIAN_POINT ( 'NONE',  ( 30.92220646078100188, 42.76218137147968434, 62.80715055817104542 ) ) ;
#13299=CARTESIAN_POINT ( 'NONE',  ( 1.352400422481993658, 50.46853102219002096, 90.57058880123798872 ) ) ;
#13300=CARTESIAN_POINT ( 'NONE',  ( -4.524181921268124462, 40.28999182795290324, 91.03933880123798872 ) ) ;
#13305=CARTESIAN_POINT ( 'NONE',  ( 31.22215374030650281, 42.76218137147968434, 78.80433879953099563 ) ) ;
#13307=VECTOR ( 'NONE', #8795, 1000.000000000000000 ) ;
#13322=CARTESIAN_POINT ( 'NONE',  ( 5.611423337425062385, 41.22389019960463230, 90.17996380123798872 ) ) ;
#13324=CARTESIAN_POINT ( 'NONE',  ( -4.524181921268124462, 40.28999182795290324, 91.19558880123797451 ) ) ;
#13327=VERTEX_POINT ( 'NONE', #8672 ) ;
#13332=CARTESIAN_POINT ( 'NONE',  ( 1.352400422481993658, 50.46853102219002096, 95.57058880123798872 ) ) ;
#13333=EDGE_LOOP ( 'NONE', ( #3623, #8176, #16190, #7115 ) ) ;
#13336=CARTESIAN_POINT ( 'NONE',  ( 6.020541483214493894, 43.49297395252375509, 92.55433879953095300 ) ) ;
#13353=CARTESIAN_POINT ( 'NONE',  ( 2.722153740306501479, 44.16218137147969003, 37.95170767603170248 ) ) ;
#13354=ORIENTED_EDGE ( 'NONE', *, *, #14148, .F. ) ;
#13355=AXIS2_PLACEMENT_3D ( 'NONE', #11720, #16602, #18292 ) ;
#13356=CARTESIAN_POINT ( 'NONE',  ( -7.677846259693481556, 40.96218137147969429, 80.55433879953099563 ) ) ;
#13359=CARTESIAN_POINT ( 'NONE',  ( 6.102441102155617969, 43.42752260303680600, 92.05496379953099506 ) ) ;
#13364=DIRECTION ( 'NONE',  ( -0.7071067811865434649, 0.7071067811865515695, 0.000000000000000000 ) ) ;
#13368=CARTESIAN_POINT ( 'NONE',  ( 5.611423337425062385, 41.22389019960463230, 94.08621380123797451 ) ) ;
#13374=EDGE_CURVE ( 'NONE', #7434, #19503, #19608, .T. ) ;
#13385=CARTESIAN_POINT ( 'NONE',  ( 2.043125170982144745, 38.48583871533720213, 93.92996380123798872 ) ) ;
#13388=ORIENTED_EDGE ( 'NONE', *, *, #13676, .F. ) ;
#13389=AXIS2_PLACEMENT_3D ( 'NONE', #4769, #15862, #1278 ) ;
#13395=ADVANCED_FACE ( 'NONE', ( #4278 ), #16955, .F. ) ;
#13400=PLANE ( 'NONE',  #19374 ) ;
#13401=CARTESIAN_POINT ( 'NONE',  ( 4.454347278305088587, 39.79502279609036464, 90.11785590924256439 ) ) ;
#13405=CARTESIAN_POINT ( 'NONE',  ( -3.226449543290886179, 47.76606447477297479, 92.55433879953076826 ) ) ;
#13408=CARTESIAN_POINT ( 'NONE',  ( -0.9988176903691428077, 49.83852402762217082, 93.30496380123798872 ) ) ;
#13413=EDGE_CURVE ( 'NONE', #4650, #10809, #4074, .T. ) ;
#13415=VERTEX_POINT ( 'NONE', #18552 ) ;
#13419=PLANE ( 'NONE',  #15389 ) ;
#13421=CARTESIAN_POINT ( 'NONE',  ( -4.812918938429301186, 42.57296343998554988, 95.05433879953095300 ) ) ;
#13424=CARTESIAN_POINT ( 'NONE',  ( 1.256812508749381774, 49.74246873332880625, 93.92996380294498238 ) ) ;
#13427=CARTESIAN_POINT ( 'NONE',  ( 6.828503391016846891, 43.33193468930419101, 90.41433880123798872 ) ) ;
#13430=DIRECTION ( 'NONE',  ( 1.000000000000000000, -0.000000000000000000, -0.000000000000000000 ) ) ;
#13433=CARTESIAN_POINT ( 'NONE',  ( 4.394343283833276992, 39.11584570990505938, 92.60183880123797451 ) ) ;
#13434=VERTEX_POINT ( 'NONE', #14172 ) ;
#13454=CARTESIAN_POINT ( 'NONE',  ( -5.058133621542618030, 44.89684013992257405, 93.92996379953099506 ) ) ;
#13455=CARTESIAN_POINT ( 'NONE',  ( 1.256812508749381774, 49.74246873332880625, 96.11746379953099506 ) ) ;
#13458=DIRECTION ( 'NONE',  ( -1.196361017915039239E-16, 0.000000000000000000, 1.000000000000000000 ) ) ;
#13460=ORIENTED_EDGE ( 'NONE', *, *, #7164, .F. ) ;
#13465=CARTESIAN_POINT ( 'NONE',  ( -0.9988176903691428077, 49.83852402762217082, 94.55496380123798872 ) ) ;
#13472=LINE ( 'NONE', #10194, #1106 ) ;
#13478=CARTESIAN_POINT ( 'NONE',  ( 3.460444912181559474, 49.25145096859824889, 95.64871380123798872 ) ) ;
#13487=CARTESIAN_POINT ( 'NONE',  ( 6.198496396448986090, 45.68315280215533392, 92.83621380123807398 ) ) ;
#13490=CARTESIAN_POINT ( 'NONE',  ( -4.524181921268124462, 40.28999182795290324, 96.19558880123798872 ) ) ;
#13492=CARTESIAN_POINT ( 'NONE',  ( -7.677846259693484221, 40.96218137147969429, 53.35433879953099989 ) ) ;
#13493=LINE ( 'NONE', #11605, #5098 ) ;
#13494=CARTESIAN_POINT ( 'NONE',  ( 6.828503391016846891, 43.33193468930419101, 90.25808880123800293 ) ) ;
#13502=CARTESIAN_POINT ( 'NONE',  ( 4.001624342216747010, 40.29782057951908314, 90.66473080991372058 ) ) ;
#13504=DIRECTION ( 'NONE',  ( 0.000000000000000000, -0.000000000000000000, 1.000000000000000000 ) ) ;
#13513=CARTESIAN_POINT ( 'NONE',  ( 0.5221537403065020788, 52.36218137147968577, 48.36106904222365444 ) ) ;
#13514=CARTESIAN_POINT ( 'NONE',  ( -4.756326795192973300, 45.27753124462999779, 95.05433879953100984 ) ) ;
#13516=CARTESIAN_POINT ( 'NONE',  ( -2.904223097202481174, 48.62752260303690122, 90.33621380294496817 ) ) ;
#13521=CARTESIAN_POINT ( 'NONE',  ( 4.394343283833276992, 39.11584570990505938, 95.10183880123797451 ) ) ;
#13525=CARTESIAN_POINT ( 'NONE',  ( -4.477846259693498254, 37.66218137147969713, 53.35433879953099989 ) ) ;
#13529=CARTESIAN_POINT ( 'NONE',  ( -0.3080929418689875576, 37.85583172076933778, 91.19558880123798872 ) ) ;
#13531=ORIENTED_EDGE ( 'NONE', *, *, #6800, .F. ) ;
#13554=CARTESIAN_POINT ( 'NONE',  ( 1.868012774839550749, 39.13936707477651566, 94.32058879953099506 ) ) ;
#13555=CARTESIAN_POINT ( 'NONE',  ( -2.904223097202481174, 48.62752260303690122, 95.02371379953099506 ) ) ;
#13557=CARTESIAN_POINT ( 'NONE',  ( 10.77494014480653561, 42.76218137147968434, 65.80574467885102763 ) ) ;
#13558=CARTESIAN_POINT ( 'NONE',  ( -3.416655825507938449, 49.09312776965069958, 94.48111517502780998 ) ) ;
#13560=LINE ( 'NONE', #5470, #12857 ) ;
#13565=CARTESIAN_POINT ( 'NONE',  ( 4.987494971863720927, 47.58855820898865829, 90.96121379953099506 ) ) ;
#13568=PLANE ( 'NONE',  #17659 ) ;
#13575=ORIENTED_EDGE ( 'NONE', *, *, #14976, .F. ) ;
#13576=VERTEX_POINT ( 'NONE', #10223 ) ;
#13578=VECTOR ( 'NONE', #17635, 1000.000000000000000 ) ;
#13582=CARTESIAN_POINT ( 'NONE',  ( -2.416137431568557314, 39.07291177436112406, 96.27371380123797451 ) ) ;
#13584=ORIENTED_EDGE ( 'NONE', *, *, #19498, .T. ) ;
#13588=LINE ( 'NONE', #10423, #11498 ) ;
#13597=VECTOR ( 'NONE', #6745, 1000.000000000000000 ) ;
#13600=FACE_OUTER_BOUND ( 'NONE', #8913, .T. ) ;
#13601=CARTESIAN_POINT ( 'NONE',  ( -2.077846259693550746, 39.65884927180063357, 95.72683880294496817 ) ) ;
#13602=AXIS2_PLACEMENT_3D ( 'NONE', #8941, #13504, #19208 ) ;
#13604=VERTEX_POINT ( 'NONE', #16903 ) ;
#13608=CARTESIAN_POINT ( 'NONE',  ( 2.722153740306497927, 51.36218137147969287, 54.55433879953099563 ) ) ;
#13610=CARTESIAN_POINT ( 'NONE',  ( 3.460444912181559474, 49.25145096859824889, 93.14871380123798872 ) ) ;
#13612=CARTESIAN_POINT ( 'NONE',  ( 30.92220646078100188, 42.76218137147968434, 62.80715055817104542 ) ) ;
#13620=DIRECTION ( 'NONE',  ( 0.000000000000000000, -1.000000000000000000, 0.000000000000000000 ) ) ;
#13621=LINE ( 'NONE', #7119, #19439 ) ;
#13623=CARTESIAN_POINT ( 'NONE',  ( -1.677846259693499542, 50.36218137147968577, 50.15433879953098995 ) ) ;
#13624=CARTESIAN_POINT ( 'NONE',  ( -4.615672533236396369, 45.70859455045284392, 95.05433879953100984 ) ) ;
#13626=CARTESIAN_POINT ( 'NONE',  ( -2.904223097202481174, 48.62752260303690122, 91.58621380294496817 ) ) ;
#13631=CARTESIAN_POINT ( 'NONE',  ( -3.350035803220276609, 49.20851703305431357, 90.88308880123797451 ) ) ;
#13633=ORIENTED_EDGE ( 'NONE', *, *, #14976, .T. ) ;
#13637=CIRCLE ( 'NONE', #10255, 4.200000000000001066 ) ;
#13640=CARTESIAN_POINT ( 'NONE',  ( 6.102441102155617969, 43.42752260303680600, 94.86746380294499659 ) ) ;
#13643=EDGE_CURVE ( 'NONE', #11174, #16680, #7323, .T. ) ;
#13645=EDGE_CURVE ( 'NONE', #10593, #10468, #15024, .T. ) ;
#13648=CARTESIAN_POINT ( 'NONE',  ( -5.368445182934975968, 51.36218137147968577, 45.55433879953098852 ) ) ;
#13651=ORIENTED_EDGE ( 'NONE', *, *, #11701, .T. ) ;
#13658=AXIS2_PLACEMENT_3D ( 'NONE', #1772, #6427, #4934 ) ;
#13661=VECTOR ( 'NONE', #8143, 1000.000000000000000 ) ;
#13664=DIRECTION ( 'NONE',  ( -1.000000000000000000, 0.000000000000000000, -0.000000000000000000 ) ) ;
#13666=CARTESIAN_POINT ( 'NONE',  ( 2.228068668033876154, 49.81017696809242778, 83.28180655319408743 ) ) ;
#13667=CARTESIAN_POINT ( 'NONE',  ( 3.948530577815480225, 39.69684013992245752, 91.89871379953099506 ) ) ;
#13668=CARTESIAN_POINT ( 'NONE',  ( -2.904223097202481174, 48.62752260303690122, 96.27371379953099506 ) ) ;
#13669=ORIENTED_EDGE ( 'NONE', *, *, #9915, .F. ) ;
#13670=CARTESIAN_POINT ( 'NONE',  ( 3.460444912181559474, 49.25145096859824889, 95.64871380123798872 ) ) ;
#13676=EDGE_CURVE ( 'NONE', #122, #6553, #2124, .T. ) ;
#13680=CARTESIAN_POINT ( 'NONE',  ( -5.154188915835984375, 42.64120994080404614, 93.61746380123797451 ) ) ;
#13682=DIRECTION ( 'NONE',  ( 1.000000000000000000, 0.000000000000000000, 0.000000000000000000 ) ) ;
#13684=CARTESIAN_POINT ( 'NONE',  ( 5.611423337425062385, 41.22389019960463230, 90.17996380123798872 ) ) ;
#13697=FACE_OUTER_BOUND ( 'NONE', #6128, .T. ) ;
#13701=VERTEX_POINT ( 'NONE', #12228 ) ;
#13708=CARTESIAN_POINT ( 'NONE',  ( 4.394343283833276992, 39.11584570990505938, 95.25808880123800293 ) ) ;
#13712=CARTESIAN_POINT ( 'NONE',  ( -3.943187491250720544, 40.73580453397070755, 91.89871380294498238 ) ) ;
#13720=CARTESIAN_POINT ( 'NONE',  ( -2.416137431568557314, 39.07291177436112406, 96.27371380123797451 ) ) ;
#13726=ORIENTED_EDGE ( 'NONE', *, *, #18570, .F. ) ;
#13727=EDGE_LOOP ( 'NONE', ( #19973, #15239, #3472, #6332, #2569 ) ) ;
#13730=LINE ( 'NONE', #15654, #17747 ) ;
#13731=CARTESIAN_POINT ( 'NONE',  ( -3.416655834670953684, 49.09312775377990334, 94.63736517561592620 ) ) ;
#13734=CARTESIAN_POINT ( 'NONE',  ( -3.943187491250720544, 40.73580453397070755, 93.14871380294496817 ) ) ;
#13738=CARTESIAN_POINT ( 'NONE',  ( -0.3080929418689875576, 37.85583172076933778, 91.19558880123798872 ) ) ;
#13740=CARTESIAN_POINT ( 'NONE',  ( 30.92220646078100188, 42.96218137147968008, 58.20715055817105110 ) ) ;
#13744=CARTESIAN_POINT ( 'NONE',  ( -7.677846259693480668, 36.96218137147968008, 45.55433879953098852 ) ) ;
#13745=CARTESIAN_POINT ( 'NONE',  ( 5.568489401881125289, 48.03437091500646261, 90.41433880123798872 ) ) ;
#13746=EDGE_LOOP ( 'NONE', ( #5570, #1458, #12680, #2995 ) ) ;
#13751=PLANE ( 'NONE',  #16917 ) ;
#13754=ORIENTED_EDGE ( 'NONE', *, *, #10160, .F. ) ;
#13759=DIRECTION ( 'NONE',  ( 1.000000000000000000, -0.000000000000000000, -0.000000000000000000 ) ) ;
#13770=CARTESIAN_POINT ( 'NONE',  ( 5.025485839985549319, 41.56218137147963887, 95.72683879953099506 ) ) ;
#13771=ORIENTED_EDGE ( 'NONE', *, *, #3745, .F. ) ;
#13772=CARTESIAN_POINT ( 'NONE',  ( 5.611423337425062385, 41.22389019960463230, 92.83621380123797451 ) ) ;
#13774=LINE ( 'NONE', #2284, #6870 ) ;
#13777=ORIENTED_EDGE ( 'NONE', *, *, #10529, .F. ) ;
#13779=CARTESIAN_POINT ( 'NONE',  ( -4.567115856812060670, 47.10047254335474065, 93.46121380123797451 ) ) ;
#13782=DIRECTION ( 'NONE',  ( 0.000000000000000000, -2.891205793294680792E-16, -1.000000000000000000 ) ) ;
#13783=PRODUCT_CONTEXT ( 'NONE', #13207, 'mechanical' ) ;
#13791=ORIENTED_EDGE ( 'NONE', *, *, #3004, .F. ) ;
#13795=CARTESIAN_POINT ( 'NONE',  ( 6.198496396448986090, 45.68315280215533392, 91.74246380123798872 ) ) ;
#13804=DIRECTION ( 'NONE',  ( -0.000000000000000000, -0.000000000000000000, -1.000000000000000000 ) ) ;
#13806=CARTESIAN_POINT ( 'NONE',  ( 31.07218010054375412, 45.56218137147968861, 64.80574467885102763 ) ) ;
#13811=CARTESIAN_POINT ( 'NONE',  ( 4.987494971863720927, 47.58855820898865829, 91.27371380294496817 ) ) ;
#13812=CARTESIAN_POINT ( 'NONE',  ( 5.722153740306500147, 44.16218137147969003, 77.84651775085080772 ) ) ;
#13813=ORIENTED_EDGE ( 'NONE', *, *, #14769, .T. ) ;
#13821=CARTESIAN_POINT ( 'NONE',  ( 4.394343283833276992, 39.11584570990505938, 95.25808880123800293 ) ) ;
#13822=DIRECTION ( 'NONE',  ( -1.334402673828310381E-16, -2.168404344970984413E-15, 1.000000000000000000 ) ) ;
#13828=PRODUCT_DEFINITION_CONTEXT ( 'detailed design', #14284, 'design' ) ;
#13831=CARTESIAN_POINT ( 'NONE',  ( 30.92220646078100188, 45.56218137147968861, 56.80715055817104542 ) ) ;
#13832=CARTESIAN_POINT ( 'NONE',  ( 10.77494014480653917, 42.96218137147968008, 61.40715055817103263 ) ) ;
#13833=CARTESIAN_POINT ( 'NONE',  ( -3.582310441719081417, 40.15725564764044009, 95.05433879953096721 ) ) ;
#13835=CARTESIAN_POINT ( 'NONE',  ( 5.025485839985549319, 41.56218137147963887, 89.78933880294498238 ) ) ;
#13845=CARTESIAN_POINT ( 'NONE',  ( 6.198496396448986090, 45.68315280215533392, 91.58621380123798872 ) ) ;
#13848=LINE ( 'NONE', #10475, #19650 ) ;
#13850=LINE ( 'NONE', #19631, #5005 ) ;
#13859=DIRECTION ( 'NONE',  ( 1.334402673828313339E-16, 1.871524341742854397E-32, -1.000000000000000000 ) ) ;
#13869=ORIENTED_EDGE ( 'NONE', *, *, #16018, .F. ) ;
#13871=CARTESIAN_POINT ( 'NONE',  ( 5.025485839985549319, 41.56218137147963887, 91.97683879953100927 ) ) ;
#13874=CARTESIAN_POINT ( 'NONE',  ( -4.524181921268124462, 40.28999182795290324, 92.44558880123798872 ) ) ;
#13876=CARTESIAN_POINT ( 'NONE',  ( -4.567115856812060670, 47.10047254335474065, 94.55496380123807398 ) ) ;
#13888=VECTOR ( 'NONE', #10707, 1000.000000000000000 ) ;
#13892=EDGE_CURVE ( 'NONE', #8376, #9419, #4445, .T. ) ;
#13895=EDGE_CURVE ( 'NONE', #14061, #12858, #9358, .T. ) ;
#13899=CARTESIAN_POINT ( 'NONE',  ( -5.784195910403845176, 44.99242805365518194, 91.03933880123798872 ) ) ;
#13914=CARTESIAN_POINT ( 'NONE',  ( 3.178197289651383262, 41.22014870947117515, 98.25514354869233102 ) ) ;
#13915=CARTESIAN_POINT ( 'NONE',  ( 1.352400422481993658, 50.46853102219002096, 95.72683880123798872 ) ) ;
#13917=VECTOR ( 'NONE', #12816, 1000.000000000000000 ) ;
#13921=CARTESIAN_POINT ( 'NONE',  ( 4.987494971863720927, 47.58855820898865829, 95.02371380294496817 ) ) ;
#13926=VECTOR ( 'NONE', #9299, 1000.000000000000000 ) ;
#13930=CARTESIAN_POINT ( 'NONE',  ( 31.22215374030650281, 42.96218137147968008, 77.40433879953098995 ) ) ;
#13931=CARTESIAN_POINT ( 'NONE',  ( 11.22215374030650281, 45.56218137147968150, 72.80433879953100984 ) ) ;
#13940=LINE ( 'NONE', #8949, #15546 ) ;
#13948=CARTESIAN_POINT ( 'NONE',  ( 3.122153740306552905, 48.66551347115873227, 90.10183880294498238 ) ) ;
#13949=EDGE_CURVE ( 'NONE', #11635, #3380, #4642, .T. ) ;
#13953=CARTESIAN_POINT ( 'NONE',  ( 5.146043734657006041, 40.41782908280415398, 90.15009084312077903 ) ) ;
#13957=CARTESIAN_POINT ( 'NONE',  ( 0.5221537403065010796, 44.16218137147969003, 77.84651775085080772 ) ) ;
#13959=DIRECTION ( 'NONE',  ( 0.000000000000000000, 0.000000000000000000, -1.000000000000000000 ) ) ;
#13960=CARTESIAN_POINT ( 'NONE',  ( -3.981178359372548492, 46.76218137147973408, 90.41433880294496817 ) ) ;
#13961=ORIENTED_EDGE ( 'NONE', *, *, #6776, .F. ) ;
#13974=CARTESIAN_POINT ( 'NONE',  ( 30.92220646078100188, 42.76218137147968434, 61.40715055817103263 ) ) ;
#13975=FACE_OUTER_BOUND ( 'NONE', #19000, .T. ) ;
#13981=VECTOR ( 'NONE', #623, 1000.000000000000000 ) ;
#13984=CARTESIAN_POINT ( 'NONE',  ( 1.256812508749381774, 49.74246873332880625, 91.11746379953096664 ) ) ;
#13987=CARTESIAN_POINT ( 'NONE',  ( 5.611423337425062385, 41.22389019960463230, 91.58621380123798872 ) ) ;
#13994=CARTESIAN_POINT ( 'NONE',  ( -4.567115856812060670, 47.10047254335474065, 92.21121380123797451 ) ) ;
#14003=CARTESIAN_POINT ( 'NONE',  ( 31.22215374030650281, 42.96218137147968008, 77.40433879953098995 ) ) ;
#14007=EDGE_LOOP ( 'NONE', ( #20272, #11398, #20237, #14070 ) ) ;
#14011=CARTESIAN_POINT ( 'NONE',  ( 4.394343283833276992, 39.11584570990505938, 95.10183880123797451 ) ) ;
#14012=CIRCLE ( 'NONE', #2458, 4.199999999999999289 ) ;
#14015=EDGE_LOOP ( 'NONE', ( #13127, #17875, #14405, #8946 ) ) ;
#14017=CARTESIAN_POINT ( 'NONE',  ( 31.07218010054375412, 42.96218137147968008, 66.20574467885104752 ) ) ;
#14024=CARTESIAN_POINT ( 'NONE',  ( -2.416137431568557314, 39.07291177436112406, 91.27371380123798872 ) ) ;
#14025=PLANE ( 'NONE',  #17922 ) ;
#14026=( BOUNDED_CURVE ( )  B_SPLINE_CURVE ( 2, ( #15425, #2443, #12442, #12544, #5622 ),
 .UNSPECIFIED., .F., .F. ) 
 B_SPLINE_CURVE_WITH_KNOTS ( ( 3, 2, 3 ),
 ( 0.1128933701044576160, 0.1302041294069655186, 0.1389341928972610829 ),
 .UNSPECIFIED. ) 
 CURVE ( )  GEOMETRIC_REPRESENTATION_ITEM ( )  RATIONAL_B_SPLINE_CURVE ( ( 0.9660722070856899713, 0.9493985675917875344, 1.000000000000000000, 0.9744809739478270671, 0.9660722130355270387 ) ) 
 REPRESENTATION_ITEM ( '' )  );
#14027=CARTESIAN_POINT ( 'NONE',  ( -4.567115856812060670, 47.10047254335474065, 92.05496380123798872 ) ) ;
#14030=CARTESIAN_POINT ( 'NONE',  ( -2.904223097202481174, 48.62752260303690122, 90.33621380294496817 ) ) ;
#14035=LINE ( 'NONE', #12656, #8908 ) ;
#14038=CIRCLE ( 'NONE', #2501, 6.200000000000000178 ) ;
#14040=FACE_OUTER_BOUND ( 'NONE', #9828, .T. ) ;
#14044=LINE ( 'NONE', #17029, #5855 ) ;
#14048=PLANE ( 'NONE',  #15569 ) ;
#14049=CARTESIAN_POINT ( 'NONE',  ( 10.77494014480653561, 42.76218137147968434, 77.80433879953099563 ) ) ;
#14050=AXIS2_PLACEMENT_3D ( 'NONE', #3082, #17345, #9583 ) ;
#14051=CARTESIAN_POINT ( 'NONE',  ( 1.352400422481993658, 50.46853102219002096, 91.82058880123801714 ) ) ;
#14054=ORIENTED_EDGE ( 'NONE', *, *, #14734, .F. ) ;
#14060=CARTESIAN_POINT ( 'NONE',  ( -4.500660556396669065, 42.81632233694663370, 93.07058880294496817 ) ) ;
#14061=VERTEX_POINT ( 'NONE', #15076 ) ;
#14066=FACE_OUTER_BOUND ( 'NONE', #5603, .T. ) ;
#14070=ORIENTED_EDGE ( 'NONE', *, *, #7699, .F. ) ;
#14076=FACE_OUTER_BOUND ( 'NONE', #15291, .T. ) ;
#14086=CARTESIAN_POINT ( 'NONE',  ( 5.611423337425062385, 41.22389019960463230, 92.83621380123797451 ) ) ;
#14093=CARTESIAN_POINT ( 'NONE',  ( 0.2965220188279399371, 38.27753855637592295, 95.05433879953093879 ) ) ;
#14099=CARTESIAN_POINT ( 'NONE',  ( 4.134898411747151670, 47.90306806511021875, 95.05422504033560926 ) ) ;
#14107=ORIENTED_EDGE ( 'NONE', *, *, #8841, .F. ) ;
#14110=CARTESIAN_POINT ( 'NONE',  ( 5.568489401881125289, 48.03437091500646261, 95.41433880123797451 ) ) ;
#14115=CYLINDRICAL_SURFACE ( 'NONE', #20487, 0.9921021478795063464 ) ;
#14116=ORIENTED_EDGE ( 'NONE', *, *, #7260, .F. ) ;
#14124=CARTESIAN_POINT ( 'NONE',  ( 6.198496396448986090, 45.68315280215533392, 90.49246380123798872 ) ) ;
#14125=CARTESIAN_POINT ( 'NONE',  ( -5.368445182934975968, 51.36218137147968577, 93.55433879953098142 ) ) ;
#14127=CARTESIAN_POINT ( 'NONE',  ( -0.8237052942265477018, 49.18499566818285018, 94.00808880294498238 ) ) ;
#14131=CARTESIAN_POINT ( 'NONE',  ( -3.638881865703802454, 47.35505628976665804, 92.88950776816830057 ) ) ;
#14135=CARTESIAN_POINT ( 'NONE',  ( 4.394343283833276992, 39.11584570990505938, 91.50808880123798872 ) ) ;
#14144=CARTESIAN_POINT ( 'NONE',  ( 11.22215374030649926, 45.56218137147968150, 64.80574467885102763 ) ) ;
#14147=CARTESIAN_POINT ( 'NONE',  ( -4.524181921268124462, 40.28999182795290324, 92.28933880123798872 ) ) ;
#14148=EDGE_CURVE ( 'NONE', #16344, #8675, #13472, .T. ) ;
#14150=DIRECTION ( 'NONE',  ( 0.000000000000000000, 0.000000000000000000, -1.000000000000000000 ) ) ;
#14154=CARTESIAN_POINT ( 'NONE',  ( -2.077846259693550746, 39.65884927180063357, 93.22683880294496817 ) ) ;
#14157=CARTESIAN_POINT ( 'NONE',  ( -4.677846259693816400, 43.47758838402643988, 93.98325776475002158 ) ) ;
#14160=LINE ( 'NONE', #20643, #17210 ) ;
#14162=DIRECTION ( 'NONE',  ( 1.000000000000000000, 0.000000000000000000, 0.000000000000000000 ) ) ;
#14163=ORIENTED_EDGE ( 'NONE', *, *, #9013, .F. ) ;
#14168=CARTESIAN_POINT ( 'NONE',  ( 35.92215374030650565, 40.96218137147972982, 93.55433879953098142 ) ) ;
#14169=CARTESIAN_POINT ( 'NONE',  ( 10.77494014480653561, 42.96218137147968008, 73.80433879953100984 ) ) ;
#14170=CARTESIAN_POINT ( 'NONE',  ( -12.18117835937254867, 39.56218137147966019, 53.35433879953099989 ) ) ;
#14172=CARTESIAN_POINT ( 'NONE',  ( 34.76745320192721778, 49.36218137147971419, 93.55433879953098142 ) ) ;
#14178=EDGE_CURVE ( 'NONE', #10420, #6493, #9228, .T. ) ;
#14179=EDGE_LOOP ( 'NONE', ( #975, #20453, #18165, #776, #18635, #16547 ) ) ;
#14180=DIRECTION ( 'NONE',  ( 0.000000000000000000, 0.000000000000000000, -1.000000000000000000 ) ) ;
#14181=CARTESIAN_POINT ( 'NONE',  ( 3.122153740306552905, 48.66551347115873227, 91.03933879953099506 ) ) ;
#14185=CARTESIAN_POINT ( 'NONE',  ( -4.677846259693498432, 44.16218137147969003, 93.95661078214054385 ) ) ;
#14192=CARTESIAN_POINT ( 'NONE',  ( -5.154188915835984375, 42.64120994080404614, 91.11746380123797451 ) ) ;
#14196=CARTESIAN_POINT ( 'NONE',  ( 5.519652126588233898, 41.52382328956674939, 95.05433879953105247 ) ) ;
#14197=EDGE_CURVE ( 'NONE', #13055, #18958, #7623, .T. ) ;
#14205=ORIENTED_EDGE ( 'NONE', *, *, #8317, .F. ) ;
#14208=ORIENTED_EDGE ( 'NONE', *, *, #4061, .T. ) ;
#14211=CARTESIAN_POINT ( 'NONE',  ( 2.043125170982144745, 38.48583871533720213, 91.42996380123798872 ) ) ;
#14213=ORIENTED_EDGE ( 'NONE', *, *, #13276, .T. ) ;
#14214=ORIENTED_EDGE ( 'NONE', *, *, #9504, .T. ) ;
#14221=CARTESIAN_POINT ( 'NONE',  ( 29.52548583998564524, 58.44153517398036257, 45.55433879953098852 ) ) ;
#14227=CARTESIAN_POINT ( 'NONE',  ( -5.154188915835984375, 42.64120994080404614, 93.61746380123797451 ) ) ;
#14231=AXIS2_PLACEMENT_3D ( 'NONE', #2793, #10791, #18954 ) ;
#14233=LINE ( 'NONE', #18922, #3044 ) ;
#14234=FACE_OUTER_BOUND ( 'NONE', #18514, .T. ) ;
#14236=CARTESIAN_POINT ( 'NONE',  ( 2.043125170982144745, 38.48583871533720213, 91.42996380123798872 ) ) ;
#14244=CARTESIAN_POINT ( 'NONE',  ( -0.8237052942265477018, 49.18499566818285018, 91.19558879953099506 ) ) ;
#14245=CARTESIAN_POINT ( 'NONE',  ( 2.228068668033876154, 49.81017696809242778, 95.05433879953098142 ) ) ;
#14248=FACE_OUTER_BOUND ( 'NONE', #19801, .T. ) ;
#14253=EDGE_CURVE ( 'NONE', #895, #7921, #2619, .T. ) ;
#14259=CARTESIAN_POINT ( 'NONE',  ( 1.256812508749381774, 49.74246873332880625, 91.42996380294499659 ) ) ;
#14265=DIRECTION ( 'NONE',  ( -1.000000000000000000, -1.213411507412056509E-16, 0.000000000000000000 ) ) ;
#14270=ADVANCED_FACE ( 'NONE', ( #17098 ), #20680, .F. ) ;
#14272=CARTESIAN_POINT ( 'NONE',  ( 5.568489401881125289, 48.03437091500646261, 94.16433880123797451 ) ) ;
#14279=EDGE_CURVE ( 'NONE', #15007, #7833, #4516, .T. ) ;
#14284=APPLICATION_CONTEXT ( 'automotive_design' ) ;
#14289=CARTESIAN_POINT ( 'NONE',  ( -0.9988176903691428077, 49.83852402762217082, 95.80496380123798872 ) ) ;
#14296=CARTESIAN_POINT ( 'NONE',  ( 2.916646314871006229, 38.79555996194933698, 95.05433879953095300 ) ) ;
#14299=ORIENTED_EDGE ( 'NONE', *, *, #14926, .F. ) ;
#14301=CARTESIAN_POINT ( 'NONE',  ( 4.454345183533989783, 39.79502090995749342, 90.27410581162071423 ) ) ;
#14310=CARTESIAN_POINT ( 'NONE',  ( 31.07218010054375412, 45.56218137147968861, 70.80574467885102763 ) ) ;
#14315=VERTEX_POINT ( 'NONE', #20884 ) ;
#14316=DIRECTION ( 'NONE',  ( 2.838338907332122006E-16, -1.000000000000000000, 0.000000000000000000 ) ) ;
#14324=VECTOR ( 'NONE', #15183, 1000.000000000000114 ) ;
#14333=PLANE ( 'NONE',  #2034 ) ;
#14341=CARTESIAN_POINT ( 'NONE',  ( 2.043125170982144745, 38.48583871533720213, 91.42996380123798872 ) ) ;
#14349=DIRECTION ( 'NONE',  ( 0.7071067811865517916, 0.7071067811865433539, -0.000000000000000000 ) ) ;
#14354=EDGE_CURVE ( 'NONE', #16139, #19569, #6678, .T. ) ;
#14364=LINE ( 'NONE', #12456, #15917 ) ;
#14366=CIRCLE ( 'NONE', #13355, 6.200000000000000178 ) ;
#14372=CARTESIAN_POINT ( 'NONE',  ( -3.943187491250720544, 40.73580453397070755, 90.64871380294496817 ) ) ;
#14384=ADVANCED_FACE ( 'NONE', ( #295 ), #1811, .F. ) ;
#14392=ADVANCED_FACE ( 'NONE', ( #13184 ), #10006, .F. ) ;
#14396=EDGE_CURVE ( 'NONE', #4661, #16560, #18179, .T. ) ;
#14397=CARTESIAN_POINT ( 'NONE',  ( -3.350035803220276609, 49.20851703305431357, 95.88308880123798872 ) ) ;
#14399=EDGE_LOOP ( 'NONE', ( #14678, #12281, #8966, #13142 ) ) ;
#14405=ORIENTED_EDGE ( 'NONE', *, *, #10529, .T. ) ;
#14416=ORIENTED_EDGE ( 'NONE', *, *, #15463, .F. ) ;
#14417=CARTESIAN_POINT ( 'NONE',  ( 31.07218010054375412, 45.56218137147968861, 70.80574467885102763 ) ) ;
#14426=CARTESIAN_POINT ( 'NONE',  ( 5.568489401881125289, 48.03437091500647682, 94.32058880123798872 ) ) ;
#14430=CARTESIAN_POINT ( 'NONE',  ( -2.904223097202481174, 48.62752260303690122, 95.02371379953099506 ) ) ;
#14438=CARTESIAN_POINT ( 'NONE',  ( 10.77494014480653561, 42.96218137147968008, 74.20433879953100131 ) ) ;
#14439=CARTESIAN_POINT ( 'NONE',  ( -5.784195910403845176, 44.99242805365518194, 92.28933880123798872 ) ) ;
#14440=EDGE_CURVE ( 'NONE', #57, #18234, #10448, .T. ) ;
#14446=EDGE_CURVE ( 'NONE', #7497, #12733, #14366, .T. ) ;
#14447=CARTESIAN_POINT ( 'NONE',  ( 26.27839330960314257, 24.25869832947912030, 85.06527890720686003 ) ) ;
#14456=( BOUNDED_SURFACE ( )  B_SPLINE_SURFACE ( 1, 2, ( 
 ( #1556, #12079, #3662, #16452, #11667, #13668, #16861, #13455, #18241, #8359, #3563, #572, #11979, #1871, #18559, #8572, #10283, #14944, #18455, #11766, #2180, #13555, #2076, #14840, #7168, #3870, #19927, #10392, #15059, #19829, #6853, #9970, #689, #10173, #7055, #5250, #8463, #16655, #259, #6748, #20033, #3764, #13253, #15160, #18144, #19729, #15269, #10068, #472, #6950, #5147, #5355, #16550, #20143, #2280, #11868, #8779, #18345, #16760, #13359, #1970, #5575, #8680, #5465, #366, #10498, #16962, #3972, #2392, #8893, #15381, #15003, #8830, #11814, #8518, #8939, #18290, #3821, #13502 ),
 ( #13720, #3922, #10446, #5729, #626, #10341, #16813, #20194, #15327, #5626, #19880, #12133, #2230, #13821, #8725, #18401, #422, #2447, #7330, #15214, #16908, #16708, #20087, #7107, #737, #3708, #12236, #6907, #519, #3608, #7220, #16599, #10230, #18610, #5524, #20299, #10117, #2335, #13408, #4024, #13610, #10550, #12035, #18509, #17017, #2131, #2020, #15428, #5404, #7001, #15113, #8633, #19978, #844, #11925, #5300, #4553, #12347, #9155, #7655, #18828, #14135, #14236, #10866, #17337, #9469, #6046, #11070, #1063, #2864, #17539, #19142, #15533, #12445, #20617, #10761, #2962, #4235, #4133 ) ),
 .UNSPECIFIED., .F., .F., .F. ) 
 B_SPLINE_SURFACE_WITH_KNOTS ( ( 2, 2 ),
 ( 3, 2, 2, 2, 2, 2, 2, 2, 2, 2, 2, 2, 2, 2, 2, 2, 2, 2, 2, 2, 2, 2, 2, 2, 2, 2, 2, 2, 2, 2, 2, 2, 2, 2, 2, 2, 2, 2, 2, 3 ),
 ( 0.000000000000000000, 1.000000000000000000 ),
 ( 0.000000000000000000, 0.02500000000000000139, 0.05000000000000000278, 0.07499999999999999722, 0.1000000000000000056, 0.1250000000000000000, 0.1499999999999999944, 0.1749999999999999889, 0.2000000000000000111, 0.2250000000000000056, 0.2500000000000000000, 0.2750000000000000222, 0.2999999999999999889, 0.3250000000000000111, 0.3499999999999999778, 0.3750000000000000000, 0.4000000000000000222, 0.4249999999999999889, 0.4500000000000000111, 0.4749999999999999778, 0.5000000000000000000, 0.5250000000000000222, 0.5500000000000000444, 0.5749999999999999556, 0.5999999999999999778, 0.6250000000000000000, 0.6500000000000000222, 0.6750000000000000444, 0.6999999999999999556, 0.7249999999999999778, 0.7500000000000000000, 0.7750000000000000222, 0.8000000000000000444, 0.8249999999999999556, 0.8499999999999999778, 0.8750000000000000000, 0.9000000000000000222, 0.9250000000000000444, 0.9499999999999999556, 0.9600310108036838042 ),
 .UNSPECIFIED. ) 
 GEOMETRIC_REPRESENTATION_ITEM ( )  RATIONAL_B_SPLINE_SURFACE ( (
 ( 1.000000000000000000, 0.9238795325112867385, 1.000000000000000000, 0.9238795325112867385, 1.000000000000000000, 0.9238795325112867385, 1.000000000000000000, 0.9238795325112867385, 1.000000000000000000, 0.9238795325112867385, 1.000000000000000000, 0.9238795325112867385, 1.000000000000000000, 0.9238795325112867385, 1.000000000000000000, 0.9238795325112867385, 1.000000000000000000, 0.9238795325112867385, 1.000000000000000000, 0.9238795325112867385, 1.000000000000000000, 0.9238795325112867385, 1.000000000000000000, 0.9238795325112867385, 1.000000000000000000, 0.9238795325112867385, 1.000000000000000000, 0.9238795325112867385, 1.000000000000000000, 0.9238795325112867385, 1.000000000000000000, 0.9238795325112867385, 1.000000000000000000, 0.9238795325112867385, 1.000000000000000000, 0.9238795325112867385, 1.000000000000000000, 0.9238795325112867385, 1.000000000000000000, 0.9238795325112867385, 1.000000000000000000, 0.9238795325112867385, 1.000000000000000000, 0.9238795325112867385, 1.000000000000000000, 0.9238795325112867385, 1.000000000000000000, 0.9238795325112867385, 1.000000000000000000, 0.9238795325112867385, 1.000000000000000000, 0.9238795325112867385, 1.000000000000000000, 0.9238795325112867385, 1.000000000000000000, 0.9238795325112867385, 1.000000000000000000, 0.9238795325112867385, 1.000000000000000000, 0.9238795325112867385, 1.000000000000000000, 0.9238795325112867385, 1.000000000000000000, 0.9238795325112867385, 1.000000000000000000, 0.9238795325112867385, 1.000000000000000000, 0.9238795325112867385, 1.000000000000000000, 0.9238795325112867385, 1.000000000000000000, 0.9238795325112867385, 1.000000000000000000, 0.9238795325112867385, 1.000000000000000000, 0.9238795325112867385, 1.000000000000000000, 0.9694573907295700455, 0.9634246409442903669),
 ( 1.000000000000000000, 0.9238795325112867385, 1.000000000000000000, 0.9238795325112867385, 1.000000000000000000, 0.9238795325112867385, 1.000000000000000000, 0.9238795325112867385, 1.000000000000000000, 0.9238795325112867385, 1.000000000000000000, 0.9238795325112867385, 1.000000000000000000, 0.9238795325112867385, 1.000000000000000000, 0.9238795325112867385, 1.000000000000000000, 0.9238795325112867385, 1.000000000000000000, 0.9238795325112867385, 1.000000000000000000, 0.9238795325112867385, 1.000000000000000000, 0.9238795325112867385, 1.000000000000000000, 0.9238795325112867385, 1.000000000000000000, 0.9238795325112867385, 1.000000000000000000, 0.9238795325112867385, 1.000000000000000000, 0.9238795325112867385, 1.000000000000000000, 0.9238795325112867385, 1.000000000000000000, 0.9238795325112867385, 1.000000000000000000, 0.9238795325112867385, 1.000000000000000000, 0.9238795325112867385, 1.000000000000000000, 0.9238795325112867385, 1.000000000000000000, 0.9238795325112867385, 1.000000000000000000, 0.9238795325112867385, 1.000000000000000000, 0.9238795325112867385, 1.000000000000000000, 0.9238795325112867385, 1.000000000000000000, 0.9238795325112867385, 1.000000000000000000, 0.9238795325112867385, 1.000000000000000000, 0.9238795325112867385, 1.000000000000000000, 0.9238795325112867385, 1.000000000000000000, 0.9238795325112867385, 1.000000000000000000, 0.9238795325112867385, 1.000000000000000000, 0.9238795325112867385, 1.000000000000000000, 0.9238795325112867385, 1.000000000000000000, 0.9238795325112867385, 1.000000000000000000, 0.9238795325112867385, 1.000000000000000000, 0.9238795325112867385, 1.000000000000000000, 0.9238795325112867385, 1.000000000000000000, 0.9238795325112867385, 1.000000000000000000, 0.9694573907295700455, 0.9634246409442903669) ) ) 
 REPRESENTATION_ITEM ( '' )  SURFACE ( )  );
#14457=EDGE_LOOP ( 'NONE', ( #20875, #5079, #13791, #8326 ) ) ;
#14463=CARTESIAN_POINT ( 'NONE',  ( -3.154801521863567881, 47.83913663364971569, 93.80036078214054385 ) ) ;
#14468=DIRECTION ( 'NONE',  ( 0.000000000000000000, -1.000000000000000000, 0.000000000000000000 ) ) ;
#14487=CARTESIAN_POINT ( 'NONE',  ( -0.3080929418689875576, 37.85583172076933778, 94.94558880123797451 ) ) ;
#14488=CARTESIAN_POINT ( 'NONE',  ( -4.567115856812060670, 47.10047254335474065, 93.30496380123798872 ) ) ;
#14497=CARTESIAN_POINT ( 'NONE',  ( 5.611423337425062385, 41.22389019960463230, 90.33621380123798872 ) ) ;
#14504=CARTESIAN_POINT ( 'NONE',  ( -0.08445379298374396104, 38.30427143568992676, 95.05433879953095300 ) ) ;
#14507=CARTESIAN_POINT ( 'NONE',  ( -4.235929252861276417, 41.08920907837907777, 92.55433879953100984 ) ) ;
#14508=DIRECTION ( 'NONE',  ( -1.193617070626243484E-16, -1.000000000000000000, -0.000000000000000000 ) ) ;
#14514=CARTESIAN_POINT ( 'NONE',  ( 30.92220646078100188, 42.96218137147968008, 57.80715055817105252 ) ) ;
#14516=VECTOR ( 'NONE', #11156, 1000.000000000000000 ) ;
#14528=CARTESIAN_POINT ( 'NONE',  ( 4.135038682601217097, 47.90320695352507130, 92.55433879953098142 ) ) ;
#14532=ORIENTED_EDGE ( 'NONE', *, *, #9631, .F. ) ;
#14534=EDGE_CURVE ( 'NONE', #2768, #7833, #16815, .T. ) ;
#14535=PLANE ( 'NONE',  #5711 ) ;
#14537=CARTESIAN_POINT ( 'NONE',  ( 3.122153740306552905, 48.66551347115873227, 96.03933879953099506 ) ) ;
#14538=ORIENTED_EDGE ( 'NONE', *, *, #11608, .T. ) ;
#14544=CARTESIAN_POINT ( 'NONE',  ( -0.4699484075729998822, 52.36218137147968577, 83.03825919817350609 ) ) ;
#14548=CARTESIAN_POINT ( 'NONE',  ( -3.350035803220276609, 49.20851703305431357, 93.22683880123798872 ) ) ;
#14562=AXIS2_PLACEMENT_3D ( 'NONE', #4367, #15562, #10891 ) ;
#14569=LINE ( 'NONE', #6363, #19477 ) ;
#14580=EDGE_CURVE ( 'NONE', #1661, #11174, #3576, .T. ) ;
#14582=ORIENTED_EDGE ( 'NONE', *, *, #17560, .T. ) ;
#14594=CARTESIAN_POINT ( 'NONE',  ( -2.904223097202481174, 48.62752260303690122, 95.33621380294498238 ) ) ;
#14595=AXIS2_PLACEMENT_3D ( 'NONE', #4087, #8900, #5909 ) ;
#14600=EDGE_LOOP ( 'NONE', ( #5669, #7214, #7275, #17749, #4778, #16660, #17107 ) ) ;
#14604=LINE ( 'NONE', #9314, #9529 ) ;
#14605=CARTESIAN_POINT ( 'NONE',  ( 1.352400422481993658, 50.46853102219002096, 90.72683880123797451 ) ) ;
#14606=CARTESIAN_POINT ( 'NONE',  ( -5.154188915835984375, 42.64120994080404614, 95.96121380123798872 ) ) ;
#14607=VERTEX_POINT ( 'NONE', #13050 ) ;
#14609=DIRECTION ( 'NONE',  ( -1.000000000000000000, -1.402518428993831676E-16, -1.196361017915039239E-16 ) ) ;
#14613=VERTEX_POINT ( 'NONE', #16553 ) ;
#14618=ORIENTED_EDGE ( 'NONE', *, *, #14981, .F. ) ;
#14620=CARTESIAN_POINT ( 'NONE',  ( 0.5221537403065010796, 44.16218137147969003, 54.55433879953099563 ) ) ;
#14626=ORIENTED_EDGE ( 'NONE', *, *, #9128, .T. ) ;
#14632=FACE_BOUND ( 'NONE', #3425, .T. ) ;
#14641=CARTESIAN_POINT ( 'NONE',  ( 6.102441102155617969, 43.42752260303680600, 94.55496379953098085 ) ) ;
#14646=DIRECTION ( 'NONE',  ( -0.7071067811865433539, -0.7071067811865516806, -1.146387601258591105E-16 ) ) ;
#14660=AXIS2_PLACEMENT_3D ( 'NONE', #13305, #3401, #8191 ) ;
#14661=ORIENTED_EDGE ( 'NONE', *, *, #16600, .T. ) ;
#14662=EDGE_CURVE ( 'NONE', #2157, #7787, #3449, .T. ) ;
#14668=CARTESIAN_POINT ( 'NONE',  ( -1.183761187420877548, 49.81017696809242068, 95.05433879953098142 ) ) ;
#14671=CARTESIAN_POINT ( 'NONE',  ( 10.77494014480653917, 42.96218137147968008, 61.40715055817103263 ) ) ;
#14672=VECTOR ( 'NONE', #14932, 1000.000000000000000 ) ;
#14675=DIRECTION ( 'NONE',  ( -1.402518428993831430E-16, 1.000000000000000000, -2.891205793294680792E-16 ) ) ;
#14677=CARTESIAN_POINT ( 'NONE',  ( -4.567115856812060670, 47.10047254335474065, 93.30496380123798872 ) ) ;
#14678=ORIENTED_EDGE ( 'NONE', *, *, #9653, .T. ) ;
#14691=PLANE ( 'NONE',  #16888 ) ;
#14696=CARTESIAN_POINT ( 'NONE',  ( -4.524181921268124462, 40.28999182795290324, 92.28933880123798872 ) ) ;
#14700=VECTOR ( 'NONE', #7911, 1000.000000000000000 ) ;
#14702=VECTOR ( 'NONE', #2106, 1000.000000000000000 ) ;
#14710=CARTESIAN_POINT ( 'NONE',  ( 3.460444912181559474, 49.25145096859824889, 91.89871380123798872 ) ) ;
#14717=CARTESIAN_POINT ( 'NONE',  ( 5.751194534584169737, 45.49804388114897336, 92.55433879953095300 ) ) ;
#14722=CARTESIAN_POINT ( 'NONE',  ( 4.135038682601217097, 47.90320695352507130, 92.55433879953098142 ) ) ;
#14723=EDGE_LOOP ( 'NONE', ( #16580, #18004, #1234, #5934 ) ) ;
#14725=CARTESIAN_POINT ( 'NONE',  ( 30.92220646078100188, 42.76218137147968434, 61.80715055817104542 ) ) ;
#14734=EDGE_CURVE ( 'NONE', #7261, #12967, #13774, .T. ) ;
#14739=CARTESIAN_POINT ( 'NONE',  ( 2.263363662449282110, 49.77488197367689793, 93.03606768333816035 ) ) ;
#14745=PLANE ( 'NONE',  #6371 ) ;
#14747=CARTESIAN_POINT ( 'NONE',  ( -2.077846259693550746, 39.65884927180063357, 96.66433879953098085 ) ) ;
#14753=CARTESIAN_POINT ( 'NONE',  ( -3.154801521863568325, 47.83913663364971569, 83.28180655319408743 ) ) ;
#14755=CARTESIAN_POINT ( 'NONE',  ( -5.154188915835984375, 42.64120994080404614, 93.46121380123797451 ) ) ;
#14762=CARTESIAN_POINT ( 'NONE',  ( -3.154801521863568325, 47.83913663364971569, 95.05036078214054385 ) ) ;
#14763=PLANE ( 'NONE',  #18067 ) ;
#14766=EDGE_LOOP ( 'NONE', ( #1753, #15806, #18226, #16505 ) ) ;
#14767=DIRECTION ( 'NONE',  ( -0.8660254037844395958, 0.4999999999999983347, 0.000000000000000000 ) ) ;
#14769=EDGE_CURVE ( 'NONE', #3265, #3130, #8783, .T. ) ;
#14770=CARTESIAN_POINT ( 'NONE',  ( 31.07218010054375412, 42.76218137147968434, 65.80574467885102763 ) ) ;
#14774=DIRECTION ( 'NONE',  ( -0.000000000000000000, -0.000000000000000000, 1.000000000000000000 ) ) ;
#14775=CARTESIAN_POINT ( 'NONE',  ( -0.3080929418689875576, 37.85583172076932357, 93.69558880123807398 ) ) ;
#14781=CARTESIAN_POINT ( 'NONE',  ( -0.3080929418689875576, 37.85583172076933778, 93.69558880123800293 ) ) ;
#14797=CARTESIAN_POINT ( 'NONE',  ( 6.828503391016846891, 43.33193468930419101, 91.50808880123798872 ) ) ;
#14807=CARTESIAN_POINT ( 'NONE',  ( -3.154801521863568325, 47.83913663364971569, 92.86286078555453116 ) ) ;
#14810=CARTESIAN_POINT ( 'NONE',  ( 4.394343283833276992, 39.11584570990505938, 95.10183880123797451 ) ) ;
#14816=CARTESIAN_POINT ( 'NONE',  ( 6.027795660425420365, 43.94244667862099618, 92.55433879953100984 ) ) ;
#14820=EDGE_LOOP ( 'NONE', ( #12597, #6228, #5007, #1643 ) ) ;
#14821=CARTESIAN_POINT ( 'NONE',  ( 11.22215374030650281, 51.36218137147968577, 62.80715055817104542 ) ) ;
#14822=PRODUCT_DEFINITION ( 'UNKNOWN', '', #2070, #13828 ) ;
#14840=CARTESIAN_POINT ( 'NONE',  ( 1.256812508749381774, 49.74246873332880625, 94.86746379953099506 ) ) ;
#14841=VERTEX_POINT ( 'NONE', #14185 ) ;
#14842=CARTESIAN_POINT ( 'NONE',  ( 1.352400422481993658, 50.46853102219002096, 95.72683880123798872 ) ) ;
#14848=CARTESIAN_POINT ( 'NONE',  ( -3.943187491250720544, 40.73580453397070755, 94.08621379953100927 ) ) ;
#14853=ORIENTED_EDGE ( 'NONE', *, *, #412, .T. ) ;
#14861=VECTOR ( 'NONE', #19553, 1000.000000000000000 ) ;
#14862=ORIENTED_EDGE ( 'NONE', *, *, #1693, .T. ) ;
#14865=CARTESIAN_POINT ( 'NONE',  ( 5.591308205070052217, 40.32050054405898720, 80.55433879953099563 ) ) ;
#14874=DIRECTION ( 'NONE',  ( 1.000000000000000000, -0.000000000000000000, -0.000000000000000000 ) ) ;
#14876=CARTESIAN_POINT ( 'NONE',  ( 2.043125170982144745, 38.48583871533720213, 93.77371380123807398 ) ) ;
#14879=CARTESIAN_POINT ( 'NONE',  ( -4.524181921268124462, 40.28999182795290324, 91.03933880123798872 ) ) ;
#14880=CARTESIAN_POINT ( 'NONE',  ( 4.394343283833276992, 39.11584570990505938, 92.60183880123797451 ) ) ;
#14883=VECTOR ( 'NONE', #14468, 1000.000000000000000 ) ;
#14900=CARTESIAN_POINT ( 'NONE',  ( -0.3080929418689875576, 37.85583172076933778, 91.19558880123798872 ) ) ;
#14903=ADVANCED_FACE ( 'NONE', ( #11021 ), #19183, .F. ) ;
#14904=CARTESIAN_POINT ( 'NONE',  ( -5.154188915835984375, 42.64120994080404614, 94.71121380123797451 ) ) ;
#14907=DIRECTION ( 'NONE',  ( 0.000000000000000000, 0.000000000000000000, 1.000000000000000000 ) ) ;
#14917=EDGE_CURVE ( 'NONE', #17731, #16572, #16006, .T. ) ;
#14923=ORIENTED_EDGE ( 'NONE', *, *, #14534, .F. ) ;
#14926=EDGE_CURVE ( 'NONE', #2580, #13095, #20870, .T. ) ;
#14932=DIRECTION ( 'NONE',  ( 0.000000000000000000, 0.000000000000000000, 1.000000000000000000 ) ) ;
#14934=ADVANCED_FACE ( 'NONE', ( #16429 ), #8435, .T. ) ;
#14941=DIRECTION ( 'NONE',  ( 0.000000000000000000, -1.000000000000000000, 2.168404344970984808E-15 ) ) ;
#14944=CARTESIAN_POINT ( 'NONE',  ( -3.943187491250720544, 40.73580453397070755, 95.33621379953099506 ) ) ;
#14945=VECTOR ( 'NONE', #17190, 1000.000000000000000 ) ;
#14951=FACE_OUTER_BOUND ( 'NONE', #16628, .T. ) ;
#14953=VERTEX_POINT ( 'NONE', #3541 ) ;
#14956=CARTESIAN_POINT ( 'NONE',  ( 1.352400422481993658, 50.46853102219002096, 94.47683880123798872 ) ) ;
#14957=VECTOR ( 'NONE', #15146, 1000.000000000000000 ) ;
#14961=CARTESIAN_POINT ( 'NONE',  ( 5.611423337425062385, 41.22389019960463230, 95.17996380123798872 ) ) ;
#14970=VERTEX_POINT ( 'NONE', #234 ) ;
#14976=EDGE_CURVE ( 'NONE', #1479, #15007, #19594, .T. ) ;
#14980=ORIENTED_EDGE ( 'NONE', *, *, #10415, .F. ) ;
#14981=EDGE_CURVE ( 'NONE', #19783, #16684, #8228, .T. ) ;
#14982=CARTESIAN_POINT ( 'NONE',  ( 1.514255888186008425, 52.36218137147968577, 52.53721119516358584 ) ) ;
#14994=CARTESIAN_POINT ( 'NONE',  ( 5.146041124512939824, 40.41782456190201600, 90.15009067557426192 ) ) ;
#14995=CARTESIAN_POINT ( 'NONE',  ( -5.154188915835984375, 42.64120994080404614, 93.46121380123797451 ) ) ;
#14996=VERTEX_POINT ( 'NONE', #17802 ) ;
#15003=CARTESIAN_POINT ( 'NONE',  ( 1.256812508749381774, 49.74246873332880625, 91.11746379953096664 ) ) ;
#15006=CARTESIAN_POINT ( 'NONE',  ( -0.2125050281363792815, 38.58189400963056670, 93.30496380294499659 ) ) ;
#15007=VERTEX_POINT ( 'NONE', #6829 ) ;
#15011=PLANE ( 'NONE',  #11793 ) ;
#15012=LINE ( 'NONE', #8737, #8239 ) ;
#15014=VECTOR ( 'NONE', #20918, 1000.000000000000000 ) ;
#15015=( BOUNDED_CURVE ( )  B_SPLINE_CURVE ( 2, ( #19555, #3388, #11496, #8504, #17968 ),
 .UNSPECIFIED., .F., .F. ) 
 B_SPLINE_CURVE_WITH_KNOTS ( ( 3, 2, 3 ),
 ( 0.2430974982970244558, 0.2604082588139463583, 0.2691383253928207320 ),
 .UNSPECIFIED. ) 
 CURVE ( )  GEOMETRIC_REPRESENTATION_ITEM ( )  RATIONAL_B_SPLINE_CURVE ( ( 0.9660722094251257275, 0.9493985640419095873, 1.000000000000000000, 0.9744809649195396162, 0.9660722070857166166 ) ) 
 REPRESENTATION_ITEM ( '' )  );
#15016=CARTESIAN_POINT ( 'NONE',  ( -1.579458713576543882, 38.67424504380988282, 95.05433879952670395 ) ) ;
#15019=CARTESIAN_POINT ( 'NONE',  ( -5.058133621542618030, 44.89684013992257405, 95.49246380294496817 ) ) ;
#15023=CARTESIAN_POINT ( 'NONE',  ( 6.198496396448986090, 45.68315280215533392, 94.08621380123798872 ) ) ;
#15024=CIRCLE ( 'NONE', #18089, 4.200000000000001066 ) ;
#15027=VECTOR ( 'NONE', #855, 1000.000000000000000 ) ;
#15029=ORIENTED_EDGE ( 'NONE', *, *, #3240, .T. ) ;
#15031=CARTESIAN_POINT ( 'NONE',  ( 2.043125170982144745, 38.48583871533720213, 91.27371380123798872 ) ) ;
#15033=DIRECTION ( 'NONE',  ( 0.5735764363510446051, 0.8191520442889927978, 9.299032798180135705E-17 ) ) ;
#15039=EDGE_CURVE ( 'NONE', #8376, #9835, #2534, .T. ) ;
#15040=VECTOR ( 'NONE', #10287, 1000.000000000000000 ) ;
#15044=VECTOR ( 'NONE', #14874, 1000.000000000000000 ) ;
#15058=CARTESIAN_POINT ( 'NONE',  ( 3.948530577815480225, 39.69684013992245752, 95.64871379953100927 ) ) ;
#15059=CARTESIAN_POINT ( 'NONE',  ( 5.025485839985549319, 41.56218137147963887, 94.47683879953099506 ) ) ;
#15065=DIRECTION ( 'NONE',  ( -0.000000000000000000, 1.000000000000000000, -0.000000000000000000 ) ) ;
#15066=ORIENTED_EDGE ( 'NONE', *, *, #783, .T. ) ;
#15068=CARTESIAN_POINT ( 'NONE',  ( -4.567115856812060670, 47.10047254335474065, 95.96121380123798872 ) ) ;
#15072=VECTOR ( 'NONE', #612, 1000.000000000000000 ) ;
#15076=CARTESIAN_POINT ( 'NONE',  ( 31.22215374030650281, 42.96218137147968008, 74.20433879953100131 ) ) ;
#15083=LINE ( 'NONE', #16884, #13236 ) ;
#15085=CARTESIAN_POINT ( 'NONE',  ( 1.352400422481993658, 50.46853102219002096, 93.22683880123798872 ) ) ;
#15087=ORIENTED_EDGE ( 'NONE', *, *, #16162, .T. ) ;
#15090=ORIENTED_EDGE ( 'NONE', *, *, #873, .F. ) ;
#15094=CARTESIAN_POINT ( 'NONE',  ( 0.5221537403065010796, 44.16218137147969003, 45.55433879953098852 ) ) ;
#15097=CARTESIAN_POINT ( 'NONE',  ( -5.368445182934982185, 36.96218137147968008, 45.55433879953098852 ) ) ;
#15104=CARTESIAN_POINT ( 'NONE',  ( -2.416137431568557314, 39.07291177436112406, 92.36746380123797451 ) ) ;
#15109=EDGE_CURVE ( 'NONE', #3380, #4927, #4807, .T. ) ;
#15111=LINE ( 'NONE', #13608, #13981 ) ;
#15113=CARTESIAN_POINT ( 'NONE',  ( -5.154188915835984375, 42.64120994080404614, 92.36746380123797451 ) ) ;
#15116=DIRECTION ( 'NONE',  ( 0.8660254037844351549, -1.033702705553087164E-16, -0.5000000000000061062 ) ) ;
#15126=CARTESIAN_POINT ( 'NONE',  ( -4.500660556396669065, 42.81632233694663370, 90.57058880294496817 ) ) ;
#15129=CARTESIAN_POINT ( 'NONE',  ( 1.352400422481993658, 50.46853102219002096, 90.72683880123797451 ) ) ;
#15137=CARTESIAN_POINT ( 'NONE',  ( -4.567115856812060670, 47.10047254335474065, 92.05496380123798872 ) ) ;
#15138=( BOUNDED_CURVE ( )  B_SPLINE_CURVE ( 2, ( #4009, #8925, #10530, #15414, #13487, #828, #7315, #19958, #5388 ),
 .UNSPECIFIED., .F., .F. ) 
 B_SPLINE_CURVE_WITH_KNOTS ( ( 3, 2, 2, 2, 3 ),
 ( 0.5133706321031978881, 0.5208165472167179955, 0.5468573745775568984, 0.5728982019383959123, 0.5936396777664850744 ),
 .UNSPECIFIED. ) 
 CURVE ( )  GEOMETRIC_REPRESENTATION_ITEM ( )  RATIONAL_B_SPLINE_CURVE ( ( 0.9689162004489071389, 0.9782346954085345825, 1.000000000000000000, 0.9238795325112867385, 1.000000000000000000, 0.9238795325112867385, 1.000000000000000000, 0.9393701738211922558, 0.9753234597473514622 ) ) 
 REPRESENTATION_ITEM ( '' )  );
#15139=ORIENTED_EDGE ( 'NONE', *, *, #15893, .F. ) ;
#15145=VERTEX_POINT ( 'NONE', #2158 ) ;
#15146=DIRECTION ( 'NONE',  ( -1.000000000000000000, -1.402518428993831676E-16, -1.196361017915039239E-16 ) ) ;
#15148=LINE ( 'NONE', #11964, #16559 ) ;
#15149=CARTESIAN_POINT ( 'NONE',  ( -5.368445182934982185, 36.96218137147968008, 93.55433879953098142 ) ) ;
#15156=EDGE_CURVE ( 'NONE', #18045, #11193, #18218, .T. ) ;
#15157=ORIENTED_EDGE ( 'NONE', *, *, #14197, .F. ) ;
#15158=PLANE ( 'NONE',  #19693 ) ;
#15159=CARTESIAN_POINT ( 'NONE',  ( 1.256812508749381774, 49.74246873332880625, 96.11746379953099506 ) ) ;
#15160=CARTESIAN_POINT ( 'NONE',  ( 6.102441102155617969, 43.42752260303680600, 93.30496379953098085 ) ) ;
#15178=ORIENTED_EDGE ( 'NONE', *, *, #20150, .F. ) ;
#15181=ORIENTED_EDGE ( 'NONE', *, *, #30, .T. ) ;
#15183=DIRECTION ( 'NONE',  ( -0.4999999999999977240, 0.8660254037844398178, 0.000000000000000000 ) ) ;
#15184=CARTESIAN_POINT ( 'NONE',  ( 5.611423337425062385, 41.22389019960463230, 94.08621380123797451 ) ) ;
#15187=VERTEX_POINT ( 'NONE', #5553 ) ;
#15195=DIRECTION ( 'NONE',  ( -0.000000000000000000, -0.000000000000000000, 1.000000000000000000 ) ) ;
#15198=CARTESIAN_POINT ( 'NONE',  ( -5.154188915835984375, 42.64120994080404614, 96.11746380123797451 ) ) ;
#15200=CARTESIAN_POINT ( 'NONE',  ( 2.916646314870772194, 38.79555996194921619, 92.55433879953098142 ) ) ;
#15201=CARTESIAN_POINT ( 'NONE',  ( -0.4699484075729998267, 52.36218137147968577, 87.21440135111343750 ) ) ;
#15202=CARTESIAN_POINT ( 'NONE',  ( -5.784195910403845176, 44.99242805365518194, 93.38308880123798872 ) ) ;
#15203=CIRCLE ( 'NONE', #7394, 5.199999999999999289 ) ;
#15205=VERTEX_POINT ( 'NONE', #3540 ) ;
#15210=VERTEX_POINT ( 'NONE', #12058 ) ;
#15214=CARTESIAN_POINT ( 'NONE',  ( -5.784195910403845176, 44.99242805365518194, 94.78933880123798872 ) ) ;
#15215=VECTOR ( 'NONE', #9276, 1000.000000000000000 ) ;
#15216=DIRECTION ( 'NONE',  ( 1.193617070626243484E-16, 1.000000000000000000, 0.000000000000000000 ) ) ;
#15218=LINE ( 'NONE', #629, #12649 ) ;
#15221=ORIENTED_EDGE ( 'NONE', *, *, #6778, .F. ) ;
#15230=CARTESIAN_POINT ( 'NONE',  ( -2.077846259693550746, 39.65884927180063357, 90.72683880294498238 ) ) ;
#15231=VECTOR ( 'NONE', #18524, 1000.000000000000000 ) ;
#15234=CARTESIAN_POINT ( 'NONE',  ( 1.352400422481993658, 50.46853102219002096, 93.07058880123798872 ) ) ;
#15239=ORIENTED_EDGE ( 'NONE', *, *, #7548, .T. ) ;
#15242=CARTESIAN_POINT ( 'NONE',  ( 1.352400422481993658, 50.46853102219002096, 91.82058880123801714 ) ) ;
#15249=DIRECTION ( 'NONE',  ( 0.000000000000000000, 0.000000000000000000, -1.000000000000000000 ) ) ;
#15252=VERTEX_POINT ( 'NONE', #16839 ) ;
#15255=DIRECTION ( 'NONE',  ( -1.193617070626243484E-16, -1.000000000000000000, -0.000000000000000000 ) ) ;
#15263=FACE_BOUND ( 'NONE', #20967, .T. ) ;
#15268=CARTESIAN_POINT ( 'NONE',  ( 4.987494971863720927, 47.58855820898865829, 93.46121379953098085 ) ) ;
#15269=CARTESIAN_POINT ( 'NONE',  ( 1.868012774839550749, 39.13936707477651566, 93.07058879953099506 ) ) ;
#15279=CARTESIAN_POINT ( 'NONE',  ( -3.350035803220276609, 49.20851703305431357, 93.38308880123798872 ) ) ;
#15285=CIRCLE ( 'NONE', #6796, 0.9921021478795063464 ) ;
#15290=VERTEX_POINT ( 'NONE', #6720 ) ;
#15291=EDGE_LOOP ( 'NONE', ( #4357, #17162, #13754 ) ) ;
#15295=ORIENTED_EDGE ( 'NONE', *, *, #1014, .T. ) ;
#15296=CARTESIAN_POINT ( 'NONE',  ( 31.22215374030650281, 42.76218137147968434, 78.80433879953099563 ) ) ;
#15297=CARTESIAN_POINT ( 'NONE',  ( 11.22215374030650281, 51.36218137147968577, 64.80574467885102763 ) ) ;
#15303=ORIENTED_EDGE ( 'NONE', *, *, #18103, .T. ) ;
#15316=CARTESIAN_POINT ( 'NONE',  ( 5.025485839985549319, 41.56218137147963887, 92.28933880294496817 ) ) ;
#15317=VECTOR ( 'NONE', #4044, 1000.000000000000000 ) ;
#15322=ORIENTED_EDGE ( 'NONE', *, *, #16747, .F. ) ;
#15325=DIRECTION ( 'NONE',  ( 0.000000000000000000, 0.000000000000000000, -1.000000000000000000 ) ) ;
#15327=CARTESIAN_POINT ( 'NONE',  ( 3.460444912181559474, 49.25145096859824889, 95.64871380123798872 ) ) ;
#15332=ORIENTED_EDGE ( 'NONE', *, *, #10784, .T. ) ;
#15339=LINE ( 'NONE', #5540, #15231 ) ;
#15340=VECTOR ( 'NONE', #8650, 1000.000000000000000 ) ;
#15343=CARTESIAN_POINT ( 'NONE',  ( 5.611423337425062385, 41.22389019960463230, 90.33621380123798872 ) ) ;
#15348=ORIENTED_EDGE ( 'NONE', *, *, #18034, .T. ) ;
#15349=AXIS2_PLACEMENT_3D ( 'NONE', #13219, #9937, #19900 ) ;
#15352=CARTESIAN_POINT ( 'NONE',  ( 3.460444912181559474, 49.25145096859824889, 92.99246380123798872 ) ) ;
#15357=CARTESIAN_POINT ( 'NONE',  ( 30.92220646078100188, 45.56218137147968861, 62.80715055817104542 ) ) ;
#15361=ADVANCED_FACE ( 'NONE', ( #2676, #769 ), #9292, .F. ) ;
#15365=CARTESIAN_POINT ( 'NONE',  ( -0.4699484075729998822, 52.36218137147968577, 83.03825919817350609 ) ) ;
#15374=VECTOR ( 'NONE', #20412, 1000.000000000000000 ) ;
#15375=ORIENTED_EDGE ( 'NONE', *, *, #4412, .T. ) ;
#15380=CARTESIAN_POINT ( 'NONE',  ( 5.544968037009670780, 45.50804040601273925, 93.38308879953099506 ) ) ;
#15381=CARTESIAN_POINT ( 'NONE',  ( -0.8237052942265477018, 49.18499566818285018, 91.19558879953099506 ) ) ;
#15384=CARTESIAN_POINT ( 'NONE',  ( -5.784195910403845176, 44.99242805365518194, 92.28933880123798872 ) ) ;
#15389=AXIS2_PLACEMENT_3D ( 'NONE', #8315, #12042, #2031 ) ;
#15392=CARTESIAN_POINT ( 'NONE',  ( 2.043125170982144745, 38.48583871533720213, 95.17996380123798872 ) ) ;
#15396=CARTESIAN_POINT ( 'NONE',  ( 5.611423337425062385, 41.22389019960463230, 91.42996380123798872 ) ) ;
#15399=ADVANCED_FACE ( 'NONE', ( #7356 ), #20327, .F. ) ;
#15406=LINE ( 'NONE', #5700, #14324 ) ;
#15407=CARTESIAN_POINT ( 'NONE',  ( 6.198496396448986090, 45.68315280215533392, 94.24246380123798872 ) ) ;
#15409=CARTESIAN_POINT ( 'NONE',  ( -3.154801521863568325, 47.83913663364971569, 83.28180655319408743 ) ) ;
#15413=AXIS2_PLACEMENT_3D ( 'NONE', #8286, #14767, #6673 ) ;
#15414=CARTESIAN_POINT ( 'NONE',  ( 5.568489401881125289, 48.03437091500647682, 92.91433880123805977 ) ) ;
#15416=LINE ( 'NONE', #13914, #10653 ) ;
#15417=CARTESIAN_POINT ( 'NONE',  ( 4.394343283833276992, 39.11584570990505938, 94.00808880123797451 ) ) ;
#15421=CARTESIAN_POINT ( 'NONE',  ( -0.2125050281363792815, 38.58189400963055959, 92.05496380294498238 ) ) ;
#15423=ORIENTED_EDGE ( 'NONE', *, *, #3745, .T. ) ;
#15424=VERTEX_POINT ( 'NONE', #189 ) ;
#15425=CARTESIAN_POINT ( 'NONE',  ( 4.199109002476567376, 47.83913663364971569, 95.05036078555451695 ) ) ;
#15428=CARTESIAN_POINT ( 'NONE',  ( -0.3080929418689875576, 37.85583172076933778, 92.60183880123797451 ) ) ;
#15433=CARTESIAN_POINT ( 'NONE',  ( -4.677846234369972045, 43.47758828951656795, 93.04575777171294249 ) ) ;
#15439=LINE ( 'NONE', #13832, #10679 ) ;
#15442=CARTESIAN_POINT ( 'NONE',  ( 1.256812508749381774, 49.74246873332880625, 92.67996380294498238 ) ) ;
#15443=CARTESIAN_POINT ( 'NONE',  ( 1.514255888186003984, 52.36218137147968577, 87.21440135111343750 ) ) ;
#15445=CARTESIAN_POINT ( 'NONE',  ( 4.134898411747151670, 47.90306806511021875, 95.05422504033560926 ) ) ;
#15450=ORIENTED_EDGE ( 'NONE', *, *, #8083, .F. ) ;
#15453=CARTESIAN_POINT ( 'NONE',  ( 4.454347278305088587, 39.79502279609036464, 90.11785590924256439 ) ) ;
#15463=EDGE_CURVE ( 'NONE', #3020, #2188, #8224, .T. ) ;
#15465=CARTESIAN_POINT ( 'NONE',  ( -1.174478664588461951, 57.66640723084523046, 54.55433879953099563 ) ) ;
#15476=CARTESIAN_POINT ( 'NONE',  ( -7.677846259693480668, 36.96218137147968008, 93.55433879953098142 ) ) ;
#15477=EDGE_CURVE ( 'NONE', #13124, #14061, #4475, .T. ) ;
#15482=CARTESIAN_POINT ( 'NONE',  ( 3.122153740306552905, 48.66551347115873227, 94.78933879953099506 ) ) ;
#15484=ORIENTED_EDGE ( 'NONE', *, *, #19875, .F. ) ;
#15485=CARTESIAN_POINT ( 'NONE',  ( -5.154188915835984375, 42.64120994080404614, 93.61746380123797451 ) ) ;
#15491=ADVANCED_FACE ( 'NONE', ( #11490 ), #1804, .F. ) ;
#15494=CARTESIAN_POINT ( 'NONE',  ( 6.828503391016846891, 43.33193468930419101, 90.41433880123798872 ) ) ;
#15495=ORIENTED_EDGE ( 'NONE', *, *, #10415, .T. ) ;
#15498=FACE_OUTER_BOUND ( 'NONE', #3645, .T. ) ;
#15502=DIRECTION ( 'NONE',  ( -1.402518428993831430E-16, 1.000000000000000000, -2.891205793294680792E-16 ) ) ;
#15509=CARTESIAN_POINT ( 'NONE',  ( -5.784195910403845176, 44.99242805365518194, 94.63308880123798872 ) ) ;
#15511=ADVANCED_FACE ( 'NONE', ( #10097 ), #8498, .F. ) ;
#15520=CARTESIAN_POINT ( 'NONE',  ( -5.784195910403845176, 44.99242805365518194, 96.03933880123796030 ) ) ;
#15525=CARTESIAN_POINT ( 'NONE',  ( -4.500660556396669065, 42.81632233694663370, 93.07058880294496817 ) ) ;
#15530=FACE_OUTER_BOUND ( 'NONE', #4438, .T. ) ;
#15531=CARTESIAN_POINT ( 'NONE',  ( 5.722153740306818115, 44.84677435893292596, 93.35825776475003579 ) ) ;
#15533=CARTESIAN_POINT ( 'NONE',  ( 3.460444912181559474, 49.25145096859824889, 90.64871380123798872 ) ) ;
#15546=VECTOR ( 'NONE', #13620, 1000.000000000000000 ) ;
#15548=CARTESIAN_POINT ( 'NONE',  ( 3.948530577815480225, 39.69684013992245752, 90.96121380294498238 ) ) ;
#15550=CARTESIAN_POINT ( 'NONE',  ( 30.92220646078100188, 45.56218137147968861, 56.80715055817104542 ) ) ;
#15551=CARTESIAN_POINT ( 'NONE',  ( 5.611423337425062385, 41.22389019960463230, 91.42996380123798872 ) ) ;
#15552=VECTOR ( 'NONE', #2560, 1000.000000000000000 ) ;
#15557=VECTOR ( 'NONE', #17840, 1000.000000000000000 ) ;
#15559=CARTESIAN_POINT ( 'NONE',  ( 6.102441102155617969, 43.42752260303680600, 92.36746380294498238 ) ) ;
#15562=DIRECTION ( 'NONE',  ( 1.193617070626243484E-16, 1.000000000000000000, 0.000000000000000000 ) ) ;
#15569=AXIS2_PLACEMENT_3D ( 'NONE', #19151, #9378, #15861 ) ;
#15570=VERTEX_POINT ( 'NONE', #6978 ) ;
#15572=DIRECTION ( 'NONE',  ( 0.000000000000000000, 0.000000000000000000, -1.000000000000000000 ) ) ;
#15574=LINE ( 'NONE', #8769, #15643 ) ;
#15579=VERTEX_POINT ( 'NONE', #18696 ) ;
#15585=CARTESIAN_POINT ( 'NONE',  ( -5.154188915835984375, 42.64120994080404614, 94.86746380123797451 ) ) ;
#15588=CARTESIAN_POINT ( 'NONE',  ( -4.524181921268124462, 40.28999182795290324, 94.94558880123797451 ) ) ;
#15591=ORIENTED_EDGE ( 'NONE', *, *, #18320, .T. ) ;
#15602=CARTESIAN_POINT ( 'NONE',  ( 2.043125170982144745, 38.48583871533720213, 91.27371380123798872 ) ) ;
#15603=VECTOR ( 'NONE', #2464, 1000.000000000000000 ) ;
#15611=EDGE_LOOP ( 'NONE', ( #1949, #19578, #20864, #6713, #16823, #5520, #13531, #9953 ) ) ;
#15612=CARTESIAN_POINT ( 'NONE',  ( 30.92220646078100188, 45.56218137147968861, 62.80715055817104542 ) ) ;
#15614=CARTESIAN_POINT ( 'NONE',  ( 6.828503391016846891, 43.33193468930419101, 90.41433880123798872 ) ) ;
#15618=FACE_OUTER_BOUND ( 'NONE', #13333, .T. ) ;
#15628=CARTESIAN_POINT ( 'NONE',  ( 5.611423337425062385, 41.22389019960463230, 91.58621380123798872 ) ) ;
#15630=EDGE_CURVE ( 'NONE', #18174, #15290, #12109, .T. ) ;
#15633=CARTESIAN_POINT ( 'NONE',  ( -2.077846259693550746, 39.65884927180063357, 94.47683880294496817 ) ) ;
#15635=CARTESIAN_POINT ( 'NONE',  ( -0.2125050281363792815, 38.58189400963055959, 90.80496380294498238 ) ) ;
#15636=VECTOR ( 'NONE', #6252, 1000.000000000000000 ) ;
#15643=VECTOR ( 'NONE', #13759, 1000.000000000000000 ) ;
#15654=CARTESIAN_POINT ( 'NONE',  ( 1.514255888186008425, 52.36218137147968577, 52.53721119516358584 ) ) ;
#15657=DIRECTION ( 'NONE',  ( -1.334402673828316297E-16, 2.168404344970984808E-15, 1.000000000000000000 ) ) ;
#15662=CARTESIAN_POINT ( 'NONE',  ( 2.043125170982144745, 38.48583871533720213, 92.52371380123798872 ) ) ;
#15667=VERTEX_POINT ( 'NONE', #7412 ) ;
#15668=STYLED_ITEM ( 'NONE', ( #8824 ), #4882 ) ;
#15669=LINE ( 'NONE', #12775, #6120 ) ;
#15670=CARTESIAN_POINT ( 'NONE',  ( -0.8237052942265477018, 49.18499566818285018, 94.00808880294498238 ) ) ;
#15681=DIRECTION ( 'NONE',  ( 0.000000000000000000, -1.000000000000000000, 0.000000000000000000 ) ) ;
#15682=CARTESIAN_POINT ( 'NONE',  ( 31.07218010054375412, 42.76218137147968434, 66.20574467885103331 ) ) ;
#15683=CARTESIAN_POINT ( 'NONE',  ( -2.416137431568557314, 39.07291177436112406, 93.61746380123797451 ) ) ;
#15685=PLANE ( 'NONE',  #12870 ) ;
#15688=AXIS2_PLACEMENT_3D ( 'NONE', #10991, #17462, #6481 ) ;
#15694=LINE ( 'NONE', #17276, #7481 ) ;
#15695=CARTESIAN_POINT ( 'NONE',  ( 5.568489401881125289, 48.03437091500646261, 94.32058880123798872 ) ) ;
#15699=CARTESIAN_POINT ( 'NONE',  ( 5.568489401881125289, 48.03437091500646261, 94.32058880123798872 ) ) ;
#15704=CARTESIAN_POINT ( 'NONE',  ( 5.025485839985549319, 41.56218137147963887, 93.22683879953099506 ) ) ;
#15707=ORIENTED_EDGE ( 'NONE', *, *, #634, .F. ) ;
#15712=ADVANCED_FACE ( 'NONE', ( #20389 ), #18906, .F. ) ;
#15717=VERTEX_POINT ( 'NONE', #19213 ) ;
#15723=CARTESIAN_POINT ( 'NONE',  ( 5.568489401881125289, 48.03437091500646261, 91.82058880123797451 ) ) ;
#15725=DIRECTION ( 'NONE',  ( -0.000000000000000000, -0.000000000000000000, 1.000000000000000000 ) ) ;
#15738=CARTESIAN_POINT ( 'NONE',  ( -0.3080929418689875576, 37.85583172076933778, 92.60183880123797451 ) ) ;
#15744=CARTESIAN_POINT ( 'NONE',  ( 4.987494971863720927, 47.58855820898865829, 92.52371380294498238 ) ) ;
#15745=ADVANCED_FACE ( 'NONE', ( #15618 ), #14115, .T. ) ;
#15756=CARTESIAN_POINT ( 'NONE',  ( 4.199109002476567376, 47.83913663364971569, 94.73786078214052964 ) ) ;
#15757=DIRECTION ( 'NONE',  ( -2.838338907332122006E-16, 1.000000000000000000, 0.000000000000000000 ) ) ;
#15758=ADVANCED_FACE ( 'NONE', ( #17729 ), #719, .T. ) ;
#15768=DIRECTION ( 'NONE',  ( 0.4999999999999977240, -0.8660254037844398178, -0.000000000000000000 ) ) ;
#15769=EDGE_CURVE ( 'NONE', #10737, #5474, #6410, .T. ) ;
#15770=AXIS2_PLACEMENT_3D ( 'NONE', #1409, #15886, #6286 ) ;
#15771=VERTEX_POINT ( 'NONE', #8234 ) ;
#15772=CARTESIAN_POINT ( 'NONE',  ( -4.567115856812060670, 47.10047254335474065, 90.80496380123797451 ) ) ;
#15778=CARTESIAN_POINT ( 'NONE',  ( -2.904223097202481174, 48.62752260303690122, 90.33621380294496817 ) ) ;
#15784=DIRECTION ( 'NONE',  ( 1.000000000000000000, 0.000000000000000000, 0.000000000000000000 ) ) ;
#15788=VERTEX_POINT ( 'NONE', #14722 ) ;
#15793=CARTESIAN_POINT ( 'NONE',  ( -2.416137431568557314, 39.07291177436112406, 96.11746380123797451 ) ) ;
#15801=CARTESIAN_POINT ( 'NONE',  ( -4.524181921268124462, 40.28999182795290324, 96.19558880123798872 ) ) ;
#15803=VERTEX_POINT ( 'NONE', #142 ) ;
#15806=ORIENTED_EDGE ( 'NONE', *, *, #6047, .T. ) ;
#15812=ORIENTED_EDGE ( 'NONE', *, *, #10424, .F. ) ;
#15826=CARTESIAN_POINT ( 'NONE',  ( -5.154188915835984375, 42.64120994080404614, 95.96121380123798872 ) ) ;
#15828=ORIENTED_EDGE ( 'NONE', *, *, #3240, .F. ) ;
#15832=ORIENTED_EDGE ( 'NONE', *, *, #11078, .T. ) ;
#15841=CARTESIAN_POINT ( 'NONE',  ( 4.394343283833276992, 39.11584570990505938, 92.75808880123797451 ) ) ;
#15846=CARTESIAN_POINT ( 'NONE',  ( 30.92220646078100188, 45.56218137147968861, 62.80715055817104542 ) ) ;
#15856=CARTESIAN_POINT ( 'NONE',  ( 1.514255888186003762, 51.36218137147968577, 83.03825919817350609 ) ) ;
#15861=DIRECTION ( 'NONE',  ( -1.000000000000000000, 0.000000000000000000, -1.196361017915039239E-16 ) ) ;
#15862=DIRECTION ( 'NONE',  ( -5.968085353131216186E-17, -0.4999999999999999445, -0.8660254037844387076 ) ) ;
#15864=ADVANCED_FACE ( 'NONE', ( #17703 ), #1755, .T. ) ;
#15867=CARTESIAN_POINT ( 'NONE',  ( 3.460444912181559474, 49.25145096859824889, 90.49246380123798872 ) ) ;
#15868=LINE ( 'NONE', #6170, #4109 ) ;
#15869=EDGE_CURVE ( 'NONE', #19551, #1329, #3332, .T. ) ;
#15872=DIRECTION ( 'NONE',  ( -0.4999999999999983347, -0.8660254037844395958, -0.000000000000000000 ) ) ;
#15873=CARTESIAN_POINT ( 'NONE',  ( 4.987494971863720927, 47.58855820898865829, 90.02371380294498238 ) ) ;
#15881=CARTESIAN_POINT ( 'NONE',  ( 30.92220646078100188, 42.76218137147968434, 57.80715055817105252 ) ) ;
#15882=ORIENTED_EDGE ( 'NONE', *, *, #11078, .F. ) ;
#15883=CARTESIAN_POINT ( 'NONE',  ( -5.368445182934975968, 51.36218137147968577, 53.35433879953099989 ) ) ;
#15885=CARTESIAN_POINT ( 'NONE',  ( 1.352400422481993658, 50.46853102219002096, 94.32058880123798872 ) ) ;
#15886=DIRECTION ( 'NONE',  ( 0.000000000000000000, 0.000000000000000000, 1.000000000000000000 ) ) ;
#15893=EDGE_CURVE ( 'NONE', #15145, #13051, #14038, .T. ) ;
#15899=CARTESIAN_POINT ( 'NONE',  ( -0.3080929418689875576, 37.85583172076933778, 92.60183880123797451 ) ) ;
#15908=DIRECTION ( 'NONE',  ( -1.000000000000000000, -3.942553354492745503E-16, -0.000000000000000000 ) ) ;
#15909=CARTESIAN_POINT ( 'NONE',  ( -3.350035803220276609, 49.20851703305431357, 92.13308880123798872 ) ) ;
#15912=CARTESIAN_POINT ( 'NONE',  ( 10.77494014480653561, 42.76218137147968434, 74.20433879953100131 ) ) ;
#15917=VECTOR ( 'NONE', #15768, 1000.000000000000114 ) ;
#15934=VERTEX_POINT ( 'NONE', #17030 ) ;
#15942=CARTESIAN_POINT ( 'NONE',  ( -0.3080929418689875576, 37.85583172076933778, 91.35183880123798872 ) ) ;
#15951=DIRECTION ( 'NONE',  ( 0.000000000000000000, 0.000000000000000000, 1.000000000000000000 ) ) ;
#15955=( BOUNDED_CURVE ( )  B_SPLINE_CURVE ( 2, ( #1813, #1492, #1596, #18079, #17863, #8396, #3498, #10008, #14876, #14775, #13186, #19660, #19346, #297, #19557, #6472, #4977 ),
 .UNSPECIFIED., .F., .F. ) 
 B_SPLINE_CURVE_WITH_KNOTS ( ( 3, 2, 2, 2, 2, 2, 2, 2, 3 ),
 ( 0.3050440133814064092, 0.3124899283300235364, 0.3385307556908612181, 0.3645715830516987888, 0.3906124104125364149, 0.4166532377733740411, 0.4426940651342116118, 0.4687348924950492934, 0.4934533006542767275 ),
 .UNSPECIFIED. ) 
 CURVE ( )  GEOMETRIC_REPRESENTATION_ITEM ( )  RATIONAL_B_SPLINE_CURVE ( ( 0.9689162008616551969, 0.9782346958905645540, 1.000000000000000000, 0.9238795325112867385, 1.000000000000000000, 0.9238795325112867385, 1.000000000000000000, 0.9238795325112867385, 1.000000000000000000, 0.9238795325112867385, 1.000000000000000000, 0.9238795325112867385, 1.000000000000000000, 0.9238795325112867385, 1.000000000000000000, 0.9277451227418798130, 0.9926614284736728910 ) ) 
 REPRESENTATION_ITEM ( '' )  );
#15962=CARTESIAN_POINT ( 'NONE',  ( -3.638881865644721270, 47.35505628986900462, 93.82700776475003579 ) ) ;
#15966=DIRECTION ( 'NONE',  ( 1.193617070626243484E-16, 1.000000000000000000, 0.000000000000000000 ) ) ;
#15967=CARTESIAN_POINT ( 'NONE',  ( 11.22215374030650281, 42.96218137147968008, 69.40574467885102194 ) ) ;
#15969=EDGE_CURVE ( 'NONE', #15210, #5897, #17137, .T. ) ;
#15975=VECTOR ( 'NONE', #793, 1000.000000000000000 ) ;
#15978=CARTESIAN_POINT ( 'NONE',  ( -2.904223097202481174, 48.62752260303690122, 94.08621380294496817 ) ) ;
#15980=CARTESIAN_POINT ( 'NONE',  ( -1.854173455793826308, 49.13976469971947125, 94.80877693069184886 ) ) ;
#15982=VECTOR ( 'NONE', #1880, 1000.000000000000000 ) ;
#15997=VERTEX_POINT ( 'NONE', #18623 ) ;
#16001=CARTESIAN_POINT ( 'NONE',  ( -3.981178359372548492, 46.76218137147973408, 91.35183879953098085 ) ) ;
#16002=PLANE ( 'NONE',  #13220 ) ;
#16006=LINE ( 'NONE', #1426, #14700 ) ;
#16010=CARTESIAN_POINT ( 'NONE',  ( 2.263363662449363822, 49.77488197367694767, 93.19231768333818877 ) ) ;
#16011=ORIENTED_EDGE ( 'NONE', *, *, #4425, .T. ) ;
#16012=CARTESIAN_POINT ( 'NONE',  ( -4.927487955684009435, 43.24703606169091330, 92.55433879953093879 ) ) ;
#16013=DIRECTION ( 'NONE',  ( -1.000000000000000000, 0.000000000000000000, 0.000000000000000000 ) ) ;
#16017=EDGE_CURVE ( 'NONE', #1583, #2188, #5061, .T. ) ;
#16018=EDGE_CURVE ( 'NONE', #5376, #4661, #15439, .T. ) ;
#16021=FACE_OUTER_BOUND ( 'NONE', #9471, .T. ) ;
#16026=EDGE_LOOP ( 'NONE', ( #16036, #4083, #10065, #6935 ) ) ;
#16029=ORIENTED_EDGE ( 'NONE', *, *, #13078, .T. ) ;
#16034=ORIENTED_EDGE ( 'NONE', *, *, #8138, .F. ) ;
#16036=ORIENTED_EDGE ( 'NONE', *, *, #19690, .F. ) ;
#16047=LINE ( 'NONE', #1787, #9408 ) ;
#16050=CARTESIAN_POINT ( 'NONE',  ( 5.568489401881125289, 48.03437091500646261, 93.07058880123797451 ) ) ;
#16057=ORIENTED_EDGE ( 'NONE', *, *, #14662, .T. ) ;
#16059=CARTESIAN_POINT ( 'NONE',  ( -1.219056181836354558, 49.77488197367695477, 94.40612966814926210 ) ) ;
#16066=DIRECTION ( 'NONE',  ( 1.000000000000000000, 6.123233995736766036E-17, 0.000000000000000000 ) ) ;
#16068=VECTOR ( 'NONE', #6677, 1000.000000000000000 ) ;
#16080=ORIENTED_EDGE ( 'NONE', *, *, #2095, .F. ) ;
#16081=CARTESIAN_POINT ( 'NONE',  ( 11.22215374030650281, 45.56218137147968861, 62.80715055817104542 ) ) ;
#16086=CARTESIAN_POINT ( 'NONE',  ( 11.22215374030650281, 51.36218137147968577, 54.55433879953099563 ) ) ;
#16093=CARTESIAN_POINT ( 'NONE',  ( 5.611423337425062385, 41.22389019960463230, 95.17996380123798872 ) ) ;
#16094=CARTESIAN_POINT ( 'NONE',  ( -5.154188915835984375, 42.64120994080404614, 93.46121380123797451 ) ) ;
#16096=PLANE ( 'NONE',  #1167 ) ;
#16098=ADVANCED_FACE ( 'NONE', ( #1595 ), #17451, .F. ) ;
#16110=CARTESIAN_POINT ( 'NONE',  ( 5.595869095536538218, 45.91955541653086925, 92.55433879953098142 ) ) ;
#16111=ADVANCED_FACE ( 'NONE', ( #7663 ), #3189, .F. ) ;
#16112=CARTESIAN_POINT ( 'NONE',  ( -1.579458713576543882, 38.67424504380988282, 95.05433879952670395 ) ) ;
#16116=DIRECTION ( 'NONE',  ( -0.000000000000000000, 1.000000000000000000, 1.734723475976787531E-14 ) ) ;
#16127=EDGE_CURVE ( 'NONE', #5582, #19569, #7978, .T. ) ;
#16128=EDGE_CURVE ( 'NONE', #14841, #12731, #18675, .T. ) ;
#16139=VERTEX_POINT ( 'NONE', #14245 ) ;
#16144=CARTESIAN_POINT ( 'NONE',  ( 3.122153740306552905, 48.66551347115873227, 93.53933879953099506 ) ) ;
#16153=CARTESIAN_POINT ( 'NONE',  ( 0.000000000000000000, 0.000000000000000000, 0.000000000000000000 ) ) ;
#16158=PLANE ( 'NONE',  #3700 ) ;
#16161=DIRECTION ( 'NONE',  ( 0.000000000000000000, 0.000000000000000000, -1.000000000000000000 ) ) ;
#16162=EDGE_CURVE ( 'NONE', #5158, #20921, #14569, .T. ) ;
#16177=CARTESIAN_POINT ( 'NONE',  ( -3.350035803220276609, 49.20851703305431357, 93.22683880123798872 ) ) ;
#16188=LINE ( 'NONE', #11725, #12814 ) ;
#16189=LINE ( 'NONE', #11101, #19771 ) ;
#16190=ORIENTED_EDGE ( 'NONE', *, *, #7622, .F. ) ;
#16194=CARTESIAN_POINT ( 'NONE',  ( 5.611423337425062385, 41.22389019960463230, 91.42996380123798872 ) ) ;
#16201=CARTESIAN_POINT ( 'NONE',  ( 8.722153740306486824, 36.96218137147968719, 95.05433879953098142 ) ) ;
#16202=EDGE_LOOP ( 'NONE', ( #5927, #20794, #15828, #8284 ) ) ;
#16203=AXIS2_PLACEMENT_3D ( 'NONE', #7445, #8843, #5308 ) ;
#16206=CARTESIAN_POINT ( 'NONE',  ( -2.416137431568557314, 39.07291177436112406, 91.27371380123798872 ) ) ;
#16207=CARTESIAN_POINT ( 'NONE',  ( -4.567115856812060670, 47.10047254335474065, 94.55496380123798872 ) ) ;
#16208=ORIENTED_EDGE ( 'NONE', *, *, #120, .F. ) ;
#16212=CARTESIAN_POINT ( 'NONE',  ( 10.77494014480653561, 42.96218137147968008, 69.80574467885101342 ) ) ;
#16216=CARTESIAN_POINT ( 'NONE',  ( -4.477846259693498254, 50.66218137147966871, 54.55433879953098852 ) ) ;
#16218=ORIENTED_EDGE ( 'NONE', *, *, #16339, .F. ) ;
#16225=LINE ( 'NONE', #4825, #7488 ) ;
#16226=CARTESIAN_POINT ( 'NONE',  ( 5.611423337425062385, 41.22389019960463230, 90.17996380123798872 ) ) ;
#16229=ORIENTED_EDGE ( 'NONE', *, *, #12998, .T. ) ;
#16231=VECTOR ( 'NONE', #17116, 1000.000000000000000 ) ;
#16232=ORIENTED_EDGE ( 'NONE', *, *, #1302, .T. ) ;
#16233=LINE ( 'NONE', #12726, #1367 ) ;
#16234=LINE ( 'NONE', #17926, #8560 ) ;
#16239=CARTESIAN_POINT ( 'NONE',  ( -5.154188915835984375, 42.64120994080404614, 93.61746380123797451 ) ) ;
#16241=VERTEX_POINT ( 'NONE', #2007 ) ;
#16246=CARTESIAN_POINT ( 'NONE',  ( -2.904223097202481174, 48.62752260303690122, 96.27371379953099506 ) ) ;
#16260=PLANE ( 'NONE',  #3716 ) ;
#16264=AXIS2_PLACEMENT_3D ( 'NONE', #17168, #18766, #2590 ) ;
#16265=ORIENTED_EDGE ( 'NONE', *, *, #1977, .F. ) ;
#16270=EDGE_CURVE ( 'NONE', #9248, #15579, #15015, .T. ) ;
#16274=FACE_OUTER_BOUND ( 'NONE', #10241, .T. ) ;
#16277=FACE_OUTER_BOUND ( 'NONE', #19417, .T. ) ;
#16278=ADVANCED_FACE ( 'NONE', ( #16382 ), #8293, .F. ) ;
#16279=VECTOR ( 'NONE', #8096, 1000.000000000000000 ) ;
#16280=ADVANCED_FACE ( 'NONE', ( #10215 ), #16693, .F. ) ;
#16281=CARTESIAN_POINT ( 'NONE',  ( 4.394343283833276992, 39.11584570990505938, 93.85183880123797451 ) ) ;
#16288=VERTEX_POINT ( 'NONE', #934 ) ;
#16289=ORIENTED_EDGE ( 'NONE', *, *, #2896, .F. ) ;
#16296=ORIENTED_EDGE ( 'NONE', *, *, #120, .T. ) ;
#16300=CARTESIAN_POINT ( 'NONE',  ( -4.567115856812060670, 47.10047254335474065, 90.80496380123797451 ) ) ;
#16306=VECTOR ( 'NONE', #12434, 1000.000000000000114 ) ;
#16309=EDGE_LOOP ( 'NONE', ( #16833, #6689, #19984, #16265 ) ) ;
#16312=CARTESIAN_POINT ( 'NONE',  ( -2.503296703960768088, 48.49064145155251992, 92.86279910766216972 ) ) ;
#16313=VECTOR ( 'NONE', #12119, 1000.000000000000000 ) ;
#16314=CARTESIAN_POINT ( 'NONE',  ( 6.198496396448986090, 45.68315280215533392, 91.74246380123798872 ) ) ;
#16315=CARTESIAN_POINT ( 'NONE',  ( -0.4699484075730043786, 51.36218137147968577, 48.36106904222365444 ) ) ;
#16318=CARTESIAN_POINT ( 'NONE',  ( 0.5221537403065020788, 52.36218137147968577, 87.21440135111343750 ) ) ;
#16330=CARTESIAN_POINT ( 'NONE',  ( 0.5221537403065010796, 44.16218137147969003, 77.84651775085080772 ) ) ;
#16336=DIRECTION ( 'NONE',  ( 2.409338161078896715E-16, -1.000000000000000000, 0.000000000000000000 ) ) ;
#16339=EDGE_CURVE ( 'NONE', #4614, #16577, #4225, .T. ) ;
#16342=CARTESIAN_POINT ( 'NONE',  ( 30.92220646078100188, 42.76218137147968434, 62.80715055817104542 ) ) ;
#16343=LINE ( 'NONE', #7836, #13661 ) ;
#16344=VERTEX_POINT ( 'NONE', #3907 ) ;
#16355=EDGE_CURVE ( 'NONE', #12967, #7893, #12220, .T. ) ;
#16359=DIRECTION ( 'NONE',  ( 0.5735764363510442720, -0.8191520442889930198, -0.000000000000000000 ) ) ;
#16360=CARTESIAN_POINT ( 'NONE',  ( -5.784195910403845176, 44.99242805365518194, 94.63308880123798872 ) ) ;
#16367=ORIENTED_EDGE ( 'NONE', *, *, #15463, .T. ) ;
#16382=FACE_OUTER_BOUND ( 'NONE', #2236, .T. ) ;
#16386=CARTESIAN_POINT ( 'NONE',  ( 11.22215374030649926, 42.96218137147968008, 77.80433879953099563 ) ) ;
#16390=CARTESIAN_POINT ( 'NONE',  ( 5.568489401881125289, 48.03437091500646261, 91.66433880123796030 ) ) ;
#16394=ADVANCED_FACE ( 'NONE', ( #12116 ), #17192, .T. ) ;
#16396=ADVANCED_FACE ( 'NONE', ( #15498 ), #12094, .F. ) ;
#16400=VECTOR ( 'NONE', #4036, 1000.000000000000000 ) ;
#16402=ORIENTED_EDGE ( 'NONE', *, *, #11741, .T. ) ;
#16409=EDGE_LOOP ( 'NONE', ( #1143, #7708, #17198 ) ) ;
#16413=CARTESIAN_POINT ( 'NONE',  ( -0.9988176903691428077, 49.83852402762217082, 90.64871380123798872 ) ) ;
#16416=FACE_OUTER_BOUND ( 'NONE', #818, .T. ) ;
#16417=CIRCLE ( 'NONE', #18392, 6.200000000000000178 ) ;
#16420=EDGE_CURVE ( 'NONE', #3871, #3020, #7238, .T. ) ;
#16421=LINE ( 'NONE', #11738, #12486 ) ;
#16425=CARTESIAN_POINT ( 'NONE',  ( 2.043125170982144745, 38.48583871533720213, 91.42996380123798872 ) ) ;
#16426=FACE_OUTER_BOUND ( 'NONE', #19730, .T. ) ;
#16429=FACE_OUTER_BOUND ( 'NONE', #12985, .T. ) ;
#16433=CARTESIAN_POINT ( 'NONE',  ( 3.547567743947607877, 48.49067789217865254, 93.48725702289965511 ) ) ;
#16440=DIRECTION ( 'NONE',  ( 1.193617070626243484E-16, 1.000000000000000000, 0.000000000000000000 ) ) ;
#16444=DIRECTION ( 'NONE',  ( -0.000000000000000000, 1.000000000000000000, -0.000000000000000000 ) ) ;
#16445=AXIS2_PLACEMENT_3D ( 'NONE', #1648, #8243, #6416 ) ;
#16452=CARTESIAN_POINT ( 'NONE',  ( -5.058133621542618030, 44.89684013992257405, 96.42996379953098085 ) ) ;
#16455=ORIENTED_EDGE ( 'NONE', *, *, #18724, .F. ) ;
#16458=CARTESIAN_POINT ( 'NONE',  ( -4.500660556396669065, 42.81632233694663370, 94.00808879953098085 ) ) ;
#16461=ORIENTED_EDGE ( 'NONE', *, *, #6047, .F. ) ;
#16464=CARTESIAN_POINT ( 'NONE',  ( -5.154188915835984375, 42.64120994080404614, 94.71121380123797451 ) ) ;
#16473=CARTESIAN_POINT ( 'NONE',  ( 0.5221537403065097394, 44.16218137147969003, 111.0905869729573681 ) ) ;
#16488=CARTESIAN_POINT ( 'NONE',  ( -0.9988176903691428077, 49.83852402762217082, 91.89871380123798872 ) ) ;
#16489=CARTESIAN_POINT ( 'NONE',  ( 5.568489401881125289, 48.03437091500646261, 92.91433880123798872 ) ) ;
#16505=ORIENTED_EDGE ( 'NONE', *, *, #3385, .T. ) ;
#16512=CARTESIAN_POINT ( 'NONE',  ( 3.948530577815480225, 39.69684013992245752, 94.71121380294496817 ) ) ;
#16515=CARTESIAN_POINT ( 'NONE',  ( 6.198496396448986090, 45.68315280215533392, 95.33621380123798872 ) ) ;
#16526=CARTESIAN_POINT ( 'NONE',  ( -1.579458713576543882, 38.67424504380988282, 95.05433879952670395 ) ) ;
#16536=CARTESIAN_POINT ( 'NONE',  ( -3.154801521863568325, 47.83913663364972280, 95.05036078214054385 ) ) ;
#16538=DIRECTION ( 'NONE',  ( 1.000000000000000000, 1.402518428993831676E-16, 0.000000000000000000 ) ) ;
#16543=AXIS2_PLACEMENT_3D ( 'NONE', #6889, #2004, #8501 ) ;
#16547=ORIENTED_EDGE ( 'NONE', *, *, #3197, .F. ) ;
#16550=CARTESIAN_POINT ( 'NONE',  ( -3.981178359372548492, 46.76218137147973408, 92.60183879953099506 ) ) ;
#16553=CARTESIAN_POINT ( 'NONE',  ( -4.477846259693498254, 37.66218137147969713, 54.55433879953098852 ) ) ;
#16555=CARTESIAN_POINT ( 'NONE',  ( -3.777846259693486974, 51.36218137147968577, 53.35433879953099279 ) ) ;
#16557=ORIENTED_EDGE ( 'NONE', *, *, #8841, .T. ) ;
#16559=VECTOR ( 'NONE', #560, 1000.000000000000000 ) ;
#16560=VERTEX_POINT ( 'NONE', #13974 ) ;
#16564=EDGE_CURVE ( 'NONE', #5867, #12858, #7483, .T. ) ;
#16572=VERTEX_POINT ( 'NONE', #1205 ) ;
#16573=FACE_OUTER_BOUND ( 'NONE', #3455, .T. ) ;
#16577=VERTEX_POINT ( 'NONE', #9305 ) ;
#16580=ORIENTED_EDGE ( 'NONE', *, *, #18103, .F. ) ;
#16582=CIRCLE ( 'NONE', #7402, 4.200000000000001066 ) ;
#16589=LINE ( 'NONE', #3599, #16313 ) ;
#16590=LINE ( 'NONE', #16386, #5792 ) ;
#16591=CARTESIAN_POINT ( 'NONE',  ( -3.350035803220276609, 49.20851703305431357, 93.22683880123798872 ) ) ;
#16592=CARTESIAN_POINT ( 'NONE',  ( 6.198496396448986090, 45.68315280215533392, 94.08621380123798872 ) ) ;
#16593=VERTEX_POINT ( 'NONE', #12387 ) ;
#16599=CARTESIAN_POINT ( 'NONE',  ( -0.3080929418689875576, 37.85583172076933778, 93.85183880123797451 ) ) ;
#16600=EDGE_CURVE ( 'NONE', #10780, #15934, #4538, .T. ) ;
#16602=DIRECTION ( 'NONE',  ( -0.000000000000000000, -0.000000000000000000, 1.000000000000000000 ) ) ;
#16605=ORIENTED_EDGE ( 'NONE', *, *, #6375, .T. ) ;
#16607=LINE ( 'NONE', #19472, #8054 ) ;
#16611=ADVANCED_FACE ( 'NONE', ( #12788 ), #10113, .T. ) ;
#16612=VECTOR ( 'NONE', #8785, 1000.000000000000000 ) ;
#16616=CARTESIAN_POINT ( 'NONE',  ( -5.058133621542618030, 44.89684013992257405, 94.24246380294498238 ) ) ;
#16619=CARTESIAN_POINT ( 'NONE',  ( 1.352400422481993658, 50.46853102219002096, 95.57058880123798872 ) ) ;
#16626=CARTESIAN_POINT ( 'NONE',  ( 5.611423337425062385, 41.22389019960463230, 95.17996380123798872 ) ) ;
#16627=( BOUNDED_CURVE ( )  B_SPLINE_CURVE ( 2, ( #6359, #7973, #11493, #10003, #17965 ),
 .UNSPECIFIED., .F., .F. ) 
 B_SPLINE_CURVE_WITH_KNOTS ( ( 3, 2, 3 ),
 ( 0.3212199771556245032, 0.3385307364581348621, 0.3472607999482700269 ),
 .UNSPECIFIED. ) 
 CURVE ( )  GEOMETRIC_REPRESENTATION_ITEM ( )  RATIONAL_B_SPLINE_CURVE ( ( 0.9660722070856944121, 0.9493985675917804290, 1.000000000000000000, 0.9744809739482959143, 0.9660722130358361248 ) ) 
 REPRESENTATION_ITEM ( '' )  );
#16628=EDGE_LOOP ( 'NONE', ( #11310, #7179, #11519, #11619, #8886, #17956, #7867, #2911, #12703, #15882, #5260, #19446 ) ) ;
#16633=CARTESIAN_POINT ( 'NONE',  ( 10.77494014480653561, 42.96218137147968008, 65.80574467885102763 ) ) ;
#16647=ORIENTED_EDGE ( 'NONE', *, *, #18945, .F. ) ;
#16651=ORIENTED_EDGE ( 'NONE', *, *, #11333, .T. ) ;
#16655=CARTESIAN_POINT ( 'NONE',  ( -2.904223097202481174, 48.62752260303690122, 93.77371379953099506 ) ) ;
#16660=ORIENTED_EDGE ( 'NONE', *, *, #1771, .F. ) ;
#16668=ORIENTED_EDGE ( 'NONE', *, *, #4652, .F. ) ;
#16671=ADVANCED_FACE ( 'NONE', ( #16277 ), #4463, .F. ) ;
#16672=SHAPE_REPRESENTATION_RELATIONSHIP ( 'NONE' , 'NONE' ,  #333, #2752 ) ;
#16680=VERTEX_POINT ( 'NONE', #13086 ) ;
#16683=CARTESIAN_POINT ( 'NONE',  ( -4.567115856812060670, 47.10047254335474065, 93.46121380123797451 ) ) ;
#16684=VERTEX_POINT ( 'NONE', #7984 ) ;
#16688=EDGE_LOOP ( 'NONE', ( #12165, #20594, #304, #1244, #11190, #15322, #14538, #6176, #7575, #250, #11253, #18849 ) ) ;
#16693=PLANE ( 'NONE',  #10335 ) ;
#16696=CARTESIAN_POINT ( 'NONE',  ( -1.218186307993492257, 38.53589529967373295, 92.55433879953098142 ) ) ;
#16699=CARTESIAN_POINT ( 'NONE',  ( 6.828503391016846891, 43.33193468930419101, 92.75808880123800293 ) ) ;
#16706=LINE ( 'NONE', #420, #4464 ) ;
#16708=CARTESIAN_POINT ( 'NONE',  ( -3.350035803220276609, 49.20851703305431357, 94.63308880123798872 ) ) ;
#16713=VERTEX_POINT ( 'NONE', #9481 ) ;
#16716=CARTESIAN_POINT ( 'NONE',  ( 5.722153740306498371, 44.16218137147968292, 94.58161078214052964 ) ) ;
#16719=AXIS2_PLACEMENT_3D ( 'NONE', #2228, #3706, #10338 ) ;
#16720=CARTESIAN_POINT ( 'NONE',  ( -4.531772010406379003, 45.91993734822838036, 95.05433879953099563 ) ) ;
#16722=CARTESIAN_POINT ( 'NONE',  ( -3.981178359372548492, 46.76218137147973408, 91.66433880294496817 ) ) ;
#16725=CARTESIAN_POINT ( 'NONE',  ( 6.828503391016846891, 43.33193468930419101, 94.00808880123798872 ) ) ;
#16729=VECTOR ( 'NONE', #16739, 1000.000000000000000 ) ;
#16730=CARTESIAN_POINT ( 'NONE',  ( 31.22215374030650281, 42.76218137147968434, 73.80433879953100984 ) ) ;
#16733=CARTESIAN_POINT ( 'NONE',  ( 3.460444912181559474, 49.25145096859824889, 90.49246380123798872 ) ) ;
#16736=CARTESIAN_POINT ( 'NONE',  ( 5.722153740305851777, 42.76884557083668881, 94.52737681315549878 ) ) ;
#16739=DIRECTION ( 'NONE',  ( -1.000000000000000000, -1.213411507412056509E-16, 0.000000000000000000 ) ) ;
#16742=VECTOR ( 'NONE', #3432, 1000.000000000000114 ) ;
#16747=EDGE_CURVE ( 'NONE', #15667, #17279, #2975, .T. ) ;
#16748=DIRECTION ( 'NONE',  ( -0.000000000000000000, -0.000000000000000000, 1.000000000000000000 ) ) ;
#16759=CARTESIAN_POINT ( 'NONE',  ( 3.948530577815480225, 39.69684013992245752, 93.14871379953099506 ) ) ;
#16760=CARTESIAN_POINT ( 'NONE',  ( 5.544968037009670780, 45.50804040601273925, 92.13308879953099506 ) ) ;
#16772=DIRECTION ( 'NONE',  ( 1.402518428993831676E-16, -1.000000000000000000, 0.000000000000000000 ) ) ;
#16774=EDGE_CURVE ( 'NONE', #13434, #18535, #8794, .T. ) ;
#16776=VECTOR ( 'NONE', #7421, 1000.000000000000000 ) ;
#16780=ORIENTED_EDGE ( 'NONE', *, *, #15869, .F. ) ;
#16785=LINE ( 'NONE', #18479, #11894 ) ;
#16787=PLANE ( 'NONE',  #10964 ) ;
#16790=AXIS2_PLACEMENT_3D ( 'NONE', #10906, #12485, #2906 ) ;
#16803=CARTESIAN_POINT ( 'NONE',  ( -0.8237052942265477018, 49.18499566818285018, 95.25808880294498238 ) ) ;
#16805=ORIENTED_EDGE ( 'NONE', *, *, #4411, .T. ) ;
#16813=CARTESIAN_POINT ( 'NONE',  ( -0.9988176903691428077, 49.83852402762217082, 95.80496380123798872 ) ) ;
#16815=LINE ( 'NONE', #10233, #3822 ) ;
#16816=CARTESIAN_POINT ( 'NONE',  ( -3.350035803220276609, 49.20851703305431357, 90.88308880123797451 ) ) ;
#16818=VERTEX_POINT ( 'NONE', #9331 ) ;
#16823=ORIENTED_EDGE ( 'NONE', *, *, #19132, .F. ) ;
#16825=CARTESIAN_POINT ( 'NONE',  ( -4.942049829789907811, 43.24669937789425234, 95.05433879953095300 ) ) ;
#16827=CARTESIAN_POINT ( 'NONE',  ( 3.122153740306552905, 48.66551347115873227, 93.85183880294498238 ) ) ;
#16831=CARTESIAN_POINT ( 'NONE',  ( 6.828503391016846891, 43.33193468930419101, 95.25808880123800293 ) ) ;
#16833=ORIENTED_EDGE ( 'NONE', *, *, #11967, .F. ) ;
#16837=CARTESIAN_POINT ( 'NONE',  ( -5.154188915835984375, 42.64120994080404614, 93.46121380123797451 ) ) ;
#16838=ORIENTED_EDGE ( 'NONE', *, *, #14440, .T. ) ;
#16839=CARTESIAN_POINT ( 'NONE',  ( 2.228068668033876154, 49.81017696809242778, 92.55433879953098142 ) ) ;
#16848=EDGE_CURVE ( 'NONE', #9648, #7336, #4305, .T. ) ;
#16860=CARTESIAN_POINT ( 'NONE',  ( 3.122153740306552905, 48.66551347115873227, 92.28933879953099506 ) ) ;
#16861=CARTESIAN_POINT ( 'NONE',  ( -0.8237052942265477018, 49.18499566818285018, 96.19558879953099506 ) ) ;
#16862=PRODUCT_DEFINITION_SHAPE ( 'NONE', 'NONE',  #14822 ) ;
#16865=CARTESIAN_POINT ( 'NONE',  ( 30.92220646078100188, 42.96218137147968008, 61.40715055817103263 ) ) ;
#16870=ORIENTED_EDGE ( 'NONE', *, *, #14354, .T. ) ;
#16872=CARTESIAN_POINT ( 'NONE',  ( 5.611423337425062385, 41.22389019960463230, 95.33621380123798872 ) ) ;
#16875=CARTESIAN_POINT ( 'NONE',  ( 6.828503391016846891, 43.33193468930419101, 90.25808880123800293 ) ) ;
#16878=ADVANCED_FACE ( 'NONE', ( #16021 ), #3338, .F. ) ;
#16879=LINE ( 'NONE', #2297, #13307 ) ;
#16880=DIRECTION ( 'NONE',  ( -1.334402673828310381E-16, -2.168404344970984808E-15, 1.000000000000000000 ) ) ;
#16884=CARTESIAN_POINT ( 'NONE',  ( -12.18117835937254867, 39.56218137147966019, 45.55433879953098852 ) ) ;
#16888=AXIS2_PLACEMENT_3D ( 'NONE', #316, #14, #13101 ) ;
#16890=EDGE_LOOP ( 'NONE', ( #1653, #10422, #638, #12642 ) ) ;
#16891=LINE ( 'NONE', #7086, #9792 ) ;
#16894=CYLINDRICAL_SURFACE ( 'NONE', #6996, 4.200000000000001066 ) ;
#16897=CARTESIAN_POINT ( 'NONE',  ( -0.9988176903691428077, 49.83852402762217082, 94.55496380123798872 ) ) ;
#16901=CARTESIAN_POINT ( 'NONE',  ( 3.948530577815480225, 39.69684013992245752, 92.21121380294495395 ) ) ;
#16903=CARTESIAN_POINT ( 'NONE',  ( -7.677846259693483333, 47.36218137147966445, 45.55433879953098852 ) ) ;
#16907=FACE_OUTER_BOUND ( 'NONE', #18286, .T. ) ;
#16908=CARTESIAN_POINT ( 'NONE',  ( -4.567115856812060670, 47.10047254335474065, 94.71121380123797451 ) ) ;
#16910=CIRCLE ( 'NONE', #3644, 6.200000000000000178 ) ;
#16913=CARTESIAN_POINT ( 'NONE',  ( 11.22215374030650281, 42.96218137147968008, 74.20433879953100131 ) ) ;
#16917=AXIS2_PLACEMENT_3D ( 'NONE', #7144, #15249, #2369 ) ;
#16921=ADVANCED_FACE ( 'NONE', ( #19510 ), #8131, .F. ) ;
#16923=CARTESIAN_POINT ( 'NONE',  ( -2.416137431568557314, 39.07291177436112406, 95.02371380123797451 ) ) ;
#16930=CARTESIAN_POINT ( 'NONE',  ( -0.3080929418689875576, 37.85583172076933778, 94.94558880123797451 ) ) ;
#16936=CARTESIAN_POINT ( 'NONE',  ( -2.077846259693550746, 39.65884927180063357, 94.47683880294496817 ) ) ;
#16955=PLANE ( 'NONE',  #1087 ) ;
#16960=CARTESIAN_POINT ( 'NONE',  ( 33.61275266354798674, 51.36218137147967866, 92.39963826115175038 ) ) ;
#16961=CARTESIAN_POINT ( 'NONE',  ( -3.981178359372548492, 46.76218137147973408, 93.85183879953099506 ) ) ;
#16962=CARTESIAN_POINT ( 'NONE',  ( -4.500660556396669065, 42.81632233694663370, 91.50808879953098085 ) ) ;
#16965=CARTESIAN_POINT ( 'NONE',  ( -2.416137431568557314, 39.07291177436112406, 92.52371380123797451 ) ) ;
#16969=ORIENTED_EDGE ( 'NONE', *, *, #18869, .T. ) ;
#16985=VECTOR ( 'NONE', #2360, 1000.000000000000000 ) ;
#16989=CARTESIAN_POINT ( 'NONE',  ( -2.416137431568557314, 39.07291177436112406, 95.02371380123797451 ) ) ;
#17002=CARTESIAN_POINT ( 'NONE',  ( -4.567115856812060670, 47.10047254335474065, 95.96121380123798872 ) ) ;
#17005=CARTESIAN_POINT ( 'NONE',  ( 31.07218010054375412, 45.56218137147968861, 70.80574467885102763 ) ) ;
#17006=CARTESIAN_POINT ( 'NONE',  ( -4.677846259693496656, 44.16218127507082158, 94.26911326394257173 ) ) ;
#17007=CARTESIAN_POINT ( 'NONE',  ( -0.8237052942265477018, 49.18499566818285018, 91.50808880294498238 ) ) ;
#17008=AXIS2_PLACEMENT_3D ( 'NONE', #18039, #13458, #8465 ) ;
#17010=DIRECTION ( 'NONE',  ( -0.000000000000000000, -0.000000000000000000, 1.000000000000000000 ) ) ;
#17013=ORIENTED_EDGE ( 'NONE', *, *, #13676, .T. ) ;
#17015=DIRECTION ( 'NONE',  ( -1.000000000000000000, 1.193617070626243484E-16, 0.000000000000000000 ) ) ;
#17017=CARTESIAN_POINT ( 'NONE',  ( 5.611423337425062385, 41.22389019960463230, 92.83621380123797451 ) ) ;
#17019=DIRECTION ( 'NONE',  ( -1.000000000000000000, -1.402518428993831676E-16, -1.196361017915039239E-16 ) ) ;
#17022=CARTESIAN_POINT ( 'NONE',  ( 11.22215374030650281, 42.96218137147968008, 61.80715055817104542 ) ) ;
#17023=ORIENTED_EDGE ( 'NONE', *, *, #13038, .F. ) ;
#17025=EDGE_CURVE ( 'NONE', #1059, #5621, #9330, .T. ) ;
#17029=CARTESIAN_POINT ( 'NONE',  ( 1.514255888186008425, 52.36218137147968577, 48.36106904222365444 ) ) ;
#17030=CARTESIAN_POINT ( 'NONE',  ( 24.32215374030650068, 44.16218137147968292, 93.55433879953098142 ) ) ;
#17033=CARTESIAN_POINT ( 'NONE',  ( 1.868012774839550749, 39.13936707477651566, 92.13308880294498238 ) ) ;
#17040=CARTESIAN_POINT ( 'NONE',  ( -4.567115856812060670, 47.10047254335474065, 92.05496380123798872 ) ) ;
#17042=DIRECTION ( 'NONE',  ( 1.000000000000000000, -0.000000000000000000, -0.000000000000000000 ) ) ;
#17043=CARTESIAN_POINT ( 'NONE',  ( 0.5221537403065019678, 51.36218137147968577, 52.53721119516358584 ) ) ;
#17048=DIRECTION ( 'NONE',  ( -1.000000000000000000, 0.000000000000000000, -0.000000000000000000 ) ) ;
#17050=CARTESIAN_POINT ( 'NONE',  ( 3.460444912181559474, 49.25145096859824889, 91.74246380123798872 ) ) ;
#17053=DIRECTION ( 'NONE',  ( 1.402518428993831676E-16, -1.000000000000000000, 1.677918375355662166E-32 ) ) ;
#17055=DIRECTION ( 'NONE',  ( -1.000000000000000000, -1.402518428993831676E-16, -1.196361017915039239E-16 ) ) ;
#17064=CARTESIAN_POINT ( 'NONE',  ( 31.07218010054375412, 42.76218137147968434, 70.80574467885102763 ) ) ;
#17066=CARTESIAN_POINT ( 'NONE',  ( 2.263363662449358493, 49.77488197367694767, 94.36419268333823140 ) ) ;
#17077=CARTESIAN_POINT ( 'NONE',  ( -0.8237052942265477018, 49.18499566818285018, 92.44558879953099506 ) ) ;
#17079=CARTESIAN_POINT ( 'NONE',  ( 2.043125170982144745, 38.48583871533720213, 95.17996380123798872 ) ) ;
#17080=CARTESIAN_POINT ( 'NONE',  ( 2.492135536370527316, 38.60615068013622420, 95.03863327408673456 ) ) ;
#17082=VECTOR ( 'NONE', #19105, 1000.000000000000000 ) ;
#17083=CARTESIAN_POINT ( 'NONE',  ( 4.199109002476567376, 47.83913663364971569, 83.28180655319408743 ) ) ;
#17086=VECTOR ( 'NONE', #3906, 1000.000000000000000 ) ;
#17088=CARTESIAN_POINT ( 'NONE',  ( 11.22215374030650281, 42.96218137147968008, 73.80433879953100984 ) ) ;
#17089=CARTESIAN_POINT ( 'NONE',  ( 5.568489401881125289, 48.03437091500646261, 95.57058880123798872 ) ) ;
#17098=FACE_OUTER_BOUND ( 'NONE', #456, .T. ) ;
#17104=CARTESIAN_POINT ( 'NONE',  ( 6.828503391016846891, 43.33193468930419101, 95.25808880123800293 ) ) ;
#17107=ORIENTED_EDGE ( 'NONE', *, *, #14354, .F. ) ;
#17116=DIRECTION ( 'NONE',  ( 0.000000000000000000, 1.000000000000000000, 0.000000000000000000 ) ) ;
#17117=DIRECTION ( 'NONE',  ( -0.000000000000000000, -2.168404344970984413E-15, -1.000000000000000000 ) ) ;
#17118=CARTESIAN_POINT ( 'NONE',  ( 5.025485839985549319, 41.56218137147963887, 91.03933880294498238 ) ) ;
#17136=DIRECTION ( 'NONE',  ( -1.000000000000000000, -1.402518428993831676E-16, -1.196361017915039239E-16 ) ) ;
#17137=LINE ( 'NONE', #13623, #7932 ) ;
#17140=CARTESIAN_POINT ( 'NONE',  ( -0.2125050281363792815, 38.58189400963055959, 92.05496380294498238 ) ) ;
#17148=ADVANCED_FACE ( 'NONE', ( #16416 ), #9932, .F. ) ;
#17151=CARTESIAN_POINT ( 'NONE',  ( -3.981178359372548492, 46.76218137147973408, 91.66433880294496817 ) ) ;
#17162=ORIENTED_EDGE ( 'NONE', *, *, #8291, .F. ) ;
#17163=DIRECTION ( 'NONE',  ( 1.000000000000000000, -1.193617070626243484E-16, 0.000000000000000000 ) ) ;
#17165=ADVANCED_FACE ( 'NONE', ( #17684 ), #16096, .F. ) ;
#17168=CARTESIAN_POINT ( 'NONE',  ( 31.07218010054375412, 45.56218137147968861, 64.80574467885102763 ) ) ;
#17174=DIRECTION ( 'NONE',  ( 1.000000000000000000, -0.000000000000000000, -0.000000000000000000 ) ) ;
#17175=CARTESIAN_POINT ( 'NONE',  ( -5.058133621542618030, 44.89684013992257405, 96.42996379953098085 ) ) ;
#17179=CARTESIAN_POINT ( 'NONE',  ( 5.568489401881125289, 48.03437091500646261, 91.82058880123797451 ) ) ;
#17190=DIRECTION ( 'NONE',  ( 1.000000000000000000, -0.000000000000000000, -0.000000000000000000 ) ) ;
#17192=( BOUNDED_SURFACE ( )  B_SPLINE_SURFACE ( 1, 2, ( 
 ( #9034, #13490, #15198, #15520, #17002, #6984, #19962, #13915, #10326, #20398, #2431, #5829, #724, #13708, #7318, #20074, #5391, #18815, #2319, #10431, #12022, #18496, #16897, #11910, #8815, #20183, #18385, #5613, #8928, #15417, #9456, #4543, #11158, #7745, #14227, #6341, #2951, #1472, #19021, #20815, #7956, #16050, #12435, #9356, #12746, #15841, #17627, #15738, #1050, #3171, #19323, #14439, #11057, #7535, #11268, #20910, #12646, #1158, #20705, #17324, #15628, #17530, #14341, #15942, #14024, #12845, #17739, #4328, #4739, #20606, #20507, #10955, #6243, #7643, #14124, #1253, #1364, #3060, #7855, #5938, #6144 ),
 ( #9252, #19128, #19222, #4639, #10856, #9567, #2747, #4442, #6034, #12535, #17428, #2853, #14961, #17842, #176, #9674, #13163, #9985, #16464, #16360, #1790, #11681, #10081, #6446, #9769, #1677, #6556, #13063, #4954, #1885, #17945, #3366, #9877, #8271, #14755, #5747, #4741, #14548, #4150, #5860, #1575, #4248, #1182, #17239, #6342, #7565, #21013, #6447, #538, #5217, #8852, #4119, #14027, #10434, #7207, #7068, #9114, #703, #3987, #18362, #15396, #2193, #15602, #7183, #2295, #8691, #20050, #10299, #20257, #5483, #11998, #7511, #18468, #3885, #10407, #16875, #13684, #5368, #20160, #1018, #9012 ) ),
 .UNSPECIFIED., .F., .F., .F. ) 
 B_SPLINE_SURFACE_WITH_KNOTS ( ( 2, 2 ),
 ( 3, 2, 2, 2, 2, 2, 2, 2, 2, 2, 2, 2, 2, 2, 2, 2, 2, 2, 2, 2, 2, 2, 2, 2, 2, 2, 2, 2, 2, 2, 2, 2, 2, 2, 2, 2, 2, 2, 2, 2, 3 ),
 ( 0.000000000000000000, 1.000000000000000000 ),
 ( 0.000000000000000000, 0.02500000000000000139, 0.05000000000000000278, 0.07499999999999999722, 0.1000000000000000056, 0.1250000000000000000, 0.1499999999999999944, 0.1749999999999999889, 0.2000000000000000111, 0.2250000000000000056, 0.2500000000000000000, 0.2750000000000000222, 0.2999999999999999889, 0.3250000000000000111, 0.3499999999999999778, 0.3750000000000000000, 0.4000000000000000222, 0.4249999999999999889, 0.4500000000000000111, 0.4749999999999999778, 0.5000000000000000000, 0.5250000000000000222, 0.5500000000000000444, 0.5749999999999999556, 0.5999999999999999778, 0.6250000000000000000, 0.6500000000000000222, 0.6750000000000000444, 0.6999999999999999556, 0.7249999999999999778, 0.7500000000000000000, 0.7750000000000000222, 0.8000000000000000444, 0.8249999999999999556, 0.8499999999999999778, 0.8750000000000000000, 0.9000000000000000222, 0.9250000000000000444, 0.9499999999999999556, 0.9600309411673831894, 0.9696312505790569691 ),
 .UNSPECIFIED. ) 
 GEOMETRIC_REPRESENTATION_ITEM ( )  RATIONAL_B_SPLINE_SURFACE ( (
 ( 1.000000000000000000, 0.9238795325112867385, 1.000000000000000000, 0.9238795325112867385, 1.000000000000000000, 0.9238795325112867385, 1.000000000000000000, 0.9238795325112867385, 1.000000000000000000, 0.9238795325112867385, 1.000000000000000000, 0.9238795325112867385, 1.000000000000000000, 0.9238795325112867385, 1.000000000000000000, 0.9238795325112867385, 1.000000000000000000, 0.9238795325112867385, 1.000000000000000000, 0.9238795325112867385, 1.000000000000000000, 0.9238795325112867385, 1.000000000000000000, 0.9238795325112867385, 1.000000000000000000, 0.9238795325112867385, 1.000000000000000000, 0.9238795325112867385, 1.000000000000000000, 0.9238795325112867385, 1.000000000000000000, 0.9238795325112867385, 1.000000000000000000, 0.9238795325112867385, 1.000000000000000000, 0.9238795325112867385, 1.000000000000000000, 0.9238795325112867385, 1.000000000000000000, 0.9238795325112867385, 1.000000000000000000, 0.9238795325112867385, 1.000000000000000000, 0.9238795325112867385, 1.000000000000000000, 0.9238795325112867385, 1.000000000000000000, 0.9238795325112867385, 1.000000000000000000, 0.9238795325112867385, 1.000000000000000000, 0.9238795325112867385, 1.000000000000000000, 0.9238795325112867385, 1.000000000000000000, 0.9238795325112867385, 1.000000000000000000, 0.9238795325112867385, 1.000000000000000000, 0.9238795325112867385, 1.000000000000000000, 0.9238795325112867385, 1.000000000000000000, 0.9238795325112867385, 1.000000000000000000, 0.9238795325112867385, 1.000000000000000000, 0.9238795325112867385, 1.000000000000000000, 0.9238795325112867385, 1.000000000000000000, 0.9238795325112867385, 1.000000000000000000, 0.9238795325112867385, 1.000000000000000000, 0.9238795325112867385, 1.000000000000000000, 0.9694576027594803413, 0.9634247247054007479, 0.9634247247054007479, 0.9634247247054007479),
 ( 1.000000000000000000, 0.9238795325112867385, 1.000000000000000000, 0.9238795325112867385, 1.000000000000000000, 0.9238795325112867385, 1.000000000000000000, 0.9238795325112867385, 1.000000000000000000, 0.9238795325112867385, 1.000000000000000000, 0.9238795325112867385, 1.000000000000000000, 0.9238795325112867385, 1.000000000000000000, 0.9238795325112867385, 1.000000000000000000, 0.9238795325112867385, 1.000000000000000000, 0.9238795325112867385, 1.000000000000000000, 0.9238795325112867385, 1.000000000000000000, 0.9238795325112867385, 1.000000000000000000, 0.9238795325112867385, 1.000000000000000000, 0.9238795325112867385, 1.000000000000000000, 0.9238795325112867385, 1.000000000000000000, 0.9238795325112867385, 1.000000000000000000, 0.9238795325112867385, 1.000000000000000000, 0.9238795325112867385, 1.000000000000000000, 0.9238795325112867385, 1.000000000000000000, 0.9238795325112867385, 1.000000000000000000, 0.9238795325112867385, 1.000000000000000000, 0.9238795325112867385, 1.000000000000000000, 0.9238795325112867385, 1.000000000000000000, 0.9238795325112867385, 1.000000000000000000, 0.9238795325112867385, 1.000000000000000000, 0.9238795325112867385, 1.000000000000000000, 0.9238795325112867385, 1.000000000000000000, 0.9238795325112867385, 1.000000000000000000, 0.9238795325112867385, 1.000000000000000000, 0.9238795325112867385, 1.000000000000000000, 0.9238795325112867385, 1.000000000000000000, 0.9238795325112867385, 1.000000000000000000, 0.9238795325112867385, 1.000000000000000000, 0.9238795325112867385, 1.000000000000000000, 0.9238795325112867385, 1.000000000000000000, 0.9238795325112867385, 1.000000000000000000, 0.9238795325112867385, 1.000000000000000000, 0.9238795325112867385, 1.000000000000000000, 0.9694576027594803413, 0.9634247247054007479, 0.9634247247054007479, 0.9634247247054007479) ) ) 
 REPRESENTATION_ITEM ( '' )  SURFACE ( )  );
#17198=ORIENTED_EDGE ( 'NONE', *, *, #11818, .T. ) ;
#17202=CARTESIAN_POINT ( 'NONE',  ( 4.199109002476567376, 47.83913663364971569, 95.05433879953098142 ) ) ;
#17203=CARTESIAN_POINT ( 'NONE',  ( -4.524181921268124462, 40.28999182795290324, 91.19558880123797451 ) ) ;
#17210=VECTOR ( 'NONE', #19164, 1000.000000000000000 ) ;
#17219=CARTESIAN_POINT ( 'NONE',  ( -4.500660556396669065, 42.81632233694663370, 94.32058880294496817 ) ) ;
#17220=CARTESIAN_POINT ( 'NONE',  ( -4.500660556396669065, 42.81632233694663370, 90.57058880294496817 ) ) ;
#17226=DIRECTION ( 'NONE',  ( 1.000000000000000000, 2.838338907332122006E-16, -0.000000000000000000 ) ) ;
#17234=CARTESIAN_POINT ( 'NONE',  ( -1.579458713576543882, 38.67424504380988282, 95.05433879952670395 ) ) ;
#17238=LINE ( 'NONE', #2664, #7757 ) ;
#17239=CARTESIAN_POINT ( 'NONE',  ( 6.828503391016846891, 43.33193468930419101, 92.75808880123800293 ) ) ;
#17241=DIRECTION ( 'NONE',  ( -0.000000000000000000, -0.000000000000000000, 1.000000000000000000 ) ) ;
#17249=VECTOR ( 'NONE', #980, 1000.000000000000000 ) ;
#17252=CARTESIAN_POINT ( 'NONE',  ( 5.544968037009670780, 45.50804040601273925, 92.44558880294498238 ) ) ;
#17258=CARTESIAN_POINT ( 'NONE',  ( 0.5221537403065010796, 44.16218137147969003, 77.84651775085080772 ) ) ;
#17261=ORIENTED_EDGE ( 'NONE', *, *, #1603, .T. ) ;
#17263=AXIS2_PLACEMENT_3D ( 'NONE', #12670, #18937, #2974 ) ;
#17264=ORIENTED_EDGE ( 'NONE', *, *, #18475, .T. ) ;
#17267=PLANE ( 'NONE',  #950 ) ;
#17268=CARTESIAN_POINT ( 'NONE',  ( 5.611423337425062385, 41.22389019960463230, 95.17996380123798872 ) ) ;
#17274=VECTOR ( 'NONE', #780, 1000.000000000000227 ) ;
#17275=ORIENTED_EDGE ( 'NONE', *, *, #1836, .T. ) ;
#17276=CARTESIAN_POINT ( 'NONE',  ( 10.77494014480653561, 42.96218137147968008, 77.80433879953099563 ) ) ;
#17277=CARTESIAN_POINT ( 'NONE',  ( 3.460444912181559474, 49.25145096859824889, 93.14871380123798872 ) ) ;
#17279=VERTEX_POINT ( 'NONE', #361 ) ;
#17280=CARTESIAN_POINT ( 'NONE',  ( 2.043125170982144745, 38.48583871533720213, 92.67996380123798872 ) ) ;
#17282=CARTESIAN_POINT ( 'NONE',  ( 30.92220646078100188, 42.76218137147968434, 56.80715055817104542 ) ) ;
#17291=CARTESIAN_POINT ( 'NONE',  ( -0.4699484075729999932, 51.36218137147968577, 83.03825919817350609 ) ) ;
#17293=VECTOR ( 'NONE', #9168, 1000.000000000000000 ) ;
#17297=ADVANCED_FACE ( 'NONE', ( #11557 ), #6849, .F. ) ;
#17306=CARTESIAN_POINT ( 'NONE',  ( 1.352400422481993658, 50.46853102219002096, 90.72683880123797451 ) ) ;
#17308=CARTESIAN_POINT ( 'NONE',  ( 11.22215374030649926, 48.36218137147968577, 80.55433879953099563 ) ) ;
#17310=VECTOR ( 'NONE', #3538, 1000.000000000000000 ) ;
#17324=CARTESIAN_POINT ( 'NONE',  ( 6.828503391016846891, 43.33193468930419101, 91.66433880123796030 ) ) ;
#17326=VECTOR ( 'NONE', #18247, 1000.000000000000000 ) ;
#17328=CARTESIAN_POINT ( 'NONE',  ( 3.122153740306552905, 48.66551347115873227, 95.10183880294498238 ) ) ;
#17331=SURFACE_SIDE_STYLE ('',( #6040 ) ) ;
#17333=DIRECTION ( 'NONE',  ( -0.000000000000000000, 1.000000000000000000, -0.000000000000000000 ) ) ;
#17335=EDGE_CURVE ( 'NONE', #2175, #2442, #157, .T. ) ;
#17337=CARTESIAN_POINT ( 'NONE',  ( -2.416137431568557314, 39.07291177436112406, 91.27371380123798872 ) ) ;
#17345=DIRECTION ( 'NONE',  ( -0.000000000000000000, -0.000000000000000000, 1.000000000000000000 ) ) ;
#17352=CARTESIAN_POINT ( 'NONE',  ( -5.154188915835984375, 42.64120994080404614, 90.96121380123797451 ) ) ;
#17359=CARTESIAN_POINT ( 'NONE',  ( -0.8237052942265477018, 49.18499566818285018, 90.25808880294496817 ) ) ;
#17377=AXIS2_PLACEMENT_3D ( 'NONE', #18609, #8724, #5728 ) ;
#17380=AXIS2_PLACEMENT_3D ( 'NONE', #13353, #18341, #3559 ) ;
#17383=CARTESIAN_POINT ( 'NONE',  ( 1.352400422481993658, 50.46853102219002096, 94.47683880123798872 ) ) ;
#17386=ORIENTED_EDGE ( 'NONE', *, *, #20989, .T. ) ;
#17394=CARTESIAN_POINT ( 'NONE',  ( -0.3080929418689875576, 37.85583172076933778, 91.35183880123798872 ) ) ;
#17395=AXIS2_PLACEMENT_3D ( 'NONE', #19728, #11354, #160 ) ;
#17411=CARTESIAN_POINT ( 'NONE',  ( 3.460444912181559474, 49.25145096859824889, 95.49246380123798872 ) ) ;
#17414=EDGE_LOOP ( 'NONE', ( #796, #2675, #12742, #20321 ) ) ;
#17415=VERTEX_POINT ( 'NONE', #6605 ) ;
#17418=ORIENTED_EDGE ( 'NONE', *, *, #13643, .F. ) ;
#17428=CARTESIAN_POINT ( 'NONE',  ( 6.198496396448986090, 45.68315280215533392, 95.33621380123798872 ) ) ;
#17433=DIRECTION ( 'NONE',  ( -1.000000000000000000, 1.193617070626243484E-16, 0.000000000000000000 ) ) ;
#17436=ORIENTED_EDGE ( 'NONE', *, *, #18098, .F. ) ;
#17437=DIRECTION ( 'NONE',  ( -0.4999999999999984457, -0.8660254037844394848, -0.000000000000000000 ) ) ;
#17446=VERTEX_POINT ( 'NONE', #9934 ) ;
#17451=CYLINDRICAL_SURFACE ( 'NONE', #14050, 4.199999999999999289 ) ;
#17452=DIRECTION ( 'NONE',  ( -1.000000000000000000, 0.000000000000000000, 0.000000000000000000 ) ) ;
#17454=CARTESIAN_POINT ( 'NONE',  ( 10.77494014480653561, 42.96218137147968008, 69.40574467885102194 ) ) ;
#17456=EDGE_CURVE ( 'NONE', #3130, #7921, #2931, .T. ) ;
#17458=VECTOR ( 'NONE', #6683, 1000.000000000000000 ) ;
#17462=DIRECTION ( 'NONE',  ( 0.000000000000000000, 0.000000000000000000, 1.000000000000000000 ) ) ;
#17463=VERTEX_POINT ( 'NONE', #25 ) ;
#17465=CARTESIAN_POINT ( 'NONE',  ( 1.868012774839550749, 39.13936707477651566, 90.88308880294496817 ) ) ;
#17466=ORIENTED_EDGE ( 'NONE', *, *, #6078, .F. ) ;
#17470=DIRECTION ( 'NONE',  ( 1.402518428993831676E-16, -1.000000000000000000, -0.000000000000000000 ) ) ;
#17473=ORIENTED_EDGE ( 'NONE', *, *, #2765, .T. ) ;
#17477=CARTESIAN_POINT ( 'NONE',  ( -4.567115856812060670, 47.10047254335474065, 93.30496380123798872 ) ) ;
#17479=CARTESIAN_POINT ( 'NONE',  ( -4.567115856812060670, 47.10047254335474065, 94.55496380123798872 ) ) ;
#17487=CARTESIAN_POINT ( 'NONE',  ( 5.025485839985549319, 41.56218137147963887, 90.72683879953099506 ) ) ;
#17489=ORIENTED_EDGE ( 'NONE', *, *, #15769, .F. ) ;
#17491=EDGE_LOOP ( 'NONE', ( #13771, #1081, #4173, #6060, #19522, #2545 ) ) ;
#17496=CARTESIAN_POINT ( 'NONE',  ( 5.722153740305850000, 42.76884557083668881, 93.27737681315549878 ) ) ;
#17500=CARTESIAN_POINT ( 'NONE',  ( 4.685659163076279832, 40.18527142738543745, 95.05433879953100984 ) ) ;
#17509=EDGE_CURVE ( 'NONE', #1203, #6639, #18209, .T. ) ;
#17513=CARTESIAN_POINT ( 'NONE',  ( -4.524181921268124462, 40.28999182795290324, 94.78933880123798872 ) ) ;
#17515=LINE ( 'NONE', #9236, #5396 ) ;
#17529=PLANE ( 'NONE',  #13254 ) ;
#17530=CARTESIAN_POINT ( 'NONE',  ( 4.394343283833276992, 39.11584570990505938, 91.50808880123798872 ) ) ;
#17539=CARTESIAN_POINT ( 'NONE',  ( -0.9988176903691428077, 49.83852402762217082, 90.80496380123797451 ) ) ;
#17542=CARTESIAN_POINT ( 'NONE',  ( -3.981178359372548492, 46.76218137147973408, 92.60183879953099506 ) ) ;
#17547=DIRECTION ( 'NONE',  ( 0.000000000000000000, 2.168404344970984808E-15, -1.000000000000000000 ) ) ;
#17560=EDGE_CURVE ( 'NONE', #4848, #3564, #10251, .T. ) ;
#17561=CARTESIAN_POINT ( 'NONE',  ( 5.544968037009670780, 45.50804040601273925, 91.19558880294498238 ) ) ;
#17573=FACE_OUTER_BOUND ( 'NONE', #1010, .T. ) ;
#17574=CARTESIAN_POINT ( 'NONE',  ( -0.9988176903691428077, 49.83852402762217082, 95.64871380123798872 ) ) ;
#17579=ORIENTED_EDGE ( 'NONE', *, *, #1930, .T. ) ;
#17584=CARTESIAN_POINT ( 'NONE',  ( -5.154188915835984375, 42.64120994080404614, 92.36746380123797451 ) ) ;
#17594=CARTESIAN_POINT ( 'NONE',  ( -4.913882109623730621, 44.60549673912475299, 92.55433879953093879 ) ) ;
#17595=CARTESIAN_POINT ( 'NONE',  ( 6.828503391016846891, 43.33193468930419101, 92.91433880123798872 ) ) ;
#17596=ORIENTED_EDGE ( 'NONE', *, *, #19482, .T. ) ;
#17608=ORIENTED_EDGE ( 'NONE', *, *, #11160, .F. ) ;
#17616=CARTESIAN_POINT ( 'NONE',  ( -1.219056181836354558, 49.77488197367695477, 93.31237966814926210 ) ) ;
#17618=EDGE_LOOP ( 'NONE', ( #731, #18687, #4185, #9992, #17275, #8839, #4969, #5990 ) ) ;
#17625=CARTESIAN_POINT ( 'NONE',  ( 0.5221537403065010796, 44.16218137147969003, 95.05433879953098142 ) ) ;
#17627=CARTESIAN_POINT ( 'NONE',  ( 2.043125170982144745, 38.48583871533720213, 92.67996380123798872 ) ) ;
#17635=DIRECTION ( 'NONE',  ( -0.000000000000000000, -0.000000000000000000, 1.000000000000000000 ) ) ;
#17636=CARTESIAN_POINT ( 'NONE',  ( 4.199109002476567376, 47.83913663364971569, 93.48786078214052964 ) ) ;
#17639=ORIENTED_EDGE ( 'NONE', *, *, #9153, .T. ) ;
#17640=AXIS2_PLACEMENT_3D ( 'NONE', #3558, #11556, #16336 ) ;
#17642=VECTOR ( 'NONE', #10179, 1000.000000000000000 ) ;
#17647=DIRECTION ( 'NONE',  ( -1.000000000000000000, 0.000000000000000000, 0.000000000000000000 ) ) ;
#17652=CARTESIAN_POINT ( 'NONE',  ( 31.07218010054375412, 42.96218137147968008, 69.40574467885102194 ) ) ;
#17654=VECTOR ( 'NONE', #17117, 1000.000000000000000 ) ;
#17659=AXIS2_PLACEMENT_3D ( 'NONE', #8907, #16772, #3986 ) ;
#17662=ORIENTED_EDGE ( 'NONE', *, *, #3112, .T. ) ;
#17663=CARTESIAN_POINT ( 'NONE',  ( -4.477846259693498254, 37.66218137147969713, 53.35433879953099989 ) ) ;
#17676=EDGE_CURVE ( 'NONE', #970, #8464, #18741, .T. ) ;
#17680=CARTESIAN_POINT ( 'NONE',  ( 2.043125170982144745, 38.48583871533720213, 93.77371380123798872 ) ) ;
#17684=FACE_OUTER_BOUND ( 'NONE', #8125, .T. ) ;
#17703=FACE_OUTER_BOUND ( 'NONE', #1655, .T. ) ;
#17725=ORIENTED_EDGE ( 'NONE', *, *, #10377, .F. ) ;
#17729=FACE_OUTER_BOUND ( 'NONE', #7953, .T. ) ;
#17730=VECTOR ( 'NONE', #20799, 1000.000000000000000 ) ;
#17731=VERTEX_POINT ( 'NONE', #6062 ) ;
#17739=CARTESIAN_POINT ( 'NONE',  ( -5.154188915835984375, 42.64120994080404614, 91.11746380123797451 ) ) ;
#17740=( NAMED_UNIT ( * ) SI_UNIT ( $, .STERADIAN. ) SOLID_ANGLE_UNIT ( ) );
#17743=VECTOR ( 'NONE', #17433, 1000.000000000000000 ) ;
#17747=VECTOR ( 'NONE', #10872, 1000.000000000000000 ) ;
#17749=ORIENTED_EDGE ( 'NONE', *, *, #6651, .T. ) ;
#17751=CARTESIAN_POINT ( 'NONE',  ( -1.535769738210056579, 49.45816841730323432, 94.29858131124046849 ) ) ;
#17755=ORIENTED_EDGE ( 'NONE', *, *, #178, .F. ) ;
#17763=DIRECTION ( 'NONE',  ( 0.000000000000000000, 0.000000000000000000, 1.000000000000000000 ) ) ;
#17766=CARTESIAN_POINT ( 'NONE',  ( -7.677846259693484221, 47.36218137147966445, 53.35433879953099989 ) ) ;
#17768=ORIENTED_EDGE ( 'NONE', *, *, #4693, .T. ) ;
#17770=AXIS2_PLACEMENT_3D ( 'NONE', #5819, #11048, #12325 ) ;
#17774=CARTESIAN_POINT ( 'NONE',  ( 0.5221537403065019678, 51.36218137147968577, 83.03825919817350609 ) ) ;
#17786=ORIENTED_EDGE ( 'NONE', *, *, #2997, .F. ) ;
#17787=CARTESIAN_POINT ( 'NONE',  ( -2.416137431568557314, 39.07291177436112406, 92.36746380123797451 ) ) ;
#17788=CARTESIAN_POINT ( 'NONE',  ( -0.9988176903691428077, 49.83852402762217082, 94.39871380123798872 ) ) ;
#17794=DIRECTION ( 'NONE',  ( -0.000000000000000000, -0.000000000000000000, 1.000000000000000000 ) ) ;
#17798=CARTESIAN_POINT ( 'NONE',  ( 5.568489401881125289, 48.03437091500646261, 91.82058880123797451 ) ) ;
#17799=EDGE_LOOP ( 'NONE', ( #4702, #11904, #3436, #8007, #3248, #3281, #19890, #14213, #9727, #4509, #6107, #1740 ) ) ;
#17800=EDGE_CURVE ( 'NONE', #17463, #7261, #15868, .T. ) ;
#17801=DIRECTION ( 'NONE',  ( 0.000000000000000000, 0.000000000000000000, 1.000000000000000000 ) ) ;
#17802=CARTESIAN_POINT ( 'NONE',  ( 11.22215374030649926, 39.96218137147969429, 80.55433879953099563 ) ) ;
#17803=CARTESIAN_POINT ( 'NONE',  ( 5.691650701599316520, 41.94760153193540475, 92.55433879953103826 ) ) ;
#17815=LINE ( 'NONE', #52, #13917 ) ;
#17819=ORIENTED_EDGE ( 'NONE', *, *, #5940, .F. ) ;
#17820=DIRECTION ( 'NONE',  ( -1.334402673828316297E-16, 2.168404344970984413E-15, 1.000000000000000000 ) ) ;
#17822=DIRECTION ( 'NONE',  ( 0.000000000000000000, -1.000000000000000000, 2.168404344970984808E-15 ) ) ;
#17831=CARTESIAN_POINT ( 'NONE',  ( 6.102441102155617969, 43.42752260303680600, 95.80496379953099506 ) ) ;
#17840=DIRECTION ( 'NONE',  ( -0.000000000000000000, -0.000000000000000000, 1.000000000000000000 ) ) ;
#17842=CARTESIAN_POINT ( 'NONE',  ( 4.394343283833276992, 39.11584570990505938, 95.10183880123797451 ) ) ;
#17844=UNCERTAINTY_MEASURE_WITH_UNIT (LENGTH_MEASURE( 1.000000000000000082E-05 ), #1678, 'distance_accuracy_value', 'NONE');
#17852=CYLINDRICAL_SURFACE ( 'NONE', #10623, 0.9921021478795020165 ) ;
#17859=CARTESIAN_POINT ( 'NONE',  ( 31.22215374030650281, 45.56218137147968861, 72.80433879953100984 ) ) ;
#17863=CARTESIAN_POINT ( 'NONE',  ( 6.198496396448986090, 45.68315280215533392, 94.08621380123807398 ) ) ;
#17867=CARTESIAN_POINT ( 'NONE',  ( -4.524181921268124462, 40.28999182795290324, 93.53933880123797451 ) ) ;
#17875=ORIENTED_EDGE ( 'NONE', *, *, #8694, .T. ) ;
#17886=CARTESIAN_POINT ( 'NONE',  ( 1.352400422481993658, 50.46853102219002096, 93.07058880123798872 ) ) ;
#17887=ADVANCED_FACE ( 'NONE', ( #9801 ), #10115, .F. ) ;
#17896=ORIENTED_EDGE ( 'NONE', *, *, #6724, .T. ) ;
#17898=FACE_BOUND ( 'NONE', #18263, .T. ) ;
#17899=CARTESIAN_POINT ( 'NONE',  ( 2.263363662449358493, 49.77488197367694767, 94.44231768333818877 ) ) ;
#17900=CARTESIAN_POINT ( 'NONE',  ( 4.394343283833276992, 39.11584570990505938, 93.85183880123797451 ) ) ;
#17908=CARTESIAN_POINT ( 'NONE',  ( -1.997856540139665737, 38.86318974171943808, 92.55433879953103826 ) ) ;
#17918=CARTESIAN_POINT ( 'NONE',  ( 3.788215052820487205, 39.19523464621513398, 90.08681233796825438 ) ) ;
#17922=AXIS2_PLACEMENT_3D ( 'NONE', #9253, #3442, #5026 ) ;
#17924=CARTESIAN_POINT ( 'NONE',  ( 11.22215374030650281, 42.76218137147968434, 66.20574467885104752 ) ) ;
#17926=CARTESIAN_POINT ( 'NONE',  ( 35.92215374030650565, 47.36218137147962892, 93.55433879953098142 ) ) ;
#17929=CARTESIAN_POINT ( 'NONE',  ( 2.043125170982144745, 38.48583871533720213, 93.92996380123798872 ) ) ;
#17931=ORIENTED_EDGE ( 'NONE', *, *, #11068, .F. ) ;
#17935=LINE ( 'NONE', #9866, #6097 ) ;
#17936=CARTESIAN_POINT ( 'NONE',  ( -5.058133621542618030, 44.89684013992257405, 92.67996379953099506 ) ) ;
#17937=ORIENTED_EDGE ( 'NONE', *, *, #426, .F. ) ;
#17939=CARTESIAN_POINT ( 'NONE',  ( 31.07218010054375412, 42.96218137147968008, 69.40574467885102194 ) ) ;
#17942=CARTESIAN_POINT ( 'NONE',  ( -3.777846259693483866, 51.36218137147968577, 54.55433879953099563 ) ) ;
#17945=CARTESIAN_POINT ( 'NONE',  ( 2.043125170982144745, 38.48583871533720213, 93.77371380123798872 ) ) ;
#17950=EDGE_CURVE ( 'NONE', #18376, #13576, #15111, .T. ) ;
#17956=ORIENTED_EDGE ( 'NONE', *, *, #8138, .T. ) ;
#17959=DIRECTION ( 'NONE',  ( -1.402518428993831676E-16, 1.000000000000000000, 0.000000000000000000 ) ) ;
#17965=CARTESIAN_POINT ( 'NONE',  ( 5.722153740306477054, 44.16218185475116798, 93.64411094854725093 ) ) ;
#17966=CARTESIAN_POINT ( 'NONE',  ( 10.77494014480653561, 42.76218137147968434, 69.40574467885102194 ) ) ;
#17968=CARTESIAN_POINT ( 'NONE',  ( -3.154801521863568325, 47.83913663364971569, 94.11286078555450274 ) ) ;
#17988=LINE ( 'NONE', #15, #20110 ) ;
#17994=EDGE_LOOP ( 'NONE', ( #15029, #1342, #6741, #1265, #73, #4139 ) ) ;
#17995=CARTESIAN_POINT ( 'NONE',  ( -4.567115856812060670, 47.10047254335474065, 92.05496380123798872 ) ) ;
#17997=CARTESIAN_POINT ( 'NONE',  ( 0.5221537403065010796, 44.16218137147969003, 45.55433879953098852 ) ) ;
#18000=VECTOR ( 'NONE', #19304, 1000.000000000000000 ) ;
#18004=ORIENTED_EDGE ( 'NONE', *, *, #14148, .T. ) ;
#18011=CARTESIAN_POINT ( 'NONE',  ( -10.17784625969349754, 51.36218137147968577, 80.55433879953099563 ) ) ;
#18021=DIRECTION ( 'NONE',  ( -1.621236893436268647E-16, -2.273814620809075225E-32, 1.000000000000000000 ) ) ;
#18033=CARTESIAN_POINT ( 'NONE',  ( -1.854173455793825864, 49.13976469971944994, 93.55877693069184886 ) ) ;
#18034=EDGE_CURVE ( 'NONE', #3547, #8376, #16706, .T. ) ;
#18039=CARTESIAN_POINT ( 'NONE',  ( 31.07218010054375412, 45.56218137147968861, 70.80574467885102763 ) ) ;
#18041=VERTEX_POINT ( 'NONE', #7328 ) ;
#18042=CARTESIAN_POINT ( 'NONE',  ( 1.514255888186008425, 52.36218137147968577, 52.53721119516358584 ) ) ;
#18043=CARTESIAN_POINT ( 'NONE',  ( -1.579458713458412822, 38.67424504376464967, 92.55433879953098142 ) ) ;
#18044=CARTESIAN_POINT ( 'NONE',  ( -2.904223097202481174, 48.62752260303690122, 93.77371379953099506 ) ) ;
#18045=VERTEX_POINT ( 'NONE', #10548 ) ;
#18049=ORIENTED_EDGE ( 'NONE', *, *, #5066, .T. ) ;
#18059=ADVANCED_FACE ( 'NONE', ( #16907 ), #2333, .T. ) ;
#18064=DIRECTION ( 'NONE',  ( 1.000000000000000000, 0.000000000000000000, 0.000000000000000000 ) ) ;
#18067=AXIS2_PLACEMENT_3D ( 'NONE', #13172, #19332, #11589 ) ;
#18079=CARTESIAN_POINT ( 'NONE',  ( 5.568489401881125289, 48.03437091500647682, 94.16433880123805977 ) ) ;
#18084=CARTESIAN_POINT ( 'NONE',  ( 2.043125170982144745, 38.48583871533720213, 91.27371380123798872 ) ) ;
#18089=AXIS2_PLACEMENT_3D ( 'NONE', #513, #19969, #20290 ) ;
#18098=EDGE_CURVE ( 'NONE', #17279, #5762, #4131, .T. ) ;
#18103=EDGE_CURVE ( 'NONE', #16344, #18958, #19878, .T. ) ;
#18105=EDGE_LOOP ( 'NONE', ( #19847, #16080, #370, #1110 ) ) ;
#18106=CARTESIAN_POINT ( 'NONE',  ( 5.146041124512939824, 40.41782456190201600, 90.15009067557426192 ) ) ;
#18109=CARTESIAN_POINT ( 'NONE',  ( -5.784195910403845176, 44.99242805365518194, 95.88308880123798872 ) ) ;
#18115=CARTESIAN_POINT ( 'NONE',  ( -5.677846259693490438, 44.16218137147969003, 80.55433879953099563 ) ) ;
#18118=ORIENTED_EDGE ( 'NONE', *, *, #1313, .F. ) ;
#18121=VECTOR ( 'NONE', #16116, 1000.000000000000000 ) ;
#18122=CARTESIAN_POINT ( 'NONE',  ( 3.694606274243302568, 39.25854522838572080, 92.55433879953095300 ) ) ;
#18124=ADVANCED_FACE ( 'NONE', ( #8631 ), #11812, .F. ) ;
#18132=CARTESIAN_POINT ( 'NONE',  ( -3.190985070539315682, 47.80295308497395013, 95.05235256388647258 ) ) ;
#18141=FACE_OUTER_BOUND ( 'NONE', #19098, .T. ) ;
#18142=ADVANCED_FACE ( 'NONE', ( #19036 ), #9043, .T. ) ;
#18144=CARTESIAN_POINT ( 'NONE',  ( 5.025485839985549319, 41.56218137147963887, 93.22683879953099506 ) ) ;
#18151=CARTESIAN_POINT ( 'NONE',  ( -3.981178359372548492, 46.76218137147973408, 95.10183879953099506 ) ) ;
#18154=ORIENTED_EDGE ( 'NONE', *, *, #14178, .F. ) ;
#18155=DIRECTION ( 'NONE',  ( -0.000000000000000000, -0.000000000000000000, 1.000000000000000000 ) ) ;
#18165=ORIENTED_EDGE ( 'NONE', *, *, #17335, .T. ) ;
#18172=ADVANCED_FACE ( 'NONE', ( #14234 ), #4448, .F. ) ;
#18174=VERTEX_POINT ( 'NONE', #4233 ) ;
#18179=LINE ( 'NONE', #6803, #9966 ) ;
#18183=DIRECTION ( 'NONE',  ( 1.402518428993831676E-16, -1.000000000000000000, 0.000000000000000000 ) ) ;
#18184=CARTESIAN_POINT ( 'NONE',  ( 6.198496396448986090, 45.68315280215533392, 90.33621380123798872 ) ) ;
#18185=CARTESIAN_POINT ( 'NONE',  ( -4.567115856812060670, 47.10047254335474065, 90.80496380123797451 ) ) ;
#18192=EDGE_CURVE ( 'NONE', #1841, #5158, #12293, .T. ) ;
#18193=CARTESIAN_POINT ( 'NONE',  ( 8.722153740306486824, 51.36218137147968577, 95.05433879953098142 ) ) ;
#18199=ORIENTED_EDGE ( 'NONE', *, *, #9485, .T. ) ;
#18203=CARTESIAN_POINT ( 'NONE',  ( 5.611423337425062385, 41.22389019960463230, 92.67996380123798872 ) ) ;
#18204=EDGE_CURVE ( 'NONE', #12799, #9648, #14035, .T. ) ;
#18207=CARTESIAN_POINT ( 'NONE',  ( -2.416137431568557314, 39.07291177436112406, 94.86746380123797451 ) ) ;
#18209=LINE ( 'NONE', #19897, #19084 ) ;
#18216=CARTESIAN_POINT ( 'NONE',  ( -0.3080929418689875576, 37.85583172076933778, 94.94558880123797451 ) ) ;
#18218=LINE ( 'NONE', #1942, #10664 ) ;
#18224=VERTEX_POINT ( 'NONE', #9364 ) ;
#18226=ORIENTED_EDGE ( 'NONE', *, *, #16564, .T. ) ;
#18234=VERTEX_POINT ( 'NONE', #4551 ) ;
#18238=ORIENTED_EDGE ( 'NONE', *, *, #6776, .T. ) ;
#18241=CARTESIAN_POINT ( 'NONE',  ( 3.122153740306552905, 48.66551347115873227, 96.03933879953099506 ) ) ;
#18247=DIRECTION ( 'NONE',  ( -1.334402673828313832E-16, 2.891205793294680792E-16, 1.000000000000000000 ) ) ;
#18248=CARTESIAN_POINT ( 'NONE',  ( -0.2125050281363792815, 38.58189400963055959, 91.74246379953099506 ) ) ;
#18249=ORIENTED_EDGE ( 'NONE', *, *, #652, .T. ) ;
#18251=CARTESIAN_POINT ( 'NONE',  ( -5.154188915835984375, 42.64120994080404614, 96.11746380123797451 ) ) ;
#18263=EDGE_LOOP ( 'NONE', ( #2253, #6967 ) ) ;
#18265=FACE_OUTER_BOUND ( 'NONE', #3720, .T. ) ;
#18266=CARTESIAN_POINT ( 'NONE',  ( -5.784195910403845176, 44.99242805365518194, 93.53933880123797451 ) ) ;
#18277=DIRECTION ( 'NONE',  ( 1.000000000000000000, 0.000000000000000000, 0.000000000000000000 ) ) ;
#18279=CARTESIAN_POINT ( 'NONE',  ( 0.3016330202435082986, 38.27734481069801831, 92.55433879953096721 ) ) ;
#18280=FACE_OUTER_BOUND ( 'NONE', #20718, .T. ) ;
#18281=CARTESIAN_POINT ( 'NONE',  ( 6.828503391016846891, 43.33193468930419101, 94.00808880123798872 ) ) ;
#18282=DIRECTION ( 'NONE',  ( 1.402518428993854849E-16, -1.000000000000000000, -1.734723475976787531E-14 ) ) ;
#18286=EDGE_LOOP ( 'NONE', ( #16011, #16402, #232, #15181 ) ) ;
#18288=CARTESIAN_POINT ( 'NONE',  ( 10.77494014480653561, 42.96218137147968008, 69.40574467885102194 ) ) ;
#18290=CARTESIAN_POINT ( 'NONE',  ( 5.025485839985549319, 41.56218137147963887, 90.72683879953099506 ) ) ;
#18292=DIRECTION ( 'NONE',  ( -1.000000000000000000, 0.000000000000000000, 0.000000000000000000 ) ) ;
#18301=CARTESIAN_POINT ( 'NONE',  ( 2.722153740306497927, 50.36218137147968577, 37.95170767603170248 ) ) ;
#18304=CARTESIAN_POINT ( 'NONE',  ( 5.544968037009670780, 45.50804040601273925, 92.44558880294498238 ) ) ;
#18307=CARTESIAN_POINT ( 'NONE',  ( 5.568489401881125289, 48.03437091500646261, 90.57058880123798872 ) ) ;
#18311=CARTESIAN_POINT ( 'NONE',  ( 0.5221537403065010796, 44.16218137147969003, 45.55433879953098852 ) ) ;
#18314=CARTESIAN_POINT ( 'NONE',  ( -2.829262219629335551, 48.16467593588394891, 92.84494095006279224 ) ) ;
#18316=CARTESIAN_POINT ( 'NONE',  ( 5.568489401881125289, 48.03437091500646261, 92.91433880123798872 ) ) ;
#18318=ADVANCED_FACE ( 'NONE', ( #9889 ), #14763, .T. ) ;
#18320=EDGE_CURVE ( 'NONE', #7787, #15579, #7006, .T. ) ;
#18324=LINE ( 'NONE', #3741, #16729 ) ;
#18341=DIRECTION ( 'NONE',  ( 1.000000000000000000, 5.595882180570345180E-16, 0.000000000000000000 ) ) ;
#18343=CARTESIAN_POINT ( 'NONE',  ( -2.825834663281994619, 48.16810349223129606, 93.78225227128625363 ) ) ;
#18344=CARTESIAN_POINT ( 'NONE',  ( -3.943187491250720544, 40.73580453397070755, 94.08621379953100927 ) ) ;
#18345=CARTESIAN_POINT ( 'NONE',  ( 4.987494971863720927, 47.58855820898865829, 92.21121379953100927 ) ) ;
#18346=VECTOR ( 'NONE', #75, 1000.000000000000000 ) ;
#18354=ADVANCED_FACE ( 'NONE', ( #9683 ), #17852, .T. ) ;
#18355=ORIENTED_EDGE ( 'NONE', *, *, #9011, .T. ) ;
#18358=ORIENTED_EDGE ( 'NONE', *, *, #873, .T. ) ;
#18360=CARTESIAN_POINT ( 'NONE',  ( 2.722153740306499703, 47.73989013547934945, 45.55433879953098852 ) ) ;
#18361=EDGE_CURVE ( 'NONE', #7434, #16241, #9782, .T. ) ;
#18362=CARTESIAN_POINT ( 'NONE',  ( 6.828503391016846891, 43.33193468930419101, 91.50808880123798872 ) ) ;
#18363=EDGE_CURVE ( 'NONE', #9648, #16344, #3373, .T. ) ;
#18366=AXIS2_PLACEMENT_3D ( 'NONE', #16153, #12647, #3061 ) ;
#18375=CARTESIAN_POINT ( 'NONE',  ( -0.3080929418689875576, 37.85583172076933778, 95.10183880123796030 ) ) ;
#18376=VERTEX_POINT ( 'NONE', #6352 ) ;
#18380=DIRECTION ( 'NONE',  ( 1.000000000000000000, -0.000000000000000000, -0.000000000000000000 ) ) ;
#18385=CARTESIAN_POINT ( 'NONE',  ( 6.198496396448986090, 45.68315280215533392, 94.24246380123798872 ) ) ;
#18389=CARTESIAN_POINT ( 'NONE',  ( 31.22215374030650281, 45.56218137147968861, 78.80433879953099563 ) ) ;
#18391=CARTESIAN_POINT ( 'NONE',  ( -3.981178359372548492, 46.76218137147973408, 95.41433880294498238 ) ) ;
#18392=AXIS2_PLACEMENT_3D ( 'NONE', #7881, #14150, #1714 ) ;
#18399=CARTESIAN_POINT ( 'NONE',  ( 10.77494014480653561, 42.96218137147968008, 77.40433879953098995 ) ) ;
#18401=CARTESIAN_POINT ( 'NONE',  ( -0.3080929418689875576, 37.85583172076933778, 95.10183880123796030 ) ) ;
#18403=DIRECTION ( 'NONE',  ( 0.000000000000000000, -1.000000000000000000, 0.000000000000000000 ) ) ;
#18407=ORIENTED_EDGE ( 'NONE', *, *, #9128, .F. ) ;
#18413=AXIS2_PLACEMENT_3D ( 'NONE', #4835, #6541, #3041 ) ;
#18417=CARTESIAN_POINT ( 'NONE',  ( 6.102441102155617969, 43.42752260303680600, 89.86746380294499659 ) ) ;
#18420=CARTESIAN_POINT ( 'NONE',  ( 2.043125170982144745, 38.48583871533720213, 91.42996380123798872 ) ) ;
#18426=ORIENTED_EDGE ( 'NONE', *, *, #1977, .T. ) ;
#18428=CARTESIAN_POINT ( 'NONE',  ( -0.8237052942265477018, 49.18499566818285018, 95.25808880294498238 ) ) ;
#18434=FACE_BOUND ( 'NONE', #20147, .T. ) ;
#18442=CIRCLE ( 'NONE', #17377, 0.9921021478795063464 ) ;
#18448=ORIENTED_EDGE ( 'NONE', *, *, #18361, .T. ) ;
#18450=EDGE_CURVE ( 'NONE', #10129, #970, #16343, .T. ) ;
#18454=CARTESIAN_POINT ( 'NONE',  ( -2.077846259693550746, 39.65884927180063357, 94.16433879953098085 ) ) ;
#18455=CARTESIAN_POINT ( 'NONE',  ( -4.500660556396669065, 42.81632233694663370, 95.25808879953098085 ) ) ;
#18461=CARTESIAN_POINT ( 'NONE',  ( -2.904223097202481174, 48.62752260303690122, 91.27371379953098085 ) ) ;
#18464=CARTESIAN_POINT ( 'NONE',  ( 4.001624342216747010, 40.29782057951908314, 90.66473080991372058 ) ) ;
#18468=CARTESIAN_POINT ( 'NONE',  ( 3.460444912181559474, 49.25145096859824889, 90.49246380123798872 ) ) ;
#18473=ADVANCED_FACE ( 'NONE', ( #13146 ), #11355, .F. ) ;
#18475=EDGE_CURVE ( 'NONE', #2806, #20010, #4621, .T. ) ;
#18478=ORIENTED_EDGE ( 'NONE', *, *, #13643, .T. ) ;
#18479=CARTESIAN_POINT ( 'NONE',  ( 31.07218010054375412, 42.96218137147968008, 65.80574467885102763 ) ) ;
#18482=CARTESIAN_POINT ( 'NONE',  ( -4.567115856812060670, 47.10047254335474065, 95.96121380123798872 ) ) ;
#18485=ADVANCED_FACE ( 'NONE', ( #11250 ), #14456, .T. ) ;
#18494=DIRECTION ( 'NONE',  ( -1.000000000000000000, 0.000000000000000000, 0.000000000000000000 ) ) ;
#18495=CARTESIAN_POINT ( 'NONE',  ( 30.92220646078100188, 42.96218137147968008, 61.80715055817104542 ) ) ;
#18496=CARTESIAN_POINT ( 'NONE',  ( -3.350035803220276609, 49.20851703305431357, 94.63308880123798872 ) ) ;
#18498=CARTESIAN_POINT ( 'NONE',  ( -1.579458713458412822, 38.67424504376464967, 92.55433879953098142 ) ) ;
#18500=CARTESIAN_POINT ( 'NONE',  ( 5.544968037009670780, 45.50804040601273925, 93.69558880294498238 ) ) ;
#18507=ADVANCED_FACE ( 'NONE', ( #20717 ), #1264, .F. ) ;
#18509=CARTESIAN_POINT ( 'NONE',  ( 6.828503391016846891, 43.33193468930419101, 92.91433880123798872 ) ) ;
#18512=DIRECTION ( 'NONE',  ( -1.193617070626243484E-16, -1.000000000000000000, -0.000000000000000000 ) ) ;
#18514=EDGE_LOOP ( 'NONE', ( #8799, #134, #5702, #16605 ) ) ;
#18524=DIRECTION ( 'NONE',  ( -2.409338161078896715E-16, 1.000000000000000000, 0.000000000000000000 ) ) ;
#18527=CARTESIAN_POINT ( 'NONE',  ( -0.9988176903691428077, 49.83852402762217082, 93.14871380123798872 ) ) ;
#18533=CARTESIAN_POINT ( 'NONE',  ( 1.514255888186008203, 51.36218137147968577, 52.53721119516358584 ) ) ;
#18534=CARTESIAN_POINT ( 'NONE',  ( 1.868012774839550749, 39.13936707477651566, 94.63308880294498238 ) ) ;
#18535=VERTEX_POINT ( 'NONE', #2764 ) ;
#18537=DIRECTION ( 'NONE',  ( 1.000000000000000000, 0.000000000000000000, 0.000000000000000000 ) ) ;
#18552=CARTESIAN_POINT ( 'NONE',  ( -1.677846259693499542, 50.36218137147968577, 54.55433879953098852 ) ) ;
#18558=CARTESIAN_POINT ( 'NONE',  ( 3.122153740306552905, 48.66551347115873227, 93.53933879953099506 ) ) ;
#18559=CARTESIAN_POINT ( 'NONE',  ( 1.868012774839550749, 39.13936707477651566, 95.57058879953099506 ) ) ;
#18562=CARTESIAN_POINT ( 'NONE',  ( -4.524181921268124462, 40.28999182795290324, 93.69558880123800293 ) ) ;
#18569=CARTESIAN_POINT ( 'NONE',  ( -2.416137431568557314, 39.07291177436112406, 96.27371380123797451 ) ) ;
#18570=EDGE_CURVE ( 'NONE', #15771, #4901, #9045, .T. ) ;
#18577=DIRECTION ( 'NONE',  ( -1.000000000000000000, 0.000000000000000000, 0.000000000000000000 ) ) ;
#18585=CARTESIAN_POINT ( 'NONE',  ( 1.352400422481993658, 50.46853102219002096, 94.47683880123798872 ) ) ;
#18590=EDGE_LOOP ( 'NONE', ( #5921, #20098, #14214, #19218 ) ) ;
#18600=CARTESIAN_POINT ( 'NONE',  ( 11.22215374030650281, 42.96218137147968008, 58.20715055817105110 ) ) ;
#18601=CARTESIAN_POINT ( 'NONE',  ( 1.868012774839550749, 39.13936707477651566, 94.63308880294498238 ) ) ;
#18603=CARTESIAN_POINT ( 'NONE',  ( -3.981178359372548492, 46.76218137147973408, 91.66433880294496817 ) ) ;
#18609=CARTESIAN_POINT ( 'NONE',  ( 0.5221537403065019678, 51.36218137147968577, 48.36106904222365444 ) ) ;
#18610=CARTESIAN_POINT ( 'NONE',  ( -4.524181921268124462, 40.28999182795290324, 93.69558880123800293 ) ) ;
#18622=CARTESIAN_POINT ( 'NONE',  ( -1.677846259693499542, 44.16218137147969003, 54.55433879953098852 ) ) ;
#18623=CARTESIAN_POINT ( 'NONE',  ( -5.368445182934982185, 36.96218137147968008, 95.05433879953098142 ) ) ;
#18626=CARTESIAN_POINT ( 'NONE',  ( -0.8237052942265477018, 49.18499566818285018, 90.25808880294496817 ) ) ;
#18635=ORIENTED_EDGE ( 'NONE', *, *, #13374, .T. ) ;
#18636=FACE_OUTER_BOUND ( 'NONE', #15611, .T. ) ;
#18637=CARTESIAN_POINT ( 'NONE',  ( -3.350035803220276609, 49.20851703305431357, 93.22683880123798872 ) ) ;
#18651=FACE_OUTER_BOUND ( 'NONE', #14007, .T. ) ;
#18653=CARTESIAN_POINT ( 'NONE',  ( 28.52215374030649997, 44.16218137147968292, 87.05433879953099563 ) ) ;
#18661=CARTESIAN_POINT ( 'NONE',  ( -2.904223097202481174, 48.62752260303690122, 92.52371379953099506 ) ) ;
#18662=ORIENTED_EDGE ( 'NONE', *, *, #11160, .T. ) ;
#18663=CARTESIAN_POINT ( 'NONE',  ( -4.567115856812060670, 47.10047254335474065, 93.46121380123797451 ) ) ;
#18670=VECTOR ( 'NONE', #19853, 1000.000000000000000 ) ;
#18671=CARTESIAN_POINT ( 'NONE',  ( 1.352400422481993658, 50.46853102219002096, 93.22683880123798872 ) ) ;
#18675=( BOUNDED_CURVE ( )  B_SPLINE_CURVE ( 2, ( #11178, #20624, #4656, #15962, #14463 ),
 .UNSPECIFIED., .F., .F. ) 
 B_SPLINE_CURVE_WITH_KNOTS ( ( 3, 2, 3 ),
 ( 0.4333811345117426495, 0.4500000000000000111, 0.4583811345117425051 ),
 .UNSPECIFIED. ) 
 CURVE ( )  GEOMETRIC_REPRESENTATION_ITEM ( )  RATIONAL_B_SPLINE_CURVE ( ( 0.9660722070828662300, 0.9493985675960723292, 1.000000000000000000, 0.9744809649152148534, 0.9660722070828664521 ) ) 
 REPRESENTATION_ITEM ( '' )  );
#18683=ADVANCED_FACE ( 'NONE', ( #10093 ), #16787, .F. ) ;
#18686=VECTOR ( 'NONE', #8891, 1000.000000000000000 ) ;
#18687=ORIENTED_EDGE ( 'NONE', *, *, #8807, .T. ) ;
#18689=CARTESIAN_POINT ( 'NONE',  ( -3.154801521863568325, 47.83913663364971569, 93.80036078214054385 ) ) ;
#18690=CARTESIAN_POINT ( 'NONE',  ( -3.350035803220276609, 49.20851703305431357, 90.88308880123797451 ) ) ;
#18694=VECTOR ( 'NONE', #20163, 1000.000000000000000 ) ;
#18696=CARTESIAN_POINT ( 'NONE',  ( -3.154801521863568325, 47.83913663364971569, 94.11286078555450274 ) ) ;
#18706=LINE ( 'NONE', #14125, #7041 ) ;
#18709=CARTESIAN_POINT ( 'NONE',  ( 1.256812508749381774, 49.74246873332880625, 95.17996380294498238 ) ) ;
#18710=ADVANCED_FACE ( 'NONE', ( #13697 ), #1165, .T. ) ;
#18711=VECTOR ( 'NONE', #4134, 1000.000000000000000 ) ;
#18724=EDGE_CURVE ( 'NONE', #15252, #5582, #11447, .T. ) ;
#18733=CARTESIAN_POINT ( 'NONE',  ( -4.224566820778121290, 46.53527118704992915, 95.05433879953105247 ) ) ;
#18735=CARTESIAN_POINT ( 'NONE',  ( -2.904223097202481174, 48.62752260303690122, 92.83621380294498238 ) ) ;
#18737=CARTESIAN_POINT ( 'NONE',  ( -10.17784625969349399, 36.96218137147968008, 54.55433879953098852 ) ) ;
#18741=LINE ( 'NONE', #2250, #10257 ) ;
#18750=CARTESIAN_POINT ( 'NONE',  ( -2.904223097202481174, 48.62752260303690122, 95.33621380294498238 ) ) ;
#18754=CARTESIAN_POINT ( 'NONE',  ( 33.61275266354798674, 51.36218137147967866, 45.55433879953098852 ) ) ;
#18761=ORIENTED_EDGE ( 'NONE', *, *, #19762, .T. ) ;
#18766=DIRECTION ( 'NONE',  ( 1.196361017915039239E-16, 0.000000000000000000, -1.000000000000000000 ) ) ;
#18776=CARTESIAN_POINT ( 'NONE',  ( -2.077846259693550746, 39.65884927180063357, 91.66433879953099506 ) ) ;
#18778=CARTESIAN_POINT ( 'NONE',  ( 5.611423337425062385, 41.22389019960463230, 95.33621380123798872 ) ) ;
#18780=CARTESIAN_POINT ( 'NONE',  ( 2.043125170982144745, 38.48583871533720213, 95.02371380123805977 ) ) ;
#18785=ORIENTED_EDGE ( 'NONE', *, *, #2765, .F. ) ;
#18801=DIRECTION ( 'NONE',  ( 0.000000000000000000, 0.000000000000000000, 1.000000000000000000 ) ) ;
#18802=CARTESIAN_POINT ( 'NONE',  ( 3.122075258343615545, 38.59543968120053847, 90.21201841395856036 ) ) ;
#18806=ORIENTED_EDGE ( 'NONE', *, *, #2550, .T. ) ;
#18815=CARTESIAN_POINT ( 'NONE',  ( -4.524181921268124462, 40.28999182795290324, 94.94558880123797451 ) ) ;
#18819=CARTESIAN_POINT ( 'NONE',  ( -3.943187491250720544, 40.73580453397070755, 90.64871380294496817 ) ) ;
#18821=FILL_AREA_STYLE_COLOUR ( '', #4764 ) ;
#18828=CARTESIAN_POINT ( 'NONE',  ( 5.611423337425062385, 41.22389019960463230, 91.58621380123798872 ) ) ;
#18833=CARTESIAN_POINT ( 'NONE',  ( -4.677846259692849173, 45.55551717212267704, 92.65237681315549878 ) ) ;
#18838=CARTESIAN_POINT ( 'NONE',  ( -4.677846259693497544, 44.16218137147969003, 77.84651775085080772 ) ) ;
#18848=CARTESIAN_POINT ( 'NONE',  ( 1.256812508749381774, 49.74246873332880625, 93.92996380294498238 ) ) ;
#18849=ORIENTED_EDGE ( 'NONE', *, *, #12626, .T. ) ;
#18855=CARTESIAN_POINT ( 'NONE',  ( 28.52215374030649997, 44.16218137147968292, 93.55433879953098142 ) ) ;
#18857=EDGE_CURVE ( 'NONE', #9111, #1841, #3437, .T. ) ;
#18859=ORIENTED_EDGE ( 'NONE', *, *, #20923, .F. ) ;
#18864=CARTESIAN_POINT ( 'NONE',  ( 2.891178763948851316, 49.58011693252095142, 93.16981103995755120 ) ) ;
#18865=CARTESIAN_POINT ( 'NONE',  ( -3.350035803220276609, 49.20851703305431357, 95.72683880123798872 ) ) ;
#18869=EDGE_CURVE ( 'NONE', #20498, #3734, #11434, .T. ) ;
#18870=EDGE_CURVE ( 'NONE', #1841, #16818, #4701, .T. ) ;
#18877=CARTESIAN_POINT ( 'NONE',  ( 6.828503391016846891, 43.33193468930419101, 95.41433880123797451 ) ) ;
#18880=CARTESIAN_POINT ( 'NONE',  ( -2.416137431568557314, 39.07291177436112406, 95.02371380123797451 ) ) ;
#18888=CARTESIAN_POINT ( 'NONE',  ( -4.524181921268124462, 40.28999182795290324, 92.44558880123798872 ) ) ;
#18902=CARTESIAN_POINT ( 'NONE',  ( -5.154188915835984375, 42.64120994080404614, 92.36746380123797451 ) ) ;
#18904=ORIENTED_EDGE ( 'NONE', *, *, #18192, .F. ) ;
#18906=PLANE ( 'NONE',  #17770 ) ;
#18915=LINE ( 'NONE', #6413, #8071 ) ;
#18917=CARTESIAN_POINT ( 'NONE',  ( 3.948530577815480225, 39.69684013992245752, 94.71121380294496817 ) ) ;
#18922=CARTESIAN_POINT ( 'NONE',  ( 31.07218010054375412, 42.96218137147968008, 69.80574467885101342 ) ) ;
#18929=VERTEX_POINT ( 'NONE', #20009 ) ;
#18934=DIRECTION ( 'NONE',  ( -0.000000000000000000, 2.168404344970984413E-15, -1.000000000000000000 ) ) ;
#18937=DIRECTION ( 'NONE',  ( -1.193617070626243484E-16, -1.000000000000000000, 0.000000000000000000 ) ) ;
#18942=B_SPLINE_CURVE_WITH_KNOTS ( 'NONE', 3,
 ( #18498, #16696, #10328, #3909, #18279, #10435, #2218, #4014, #509, #15200 ),
 .UNSPECIFIED., .F., .F.,
 ( 4, 2, 2, 2, 4 ),
 ( 0.000000000000000000, 0.001160160651305638902, 0.002320321302611277371, 0.003480481953916916490, 0.004640642605222555610 ),
 .UNSPECIFIED. ) ;
#18945=EDGE_CURVE ( 'NONE', #11018, #11438, #18324, .T. ) ;
#18946=CYLINDRICAL_SURFACE ( 'NONE', #729, 5.199999999999999289 ) ;
#18947=ORIENTED_EDGE ( 'NONE', *, *, #2997, .T. ) ;
#18950=CARTESIAN_POINT ( 'NONE',  ( -0.8237052942265477018, 49.18499566818285018, 91.50808880294498238 ) ) ;
#18954=DIRECTION ( 'NONE',  ( 1.000000000000000000, 0.000000000000000000, 0.000000000000000000 ) ) ;
#18956=CARTESIAN_POINT ( 'NONE',  ( 33.61275266354798674, 36.96218137147968719, 92.39963826115175038 ) ) ;
#18958=VERTEX_POINT ( 'NONE', #2163 ) ;
#18962=ORIENTED_EDGE ( 'NONE', *, *, #11859, .F. ) ;
#18964=CARTESIAN_POINT ( 'NONE',  ( 5.568489401881125289, 48.03437091500646261, 95.41433880123797451 ) ) ;
#18965=CARTESIAN_POINT ( 'NONE',  ( -4.524181921268124462, 40.28999182795290324, 96.03933880123798872 ) ) ;
#18966=FACE_OUTER_BOUND ( 'NONE', #14723, .T. ) ;
#18968=CARTESIAN_POINT ( 'NONE',  ( 35.92215374030650565, 51.36218137147967866, 93.55433879953098142 ) ) ;
#18977=CARTESIAN_POINT ( 'NONE',  ( -5.784195910403845176, 44.99242805365518194, 96.03933880123796030 ) ) ;
#18987=CARTESIAN_POINT ( 'NONE',  ( 11.22215374030650281, 42.96218137147968008, 73.80433879953100984 ) ) ;
#18988=CARTESIAN_POINT ( 'NONE',  ( 6.198496396448986090, 45.68315280215533392, 91.74246380123798872 ) ) ;
#18989=ORIENTED_EDGE ( 'NONE', *, *, #14926, .T. ) ;
#19000=EDGE_LOOP ( 'NONE', ( #19944, #16218, #9001, #19898 ) ) ;
#19002=EDGE_CURVE ( 'NONE', #15934, #10780, #14012, .T. ) ;
#19004=CARTESIAN_POINT ( 'NONE',  ( 4.394343283833276992, 39.11584570990505938, 92.75808880123797451 ) ) ;
#19021=CARTESIAN_POINT ( 'NONE',  ( -0.9988176903691428077, 49.83852402762217082, 93.30496380123798872 ) ) ;
#19034=CARTESIAN_POINT ( 'NONE',  ( -4.677846259693498432, 44.16218137147969003, 92.70661078214052964 ) ) ;
#19036=FACE_OUTER_BOUND ( 'NONE', #14820, .T. ) ;
#19040=CARTESIAN_POINT ( 'NONE',  ( 5.544968037009670780, 45.50804040601273925, 94.63308879953099506 ) ) ;
#19044=ORIENTED_EDGE ( 'NONE', *, *, #10411, .F. ) ;
#19049=DIRECTION ( 'NONE',  ( 1.000000000000000000, 0.000000000000000000, 0.000000000000000000 ) ) ;
#19051=CARTESIAN_POINT ( 'NONE',  ( 3.178197289651381485, 47.10421403348819780, 98.25514354869233102 ) ) ;
#19054=CARTESIAN_POINT ( 'NONE',  ( 0.5221537403065020788, 52.36218137147968577, 52.53721119516358584 ) ) ;
#19056=CARTESIAN_POINT ( 'NONE',  ( 2.043125170982144745, 38.48583871533720213, 91.27371380123798872 ) ) ;
#19063=CARTESIAN_POINT ( 'NONE',  ( -3.943187491250720544, 40.73580453397070755, 94.39871380294496817 ) ) ;
#19066=CARTESIAN_POINT ( 'NONE',  ( 31.07218010054375412, 42.76218137147968434, 69.80574467885101342 ) ) ;
#19075=CARTESIAN_POINT ( 'NONE',  ( 35.92215374030650565, 51.36218137147967866, 93.55433879953098142 ) ) ;
#19077=CARTESIAN_POINT ( 'NONE',  ( -4.524181921268124462, 40.28999182795290324, 94.78933880123798872 ) ) ;
#19084=VECTOR ( 'NONE', #1840, 1000.000000000000000 ) ;
#19088=CARTESIAN_POINT ( 'NONE',  ( -4.500660556396669065, 42.81632233694663370, 91.50808879953098085 ) ) ;
#19095=CARTESIAN_POINT ( 'NONE',  ( -0.2125050281363792815, 38.58189400963056670, 92.99246379953098085 ) ) ;
#19098=EDGE_LOOP ( 'NONE', ( #12326, #17896, #17639, #7839 ) ) ;
#19100=CARTESIAN_POINT ( 'NONE',  ( 6.014045509560256519, 43.93915269363458265, 95.05433879953099563 ) ) ;
#19105=DIRECTION ( 'NONE',  ( -1.000000000000000000, 0.000000000000000000, 0.000000000000000000 ) ) ;
#19106=ORIENTED_EDGE ( 'NONE', *, *, #19375, .F. ) ;
#19110=CARTESIAN_POINT ( 'NONE',  ( 33.61275266354798674, 51.36218137147967866, 93.55433879953098142 ) ) ;
#19112=CARTESIAN_POINT ( 'NONE',  ( -0.9988176903691428077, 49.83852402762217082, 95.64871380123798872 ) ) ;
#19117=CARTESIAN_POINT ( 'NONE',  ( 11.22215374030650281, 42.76218137147968434, 62.80715055817104542 ) ) ;
#19124=ORIENTED_EDGE ( 'NONE', *, *, #15039, .F. ) ;
#19128=CARTESIAN_POINT ( 'NONE',  ( -4.524181921268124462, 40.28999182795290324, 96.03933880123798872 ) ) ;
#19132=EDGE_CURVE ( 'NONE', #19783, #20542, #16189, .T. ) ;
#19136=DIRECTION ( 'NONE',  ( 0.4472135954999563734, 0.7745966692414840704, 0.4472135954999582608 ) ) ;
#19137=LINE ( 'NONE', #7651, #8475 ) ;
#19142=CARTESIAN_POINT ( 'NONE',  ( 1.352400422481993658, 50.46853102219002096, 90.72683880123797451 ) ) ;
#19143=EDGE_CURVE ( 'NONE', #13434, #3547, #1400, .T. ) ;
#19151=CARTESIAN_POINT ( 'NONE',  ( 30.92220646078100188, 45.56218137147968861, 56.80715055817104542 ) ) ;
#19154=EDGE_CURVE ( 'NONE', #16593, #17446, #17988, .T. ) ;
#19159=CARTESIAN_POINT ( 'NONE',  ( 4.987494971863720927, 47.58855820898865829, 91.27371380294496817 ) ) ;
#19160=VERTEX_POINT ( 'NONE', #15881 ) ;
#19164=DIRECTION ( 'NONE',  ( 1.000000000000000000, -0.000000000000000000, -0.000000000000000000 ) ) ;
#19165=CARTESIAN_POINT ( 'NONE',  ( 26.27839330960315678, 64.06566441348024910, 85.06527890720687424 ) ) ;
#19170=CARTESIAN_POINT ( 'NONE',  ( -5.154188915835984375, 42.64120994080404614, 95.96121380123798872 ) ) ;
#19174=ORIENTED_EDGE ( 'NONE', *, *, #20892, .F. ) ;
#19178=CARTESIAN_POINT ( 'NONE',  ( 1.352400422481993658, 50.46853102219002096, 93.22683880123798872 ) ) ;
#19183=PLANE ( 'NONE',  #11316 ) ;
#19184=ORIENTED_EDGE ( 'NONE', *, *, #3008, .T. ) ;
#19190=CARTESIAN_POINT ( 'NONE',  ( 2.043125170982144745, 38.48583871533720213, 91.42996380123798872 ) ) ;
#19204=CARTESIAN_POINT ( 'NONE',  ( 11.22215374030650281, 42.76218137147968434, 74.20433879953100131 ) ) ;
#19208=DIRECTION ( 'NONE',  ( 1.000000000000000000, 0.000000000000000000, -0.000000000000000000 ) ) ;
#19213=CARTESIAN_POINT ( 'NONE',  ( 31.22215374030650281, 42.76218137147968434, 77.80433879953099563 ) ) ;
#19216=DIRECTION ( 'NONE',  ( -0.7071067811865434649, -0.7071067811865515695, 0.000000000000000000 ) ) ;
#19218=ORIENTED_EDGE ( 'NONE', *, *, #15769, .T. ) ;
#19222=CARTESIAN_POINT ( 'NONE',  ( -5.154188915835984375, 42.64120994080404614, 95.96121380123798872 ) ) ;
#19224=CARTESIAN_POINT ( 'NONE',  ( 3.122153740306552905, 48.66551347115873227, 90.10183880294498238 ) ) ;
#19227=CARTESIAN_POINT ( 'NONE',  ( 13.32022995165973001, 51.36218137147968577, 92.39963826115175038 ) ) ;
#19232=EDGE_CURVE ( 'NONE', #17731, #10499, #13621, .T. ) ;
#19235=ADVANCED_FACE ( 'NONE', ( #9924 ), #13419, .F. ) ;
#19242=EDGE_CURVE ( 'NONE', #7731, #13604, #15012, .T. ) ;
#19247=DIRECTION ( 'NONE',  ( -0.4999999999999983347, -0.8660254037844395958, 0.000000000000000000 ) ) ;
#19248=CIRCLE ( 'NONE', #1590, 4.200000000000001066 ) ;
#19249=ORIENTED_EDGE ( 'NONE', *, *, #20873, .F. ) ;
#19257=ORIENTED_EDGE ( 'NONE', *, *, #10784, .F. ) ;
#19259=AXIS2_PLACEMENT_3D ( 'NONE', #19888, #11308, #115 ) ;
#19280=CARTESIAN_POINT ( 'NONE',  ( -5.784195910403845176, 44.99242805365518194, 93.53933880123797451 ) ) ;
#19290=CARTESIAN_POINT ( 'NONE',  ( -3.226449543290886179, 47.76606447477297479, 92.55433879953076826 ) ) ;
#19304=DIRECTION ( 'NONE',  ( -0.000000000000000000, -0.000000000000000000, -1.000000000000000000 ) ) ;
#19313=CARTESIAN_POINT ( 'NONE',  ( -3.943187491250720544, 40.73580453397070755, 96.58621379953099506 ) ) ;
#19320=DIRECTION ( 'NONE',  ( 1.000000000000000000, -1.193617070626243484E-16, 0.000000000000000000 ) ) ;
#19323=CARTESIAN_POINT ( 'NONE',  ( -5.154188915835984375, 42.64120994080404614, 92.36746380123797451 ) ) ;
#19329=CARTESIAN_POINT ( 'NONE',  ( -3.981178359372548492, 46.76218137147973408, 92.91433880294496817 ) ) ;
#19332=DIRECTION ( 'NONE',  ( 0.000000000000000000, 0.000000000000000000, 1.000000000000000000 ) ) ;
#19341=LINE ( 'NONE', #293, #14861 ) ;
#19346=CARTESIAN_POINT ( 'NONE',  ( -5.154188915835984375, 42.64120994080404614, 93.46121380123805977 ) ) ;
#19352=EDGE_CURVE ( 'NONE', #531, #14061, #4144, .T. ) ;
#19355=FACE_OUTER_BOUND ( 'NONE', #4606, .T. ) ;
#19357=EDGE_CURVE ( 'NONE', #11321, #10416, #14044, .T. ) ;
#19372=VERTEX_POINT ( 'NONE', #20623 ) ;
#19373=CARTESIAN_POINT ( 'NONE',  ( 3.460444912181559474, 49.25145096859824889, 94.24246380123798872 ) ) ;
#19374=AXIS2_PLACEMENT_3D ( 'NONE', #18389, #2121, #510 ) ;
#19375=EDGE_CURVE ( 'NONE', #19551, #15771, #4242, .T. ) ;
#19376=CARTESIAN_POINT ( 'NONE',  ( 4.394343283833276992, 39.11584570990505938, 91.35183880123798872 ) ) ;
#19388=CARTESIAN_POINT ( 'NONE',  ( 6.828503391016846891, 43.33193468930419101, 91.66433880123796030 ) ) ;
#19390=EDGE_LOOP ( 'NONE', ( #70, #19420, #3973, #14054 ) ) ;
#19393=CARTESIAN_POINT ( 'NONE',  ( 4.208451567978901409, 39.70256125636758071, 92.55433879953093879 ) ) ;
#19399=VERTEX_POINT ( 'NONE', #20424 ) ;
#19413=DIRECTION ( 'NONE',  ( 0.4999999999999981126, -0.8660254037844397068, -0.000000000000000000 ) ) ;
#19414=FACE_OUTER_BOUND ( 'NONE', #11948, .T. ) ;
#19417=EDGE_LOOP ( 'NONE', ( #8258, #5051, #19044, #15484 ) ) ;
#19418=CARTESIAN_POINT ( 'NONE',  ( 2.263363662449358493, 49.77488197367694767, 94.44231768333818877 ) ) ;
#19420=ORIENTED_EDGE ( 'NONE', *, *, #10805, .F. ) ;
#19424=CARTESIAN_POINT ( 'NONE',  ( 5.025485839985549319, 41.56218137147963887, 95.72683879953099506 ) ) ;
#19439=VECTOR ( 'NONE', #3719, 1000.000000000000000 ) ;
#19446=ORIENTED_EDGE ( 'NONE', *, *, #3381, .T. ) ;
#19460=CARTESIAN_POINT ( 'NONE',  ( 1.352400422481993658, 50.46853102219002096, 91.82058880123801714 ) ) ;
#19461=ORIENTED_EDGE ( 'NONE', *, *, #7004, .T. ) ;
#19472=CARTESIAN_POINT ( 'NONE',  ( 11.22215374030650281, 42.96218137147968008, 61.80715055817104542 ) ) ;
#19477=VECTOR ( 'NONE', #9374, 1000.000000000000000 ) ;
#19479=CARTESIAN_POINT ( 'NONE',  ( 3.122153740306552905, 48.66551347115873227, 95.10183880294498238 ) ) ;
#19480=CARTESIAN_POINT ( 'NONE',  ( 11.22215374030649926, 42.76218137147968434, 77.80433879953099563 ) ) ;
#19482=EDGE_CURVE ( 'NONE', #972, #10052, #20309, .T. ) ;
#19486=CARTESIAN_POINT ( 'NONE',  ( 0.5221537403065010796, 44.16218137147969003, 92.55433879953098142 ) ) ;
#19490=CARTESIAN_POINT ( 'NONE',  ( -3.350035803220276609, 49.20851703305431357, 92.13308880123798872 ) ) ;
#19491=CARTESIAN_POINT ( 'NONE',  ( 5.611423337425062385, 41.22389019960463230, 93.92996380123798872 ) ) ;
#19493=EDGE_CURVE ( 'NONE', #16288, #5383, #13730, .T. ) ;
#19496=CARTESIAN_POINT ( 'NONE',  ( 5.438522061964698118, 41.32291878214397940, 92.55433879953102405 ) ) ;
#19498=EDGE_CURVE ( 'NONE', #13415, #11839, #5635, .T. ) ;
#19502=DIRECTION ( 'NONE',  ( 1.000000000000000000, 0.000000000000000000, 0.000000000000000000 ) ) ;
#19503=VERTEX_POINT ( 'NONE', #20527 ) ;
#19508=DIRECTION ( 'NONE',  ( -0.000000000000000000, -0.000000000000000000, 1.000000000000000000 ) ) ;
#19510=FACE_OUTER_BOUND ( 'NONE', #20057, .T. ) ;
#19520=CARTESIAN_POINT ( 'NONE',  ( 2.877538411150256437, 49.16070722497604351, 92.79646262933300704 ) ) ;
#19522=ORIENTED_EDGE ( 'NONE', *, *, #1121, .T. ) ;
#19523=CARTESIAN_POINT ( 'NONE',  ( -4.567115856812060670, 47.10047254335474065, 93.46121380123797451 ) ) ;
#19524=CARTESIAN_POINT ( 'NONE',  ( 2.916646314871006229, 38.79555996194933698, 95.05433879953095300 ) ) ;
#19528=CARTESIAN_POINT ( 'NONE',  ( -3.943187491250720544, 40.73580453397070755, 92.83621379953099506 ) ) ;
#19535=DIRECTION ( 'NONE',  ( 1.000000000000000000, 0.000000000000000000, -0.000000000000000000 ) ) ;
#19536=CARTESIAN_POINT ( 'NONE',  ( 2.898327458951320157, 49.13991817717495536, 94.03907478705464484 ) ) ;
#19545=LINE ( 'NONE', #12961, #15636 ) ;
#19546=CARTESIAN_POINT ( 'NONE',  ( -2.503296703960774305, 48.49064145155254124, 94.11279910766216972 ) ) ;
#19549=ORIENTED_EDGE ( 'NONE', *, *, #2550, .F. ) ;
#19550=CARTESIAN_POINT ( 'NONE',  ( 10.77494014480653561, 42.96218137147968008, 74.20433879953100131 ) ) ;
#19551=VERTEX_POINT ( 'NONE', #17859 ) ;
#19552=DIRECTION ( 'NONE',  ( -1.000000000000000000, 3.304235192336774723E-15, 0.000000000000000000 ) ) ;
#19553=DIRECTION ( 'NONE',  ( -0.000000000000000000, -0.000000000000000000, 1.000000000000000000 ) ) ;
#19554=LINE ( 'NONE', #6787, #6876 ) ;
#19555=CARTESIAN_POINT ( 'NONE',  ( -4.677846259693496656, 44.16218127507082158, 94.26911326394257173 ) ) ;
#19557=CARTESIAN_POINT ( 'NONE',  ( -4.567115856812060670, 47.10047254335474065, 93.30496380123805977 ) ) ;
#19561=CARTESIAN_POINT ( 'NONE',  ( -3.350035803220276609, 49.20851703305431357, 91.97683880123797451 ) ) ;
#19569=VERTEX_POINT ( 'NONE', #12862 ) ;
#19578=ORIENTED_EDGE ( 'NONE', *, *, #15039, .T. ) ;
#19579=CARTESIAN_POINT ( 'NONE',  ( 2.043125170982144745, 38.48583871533720213, 92.52371380123798872 ) ) ;
#19580=DIRECTION ( 'NONE',  ( -0.000000000000000000, -0.000000000000000000, 1.000000000000000000 ) ) ;
#19586=EDGE_LOOP ( 'NONE', ( #7007, #7031, #18806, #14661 ) ) ;
#19594=LINE ( 'NONE', #18011, #1806 ) ;
#19597=LINE ( 'NONE', #1750, #7449 ) ;
#19599=ORIENTED_EDGE ( 'NONE', *, *, #6156, .T. ) ;
#19600=PLANE ( 'NONE',  #3396 ) ;
#19608=LINE ( 'NONE', #18968, #10960 ) ;
#19616=VECTOR ( 'NONE', #20100, 1000.000000000000000 ) ;
#19620=CARTESIAN_POINT ( 'NONE',  ( 31.22215374030650281, 42.96218137147968008, 73.80433879953100984 ) ) ;
#19623=CARTESIAN_POINT ( 'NONE',  ( -2.416137431568557314, 39.07291177436112406, 96.27371380123797451 ) ) ;
#19625=ORIENTED_EDGE ( 'NONE', *, *, #4652, .T. ) ;
#19629=CARTESIAN_POINT ( 'NONE',  ( -2.077846259693550746, 39.65884927180063357, 94.16433879953098085 ) ) ;
#19631=CARTESIAN_POINT ( 'NONE',  ( 31.22215374030650281, 42.76218137147968434, 72.80433879953100984 ) ) ;
#19636=CARTESIAN_POINT ( 'NONE',  ( 11.22215374030649926, 42.76218137147968434, 80.55433879953099563 ) ) ;
#19649=ORIENTED_EDGE ( 'NONE', *, *, #20989, .F. ) ;
#19650=VECTOR ( 'NONE', #11845, 1000.000000000000000 ) ;
#19654=ORIENTED_EDGE ( 'NONE', *, *, #20150, .T. ) ;
#19655=CARTESIAN_POINT ( 'NONE',  ( -5.368445182934982185, 36.96218137147968008, 93.55433879953098142 ) ) ;
#19660=CARTESIAN_POINT ( 'NONE',  ( -4.524181921268124462, 40.28999182795290324, 93.53933880123804556 ) ) ;
#19665=CARTESIAN_POINT ( 'NONE',  ( 5.611423337425062385, 41.22389019960463230, 91.42996380123798872 ) ) ;
#19666=ORIENTED_EDGE ( 'NONE', *, *, #4537, .T. ) ;
#19678=LINE ( 'NONE', #1724, #16279 ) ;
#19680=CARTESIAN_POINT ( 'NONE',  ( -7.677846259693480668, 36.96218137147968008, 95.05433879953098142 ) ) ;
#19687=CARTESIAN_POINT ( 'NONE',  ( 5.568489401881125289, 48.03437091500646261, 91.66433880123796030 ) ) ;
#19690=EDGE_CURVE ( 'NONE', #15667, #7917, #11703, .T. ) ;
#19691=CARTESIAN_POINT ( 'NONE',  ( 6.828503391016846891, 43.33193468930419101, 92.75808880123800293 ) ) ;
#19693=AXIS2_PLACEMENT_3D ( 'NONE', #3660, #11665, #13250 ) ;
#19700=CARTESIAN_POINT ( 'NONE',  ( 6.198496396448986090, 45.68315280215533392, 90.49246380123798872 ) ) ;
#19722=EDGE_CURVE ( 'NONE', #15570, #19783, #11909, .T. ) ;
#19723=ORIENTED_EDGE ( 'NONE', *, *, #13413, .T. ) ;
#19727=CARTESIAN_POINT ( 'NONE',  ( 2.263363662449363822, 49.77488197367694767, 93.11419268333823140 ) ) ;
#19728=CARTESIAN_POINT ( 'NONE',  ( -0.4699484075730042676, 52.36218137147968577, 52.53721119516358584 ) ) ;
#19729=CARTESIAN_POINT ( 'NONE',  ( 3.948530577815480225, 39.69684013992245752, 93.14871379953099506 ) ) ;
#19730=EDGE_LOOP ( 'NONE', ( #10942, #12384, #5400, #2014, #12407, #4672, #2415 ) ) ;
#19735=CARTESIAN_POINT ( 'NONE',  ( -0.8237052942265477018, 49.18499566818285018, 94.94558879953099506 ) ) ;
#19736=ORIENTED_EDGE ( 'NONE', *, *, #11832, .T. ) ;
#19739=FACE_OUTER_BOUND ( 'NONE', #6421, .T. ) ;
#19748=ORIENTED_EDGE ( 'NONE', *, *, #2595, .F. ) ;
#19751=CARTESIAN_POINT ( 'NONE',  ( -2.829262219629336883, 48.16467593588394891, 94.09494095006277803 ) ) ;
#19758=LINE ( 'NONE', #8708, #6038 ) ;
#19762=EDGE_CURVE ( 'NONE', #13095, #10052, #19554, .T. ) ;
#19763=DIRECTION ( 'NONE',  ( -1.402518428993831676E-16, 1.000000000000000000, -1.677918375355662166E-32 ) ) ;
#19764=DIRECTION ( 'NONE',  ( 1.402518428993831676E-16, -1.000000000000000000, 0.000000000000000000 ) ) ;
#19770=CARTESIAN_POINT ( 'NONE',  ( 5.568489401881125289, 48.03437091500646261, 90.41433880123798872 ) ) ;
#19771=VECTOR ( 'NONE', #7997, 1000.000000000000000 ) ;
#19773=CARTESIAN_POINT ( 'NONE',  ( -5.154188915835984375, 42.64120994080404614, 90.96121380123797451 ) ) ;
#19783=VERTEX_POINT ( 'NONE', #15097 ) ;
#19792=ORIENTED_EDGE ( 'NONE', *, *, #15109, .F. ) ;
#19793=CARTESIAN_POINT ( 'NONE',  ( -2.077846259693550746, 39.65884927180063357, 94.47683880294496817 ) ) ;
#19796=VECTOR ( 'NONE', #17801, 1000.000000000000000 ) ;
#19797=CARTESIAN_POINT ( 'NONE',  ( -2.416137431568557314, 39.07291177436112406, 91.27371380123798872 ) ) ;
#19799=ORIENTED_EDGE ( 'NONE', *, *, #18570, .T. ) ;
#19800=DIRECTION ( 'NONE',  ( 0.000000000000000000, 0.000000000000000000, 1.000000000000000000 ) ) ;
#19801=EDGE_LOOP ( 'NONE', ( #17436, #16029, #3198, #19921 ) ) ;
#19804=CARTESIAN_POINT ( 'NONE',  ( 3.460444912181559474, 49.25145096859824889, 95.49246380123798872 ) ) ;
#19809=CARTESIAN_POINT ( 'NONE',  ( 5.815517440877807864, 45.28237139676105016, 92.55433879953096721 ) ) ;
#19828=FACE_BOUND ( 'NONE', #16688, .T. ) ;
#19829=CARTESIAN_POINT ( 'NONE',  ( 3.948530577815480225, 39.69684013992245752, 94.39871379953098085 ) ) ;
#19834=PLANE ( 'NONE',  #4680 ) ;
#19835=LINE ( 'NONE', #3668, #17642 ) ;
#19836=CARTESIAN_POINT ( 'NONE',  ( 5.025485839985549319, 41.56218137147963887, 91.97683879953100927 ) ) ;
#19837=ORIENTED_EDGE ( 'NONE', *, *, #20369, .F. ) ;
#19839=ORIENTED_EDGE ( 'NONE', *, *, #7931, .F. ) ;
#19843=( BOUNDED_CURVE ( )  B_SPLINE_CURVE ( 2, ( #2759, #9360, #19329, #14131, #4747 ),
 .UNSPECIFIED., .F., .F. ) 
 B_SPLINE_CURVE_WITH_KNOTS ( ( 3, 2, 3 ),
 ( 0.4514241053481902743, 0.4687348658651156463, 0.4774649324440010667 ),
 .UNSPECIFIED. ) 
 CURVE ( )  GEOMETRIC_REPRESENTATION_ITEM ( )  RATIONAL_B_SPLINE_CURVE ( ( 0.9660722094251321668, 0.9493985640418991512, 1.000000000000000000, 0.9744809649195071977, 0.9660722070856953003 ) ) 
 REPRESENTATION_ITEM ( '' )  );
#19847=ORIENTED_EDGE ( 'NONE', *, *, #19690, .T. ) ;
#19853=DIRECTION ( 'NONE',  ( 1.402518428993831676E-16, -1.000000000000000000, -0.000000000000000000 ) ) ;
#19855=CARTESIAN_POINT ( 'NONE',  ( -2.416137431568557314, 39.07291177436112406, 93.77371380123797451 ) ) ;
#19857=ORIENTED_EDGE ( 'NONE', *, *, #19375, .T. ) ;
#19870=CARTESIAN_POINT ( 'NONE',  ( 5.568489401881125289, 48.03437091500646261, 92.91433880123798872 ) ) ;
#19872=EDGE_CURVE ( 'NONE', #7261, #8801, #8927, .T. ) ;
#19875=EDGE_CURVE ( 'NONE', #18535, #4997, #15416, .T. ) ;
#19876=ORIENTED_EDGE ( 'NONE', *, *, #9988, .F. ) ;
#19877=DIRECTION ( 'NONE',  ( -0.8660254037844351549, -1.050845190663206368E-16, 0.5000000000000061062 ) ) ;
#19878=LINE ( 'NONE', #18399, #6167 ) ;
#19880=CARTESIAN_POINT ( 'NONE',  ( 6.198496396448986090, 45.68315280215533392, 95.49246380123798872 ) ) ;
#19885=LINE ( 'NONE', #18193, #2021 ) ;
#19888=CARTESIAN_POINT ( 'NONE',  ( 0.5221537403065020788, 52.36218137147968577, 87.21440135111343750 ) ) ;
#19890=ORIENTED_EDGE ( 'NONE', *, *, #19132, .T. ) ;
#19891=CARTESIAN_POINT ( 'NONE',  ( -4.970565407269693203, 43.69858568107365926, 95.05433879953102405 ) ) ;
#19893=CARTESIAN_POINT ( 'NONE',  ( 5.025485839985549319, 41.56218137147963887, 94.78933880294496817 ) ) ;
#19895=CARTESIAN_POINT ( 'NONE',  ( -5.154188915835984375, 42.64120994080404614, 95.96121380123798872 ) ) ;
#19897=CARTESIAN_POINT ( 'NONE',  ( -1.219056181836354558, 49.77488197367695477, 93.23425466814931895 ) ) ;
#19898=ORIENTED_EDGE ( 'NONE', *, *, #12626, .F. ) ;
#19900=DIRECTION ( 'NONE',  ( 0.000000000000000000, 1.000000000000000000, 1.734723475976787846E-14 ) ) ;
#19904=CARTESIAN_POINT ( 'NONE',  ( -2.416137431568557314, 39.07291177436112406, 92.36746380123797451 ) ) ;
#19909=VECTOR ( 'NONE', #17470, 1000.000000000000000 ) ;
#19921=ORIENTED_EDGE ( 'NONE', *, *, #6737, .T. ) ;
#19922=CARTESIAN_POINT ( 'NONE',  ( 13.32277635493561974, 51.36218137147968577, 93.55433879953098142 ) ) ;
#19926=CARTESIAN_POINT ( 'NONE',  ( -0.2125050281363792815, 38.58189400963055959, 95.49246379953098085 ) ) ;
#19927=CARTESIAN_POINT ( 'NONE',  ( 5.544968037009670780, 45.50804040601273925, 94.63308879953099506 ) ) ;
#19935=VERTEX_POINT ( 'NONE', #2639 ) ;
#19940=CARTESIAN_POINT ( 'NONE',  ( 3.544512597232735818, 48.49373303889355213, 93.87251462254160117 ) ) ;
#19944=ORIENTED_EDGE ( 'NONE', *, *, #6328, .F. ) ;
#19951=CARTESIAN_POINT ( 'NONE',  ( 5.568489401881125289, 48.03437091500646261, 95.57058880123798872 ) ) ;
#19952=ORIENTED_EDGE ( 'NONE', *, *, #8307, .T. ) ;
#19953=DIRECTION ( 'NONE',  ( -0.000000000000000000, -0.000000000000000000, 1.000000000000000000 ) ) ;
#19958=CARTESIAN_POINT ( 'NONE',  ( 4.658006975973914443, 39.57252462080383992, 92.61876351041205169 ) ) ;
#19959=FACE_OUTER_BOUND ( 'NONE', #16890, .T. ) ;
#19961=EDGE_CURVE ( 'NONE', #4927, #15997, #20506, .T. ) ;
#19962=CARTESIAN_POINT ( 'NONE',  ( -0.9988176903691428077, 49.83852402762217082, 95.80496380123798872 ) ) ;
#19967=CARTESIAN_POINT ( 'NONE',  ( 5.722153740306477054, 44.16218185475116798, 93.64411094854726514 ) ) ;
#19968=CARTESIAN_POINT ( 'NONE',  ( 2.043125170982144745, 38.48583871533720213, 91.27371380123798872 ) ) ;
#19969=DIRECTION ( 'NONE',  ( -1.621236893436268647E-16, -2.273814620809075225E-32, 1.000000000000000000 ) ) ;
#19972=AXIS2_PLACEMENT_3D ( 'NONE', #18653, #20343, #2493 ) ;
#19973=ORIENTED_EDGE ( 'NONE', *, *, #18361, .F. ) ;
#19978=CARTESIAN_POINT ( 'NONE',  ( -4.567115856812060670, 47.10047254335474065, 92.21121380123797451 ) ) ;
#19983=CARTESIAN_POINT ( 'NONE',  ( 1.868012774839550749, 39.13936707477651566, 93.38308880294498238 ) ) ;
#19984=ORIENTED_EDGE ( 'NONE', *, *, #13645, .T. ) ;
#19991=CARTESIAN_POINT ( 'NONE',  ( -3.226449543290803135, 47.76606447477306716, 95.05433879953076826 ) ) ;
#19992=CARTESIAN_POINT ( 'NONE',  ( 1.256812508749381774, 49.74246873332880625, 90.17996380294496817 ) ) ;
#19994=CARTESIAN_POINT ( 'NONE',  ( -0.3080929418689875576, 37.85583172076933778, 93.69558880123800293 ) ) ;
#19998=VECTOR ( 'NONE', #13023, 1000.000000000000000 ) ;
#20000=CARTESIAN_POINT ( 'NONE',  ( 31.07218010054375412, 42.96218137147968008, 65.80574467885102763 ) ) ;
#20001=CARTESIAN_POINT ( 'NONE',  ( -5.784195910403845176, 44.99242805365518194, 92.13308880123798872 ) ) ;
#20009=CARTESIAN_POINT ( 'NONE',  ( -0.4699484075730042676, 52.36218137147968577, 48.36106904222365444 ) ) ;
#20010=VERTEX_POINT ( 'NONE', #7853 ) ;
#20017=CARTESIAN_POINT ( 'NONE',  ( 31.22215374030650281, 42.76218137147968434, 77.40433879953098995 ) ) ;
#20024=ADVANCED_FACE ( 'NONE', ( #7955 ), #17529, .F. ) ;
#20028=ORIENTED_EDGE ( 'NONE', *, *, #412, .F. ) ;
#20030=ORIENTED_EDGE ( 'NONE', *, *, #16600, .F. ) ;
#20032=CARTESIAN_POINT ( 'NONE',  ( -0.2125050281363792815, 38.58189400963055959, 94.24246379953099506 ) ) ;
#20033=CARTESIAN_POINT ( 'NONE',  ( 3.122153740306552905, 48.66551347115873227, 93.53933879953099506 ) ) ;
#20040=ORIENTED_EDGE ( 'NONE', *, *, #3917, .T. ) ;
#20043=ORIENTED_EDGE ( 'NONE', *, *, #15630, .F. ) ;
#20044=LINE ( 'NONE', #904, #2385 ) ;
#20045=CARTESIAN_POINT ( 'NONE',  ( -4.524181921268124462, 40.28999182795290324, 93.69558880123800293 ) ) ;
#20046=VECTOR ( 'NONE', #12877, 1000.000000000000000 ) ;
#20050=CARTESIAN_POINT ( 'NONE',  ( -5.154188915835984375, 42.64120994080404614, 90.96121380123797451 ) ) ;
#20051=SHAPE_DEFINITION_REPRESENTATION ( #16862, #333 ) ;
#20057=EDGE_LOOP ( 'NONE', ( #17386, #2002, #15066, #3220 ) ) ;
#20074=CARTESIAN_POINT ( 'NONE',  ( -0.3080929418689875576, 37.85583172076933778, 95.10183880123796030 ) ) ;
#20079=CARTESIAN_POINT ( 'NONE',  ( 3.460444912181559474, 49.25145096859824889, 94.24246380123798872 ) ) ;
#20085=DIRECTION ( 'NONE',  ( 1.193617070626243484E-16, 1.000000000000000000, 0.000000000000000000 ) ) ;
#20087=CARTESIAN_POINT ( 'NONE',  ( -0.9988176903691428077, 49.83852402762217082, 94.55496380123798872 ) ) ;
#20089=LINE ( 'NONE', #8727, #18711 ) ;
#20090=DIRECTION ( 'NONE',  ( -1.000000000000000000, -1.621236893436269386E-16, 0.000000000000000000 ) ) ;
#20091=CARTESIAN_POINT ( 'NONE',  ( 11.22215374030650281, 42.76218137147968434, 56.80715055817104542 ) ) ;
#20093=ORIENTED_EDGE ( 'NONE', *, *, #2211, .T. ) ;
#20098=ORIENTED_EDGE ( 'NONE', *, *, #12464, .T. ) ;
#20100=DIRECTION ( 'NONE',  ( -0.000000000000000000, -0.000000000000000000, 1.000000000000000000 ) ) ;
#20103=CARTESIAN_POINT ( 'NONE',  ( 1.868012774839550749, 39.13936707477651566, 90.88308880294496817 ) ) ;
#20106=CARTESIAN_POINT ( 'NONE',  ( 3.122075258343615545, 38.59543968120053847, 90.21201841395856036 ) ) ;
#20107=VECTOR ( 'NONE', #1134, 1000.000000000000000 ) ;
#20109=EDGE_LOOP ( 'NONE', ( #4315, #16208, #11335, #20828 ) ) ;
#20110=VECTOR ( 'NONE', #6383, 1000.000000000000000 ) ;
#20112=ORIENTED_EDGE ( 'NONE', *, *, #19482, .F. ) ;
#20115=CARTESIAN_POINT ( 'NONE',  ( -4.524181921268124462, 40.28999182795290324, 93.53933880123797451 ) ) ;
#20118=DIRECTION ( 'NONE',  ( 0.000000000000000000, 0.000000000000000000, 1.000000000000000000 ) ) ;
#20120=FACE_OUTER_BOUND ( 'NONE', #5500, .T. ) ;
#20125=VECTOR ( 'NONE', #20600, 1000.000000000000000 ) ;
#20128=LINE ( 'NONE', #8767, #10109 ) ;
#20142=CARTESIAN_POINT ( 'NONE',  ( -5.058133621542618030, 44.89684013992257405, 95.17996379953099506 ) ) ;
#20143=CARTESIAN_POINT ( 'NONE',  ( -2.904223097202481174, 48.62752260303690122, 92.52371379953099506 ) ) ;
#20145=CARTESIAN_POINT ( 'NONE',  ( -0.9988176903691428077, 49.83852402762217082, 94.55496380123798872 ) ) ;
#20147=EDGE_LOOP ( 'NONE', ( #15832, #12631, #7056, #4046, #1849, #284, #11587 ) ) ;
#20150=EDGE_CURVE ( 'NONE', #13576, #1059, #5367, .T. ) ;
#20154=CARTESIAN_POINT ( 'NONE',  ( 2.043125170982144745, 38.48583871533720213, 93.92996380123798872 ) ) ;
#20160=CARTESIAN_POINT ( 'NONE',  ( 4.454354847297358866, 39.79502961122975790, 90.11785626197793420 ) ) ;
#20163=DIRECTION ( 'NONE',  ( 1.000000000000000000, -0.000000000000000000, -0.000000000000000000 ) ) ;
#20174=EDGE_CURVE ( 'NONE', #14996, #16593, #6963, .T. ) ;
#20181=CARTESIAN_POINT ( 'NONE',  ( 0.5221537403065097394, 44.16218137147969003, 111.0905869729573681 ) ) ;
#20183=CARTESIAN_POINT ( 'NONE',  ( 5.568489401881125289, 48.03437091500646261, 94.32058880123798872 ) ) ;
#20185=LINE ( 'NONE', #17005, #9517 ) ;
#20187=CARTESIAN_POINT ( 'NONE',  ( -4.500660556396669065, 42.81632233694663370, 91.82058880294496817 ) ) ;
#20190=ORIENTED_EDGE ( 'NONE', *, *, #16162, .F. ) ;
#20194=CARTESIAN_POINT ( 'NONE',  ( 1.352400422481993658, 50.46853102219002096, 95.72683880123798872 ) ) ;
#20195=CARTESIAN_POINT ( 'NONE',  ( 11.22215374030650281, 42.96218137147968008, 61.40715055817103263 ) ) ;
#20203=CARTESIAN_POINT ( 'NONE',  ( 31.22215374030650281, 45.56218137147968861, 72.80433879953100984 ) ) ;
#20204=CARTESIAN_POINT ( 'NONE',  ( -5.154188915835984375, 42.64120994080404614, 94.86746380123797451 ) ) ;
#20207=CARTESIAN_POINT ( 'NONE',  ( 4.987494971863720927, 47.58855820898865829, 91.27371380294496817 ) ) ;
#20209=CARTESIAN_POINT ( 'NONE',  ( -2.416137431568557314, 39.07291177436112406, 91.11746380123798872 ) ) ;
#20215=CARTESIAN_POINT ( 'NONE',  ( -5.784195910403845176, 44.99242805365518194, 93.38308880123798872 ) ) ;
#20216=ORIENTED_EDGE ( 'NONE', *, *, #7104, .T. ) ;
#20223=ORIENTED_EDGE ( 'NONE', *, *, #12126, .T. ) ;
#20226=ORIENTED_EDGE ( 'NONE', *, *, #12574, .T. ) ;
#20227=LINE ( 'NONE', #15465, #17274 ) ;
#20230=EDGE_CURVE ( 'NONE', #18234, #970, #5160, .T. ) ;
#20233=DIRECTION ( 'NONE',  ( 1.402518428993854849E-16, -1.000000000000000000, -1.734723475976787846E-14 ) ) ;
#20237=ORIENTED_EDGE ( 'NONE', *, *, #14440, .F. ) ;
#20241=EDGE_CURVE ( 'NONE', #16818, #2422, #3529, .T. ) ;
#20242=CARTESIAN_POINT ( 'NONE',  ( 1.868012774839550749, 39.13936707477651566, 93.07058879953099506 ) ) ;
#20245=CARTESIAN_POINT ( 'NONE',  ( -4.567115856812060670, 47.10047254335474065, 92.21121380123797451 ) ) ;
#20249=PLANE ( 'NONE',  #14595 ) ;
#20251=EDGE_LOOP ( 'NONE', ( #18785, #13150, #18358, #16296, #20353, #997, #17786, #4281, #17489, #1664, #5998, #10869 ) ) ;
#20257=CARTESIAN_POINT ( 'NONE',  ( -4.567115856812060670, 47.10047254335474065, 90.80496380123797451 ) ) ;
#20270=CARTESIAN_POINT ( 'NONE',  ( 5.568489401881125289, 48.03437091500646261, 90.57058880123798872 ) ) ;
#20272=ORIENTED_EDGE ( 'NONE', *, *, #17676, .F. ) ;
#20283=DIRECTION ( 'NONE',  ( -1.334402673828313339E-16, -1.619179559944692391E-32, 1.000000000000000000 ) ) ;
#20285=ADVANCED_FACE ( 'NONE', ( #3882 ), #13568, .F. ) ;
#20289=CARTESIAN_POINT ( 'NONE',  ( -2.077846259693550746, 39.65884927180063357, 94.47683880294496817 ) ) ;
#20290=DIRECTION ( 'NONE',  ( -1.000000000000000000, 0.000000000000000000, 0.000000000000000000 ) ) ;
#20293=EDGE_CURVE ( 'NONE', #3130, #19551, #5480, .T. ) ;
#20296=DIRECTION ( 'NONE',  ( 0.000000000000000000, -0.000000000000000000, 1.000000000000000000 ) ) ;
#20299=CARTESIAN_POINT ( 'NONE',  ( -5.784195910403845176, 44.99242805365518194, 93.53933880123797451 ) ) ;
#20309=LINE ( 'NONE', #13831, #15027 ) ;
#20311=CARTESIAN_POINT ( 'NONE',  ( -4.007284936692978583, 40.69155966471626584, 95.05433879953098142 ) ) ;
#20313=CARTESIAN_POINT ( 'NONE',  ( 6.722153740306509917, 44.16218137147969003, 92.55433879953098142 ) ) ;
#20319=B_SPLINE_CURVE_WITH_KNOTS ( 'NONE', 3,
 ( #2155, #10040, #8654, #16312, #18314, #14807 ),
 .UNSPECIFIED., .F., .F.,
 ( 4, 2, 4 ),
 ( 0.000000000000000000, 0.001381092432504990586, 0.002762184865009981172 ),
 .UNSPECIFIED. ) ;
#20321=ORIENTED_EDGE ( 'NONE', *, *, #3917, .F. ) ;
#20325=CARTESIAN_POINT ( 'NONE',  ( 6.828503391016846891, 43.33193468930419101, 91.50808880123798872 ) ) ;
#20327=PLANE ( 'NONE',  #9628 ) ;
#20329=LINE ( 'NONE', #10585, #6386 ) ;
#20341=DIRECTION ( 'NONE',  ( 1.402518428993831676E-16, -1.000000000000000000, 0.000000000000000000 ) ) ;
#20343=DIRECTION ( 'NONE',  ( 0.000000000000000000, 0.000000000000000000, 1.000000000000000000 ) ) ;
#20345=DIRECTION ( 'NONE',  ( 1.196361017915039239E-16, 0.000000000000000000, -1.000000000000000000 ) ) ;
#20349=ORIENTED_EDGE ( 'NONE', *, *, #11741, .F. ) ;
#20352=CARTESIAN_POINT ( 'NONE',  ( 1.868012774839550749, 39.13936707477651566, 91.82058879953099506 ) ) ;
#20353=ORIENTED_EDGE ( 'NONE', *, *, #16339, .T. ) ;
#20354=EDGE_CURVE ( 'NONE', #8963, #1387, #8162, .T. ) ;
#20356=CARTESIAN_POINT ( 'NONE',  ( -2.416137431568557314, 39.07291177436112406, 93.77371380123797451 ) ) ;
#20364=AXIS2_PLACEMENT_3D ( 'NONE', #280, #3791, #183 ) ;
#20369=EDGE_CURVE ( 'NONE', #6553, #4848, #7067, .T. ) ;
#20373=AXIS2_PLACEMENT_3D ( 'NONE', #16330, #19508, #11546 ) ;
#20377=EDGE_LOOP ( 'NONE', ( #14107, #12525, #9432, #19549 ) ) ;
#20383=CARTESIAN_POINT ( 'NONE',  ( -4.567115856812060670, 47.10047254335474065, 90.96121380123797451 ) ) ;
#20389=FACE_OUTER_BOUND ( 'NONE', #13746, .T. ) ;
#20398=CARTESIAN_POINT ( 'NONE',  ( 5.568489401881125289, 48.03437091500646261, 95.57058880123798872 ) ) ;
#20403=CARTESIAN_POINT ( 'NONE',  ( -3.981178359372548492, 46.76218137147973408, 92.91433880294496817 ) ) ;
#20404=VECTOR ( 'NONE', #5730, 1000.000000000000000 ) ;
#20411=DIRECTION ( 'NONE',  ( 0.000000000000000000, -1.000000000000000000, 0.000000000000000000 ) ) ;
#20412=DIRECTION ( 'NONE',  ( 0.000000000000000000, -1.000000000000000000, 0.000000000000000000 ) ) ;
#20422=DIRECTION ( 'NONE',  ( -0.000000000000000000, -0.000000000000000000, -1.000000000000000000 ) ) ;
#20424=CARTESIAN_POINT ( 'NONE',  ( 1.514255888186003984, 52.36218137147968577, 87.21440135111343750 ) ) ;
#20429=CARTESIAN_POINT ( 'NONE',  ( -4.500660556396669065, 42.81632233694663370, 93.07058880294496817 ) ) ;
#20433=LINE ( 'NONE', #5862, #11205 ) ;
#20434=CARTESIAN_POINT ( 'NONE',  ( 4.454354847297358866, 39.79502961122975790, 90.11785626197793420 ) ) ;
#20442=CARTESIAN_POINT ( 'NONE',  ( 1.256812508749381774, 49.74246873332880625, 90.17996380294496817 ) ) ;
#20445=CARTESIAN_POINT ( 'NONE',  ( -3.154801521863568325, 47.83913663364971569, 95.05433879953098142 ) ) ;
#20450=ORIENTED_EDGE ( 'NONE', *, *, #11294, .F. ) ;
#20453=ORIENTED_EDGE ( 'NONE', *, *, #8083, .T. ) ;
#20455=CARTESIAN_POINT ( 'NONE',  ( 10.77494014480653917, 42.96218137147968008, 58.20715055817105110 ) ) ;
#20466=CARTESIAN_POINT ( 'NONE',  ( 4.613683346302097199, 40.84891852973634485, 90.69696562749766144 ) ) ;
#20469=CARTESIAN_POINT ( 'NONE',  ( -0.3080929418689875576, 37.85583172076933778, 95.10183880123796030 ) ) ;
#20470=CARTESIAN_POINT ( 'NONE',  ( -1.219056181836354558, 49.77488197367695477, 94.40612966814926210 ) ) ;
#20479=CARTESIAN_POINT ( 'NONE',  ( -0.3080929418689875576, 37.85583172076933778, 92.60183880123797451 ) ) ;
#20487=AXIS2_PLACEMENT_3D ( 'NONE', #12426, #20497, #20596 ) ;
#20488=DIRECTION ( 'NONE',  ( 0.000000000000000000, 2.891205793294680792E-16, 1.000000000000000000 ) ) ;
#20494=CARTESIAN_POINT ( 'NONE',  ( -4.567115856812060670, 47.10047254335474065, 92.21121380123797451 ) ) ;
#20496=ORIENTED_EDGE ( 'NONE', *, *, #1045, .T. ) ;
#20497=DIRECTION ( 'NONE',  ( -1.193617070626243484E-16, -1.000000000000000000, -0.000000000000000000 ) ) ;
#20498=VERTEX_POINT ( 'NONE', #17291 ) ;
#20506=LINE ( 'NONE', #5937, #16306 ) ;
#20507=CARTESIAN_POINT ( 'NONE',  ( -0.9988176903691428077, 49.83852402762217082, 90.80496380123797451 ) ) ;
#20509=CARTESIAN_POINT ( 'NONE',  ( 3.948530577815479337, 39.69684013992245752, 94.71121380294498238 ) ) ;
#20510=EDGE_CURVE ( 'NONE', #18041, #2157, #10139, .T. ) ;
#20511=CARTESIAN_POINT ( 'NONE',  ( -0.8237052942265477018, 49.18499566818285018, 90.25808880294496817 ) ) ;
#20515=AXIS2_PLACEMENT_3D ( 'NONE', #9614, #4897, #22 ) ;
#20522=CARTESIAN_POINT ( 'NONE',  ( -7.677846259693485109, 51.36218137147968577, 93.55433879953098142 ) ) ;
#20527=CARTESIAN_POINT ( 'NONE',  ( 35.92215374030650565, 47.36218137147962892, 93.55433879953098142 ) ) ;
#20537=CARTESIAN_POINT ( 'NONE',  ( 5.611423337425062385, 41.22389019960463230, 92.67996380123798872 ) ) ;
#20542=VERTEX_POINT ( 'NONE', #6813 ) ;
#20543=DIRECTION ( 'NONE',  ( -0.7071067811865433539, 0.7071067811865517916, -0.000000000000000000 ) ) ;
#20544=CARTESIAN_POINT ( 'NONE',  ( 3.122153740306552905, 48.66551347115873227, 91.35183880294498238 ) ) ;
#20547=LINE ( 'NONE', #9074, #7432 ) ;
#20550=LINE ( 'NONE', #7891, #2272 ) ;
#20554=ORIENTED_EDGE ( 'NONE', *, *, #6375, .F. ) ;
#20557=CARTESIAN_POINT ( 'NONE',  ( -3.350035803220276609, 49.20851703305431357, 95.72683880123798872 ) ) ;
#20558=CARTESIAN_POINT ( 'NONE',  ( 3.460444912181559474, 49.25145096859824889, 95.49246380123798872 ) ) ;
#20559=DIRECTION ( 'NONE',  ( 0.000000000000000000, 0.000000000000000000, -1.000000000000000000 ) ) ;
#20563=ORIENTED_EDGE ( 'NONE', *, *, #4186, .F. ) ;
#20569=CARTESIAN_POINT ( 'NONE',  ( 5.568489401881125289, 48.03437091500646261, 95.57058880123798872 ) ) ;
#20570=CARTESIAN_POINT ( 'NONE',  ( 11.32022995165976198, 38.96218137147968008, 93.55433879953098142 ) ) ;
#20573=VERTEX_POINT ( 'NONE', #2144 ) ;
#20578=B_SPLINE_CURVE_WITH_KNOTS ( 'NONE', 3,
 ( #19290, #6104, #1432, #12711, #20775, #4603, #6211, #11124, #17594, #3021, #9528, #16012, #6306, #3131, #12807, #8021, #14507, #6409, #3232, #2057, #5235, #10051, #17908, #9734 ),
 .UNSPECIFIED., .F., .F.,
 ( 4, 2, 2, 2, 2, 2, 2, 2, 2, 2, 2, 4 ),
 ( 0.000000000000000000, 0.001360085407871233776, 0.002040128111806841556, 0.002720170815742449337, 0.004080256223613664898, 0.004760298927549273980, 0.005440341631484881327, 0.006800427039356100357, 0.007480469743291708572, 0.008160512447227315919, 0.009520597855098516735, 0.01088068326296971755 ),
 .UNSPECIFIED. ) ;
#20580=ORIENTED_EDGE ( 'NONE', *, *, #5992, .T. ) ;
#20582=CARTESIAN_POINT ( 'NONE',  ( 4.483525963726956221, 47.60918346696958281, 95.05433879953102405 ) ) ;
#20589=ORIENTED_EDGE ( 'NONE', *, *, #16355, .T. ) ;
#20592=CARTESIAN_POINT ( 'NONE',  ( 3.460444912181559474, 49.25145096859824889, 91.89871380123798872 ) ) ;
#20593=ORIENTED_EDGE ( 'NONE', *, *, #8887, .T. ) ;
#20594=ORIENTED_EDGE ( 'NONE', *, *, #8317, .T. ) ;
#20595=CARTESIAN_POINT ( 'NONE',  ( -5.368445182934975968, 51.36218137147968577, 95.05433879953098142 ) ) ;
#20596=DIRECTION ( 'NONE',  ( 1.000000000000000000, 0.000000000000000000, 0.000000000000000000 ) ) ;
#20600=DIRECTION ( 'NONE',  ( 0.4999999999999981126, -0.8660254037844397068, -0.000000000000000000 ) ) ;
#20601=VECTOR ( 'NONE', #11265, 1000.000000000000000 ) ;
#20606=CARTESIAN_POINT ( 'NONE',  ( -3.350035803220276609, 49.20851703305431357, 90.88308880123797451 ) ) ;
#20614=LINE ( 'NONE', #7754, #11545 ) ;
#20615=CARTESIAN_POINT ( 'NONE',  ( 5.722153740306500147, 44.16218137147968292, 93.33161078214054385 ) ) ;
#20617=CARTESIAN_POINT ( 'NONE',  ( 6.198496396448986090, 45.68315280215533392, 90.49246380123798872 ) ) ;
#20619=PLANE ( 'NONE',  #3790 ) ;
#20620=ORIENTED_EDGE ( 'NONE', *, *, #1930, .F. ) ;
#20621=CARTESIAN_POINT ( 'NONE',  ( 35.92215374030650565, 47.36218137147962892, 45.55433879953098852 ) ) ;
#20623=CARTESIAN_POINT ( 'NONE',  ( 32.72215374030650281, 44.16218137147968292, 87.05433879953099563 ) ) ;
#20624=CARTESIAN_POINT ( 'NONE',  ( -4.677846259692850950, 45.55551717212265572, 93.90237681315545615 ) ) ;
#20625=CARTESIAN_POINT ( 'NONE',  ( -7.677846259693485109, 51.36218137147968577, 45.55433879953098852 ) ) ;
#20628=FACE_BOUND ( 'NONE', #17414, .T. ) ;
#20635=ORIENTED_EDGE ( 'NONE', *, *, #3197, .T. ) ;
#20638=CARTESIAN_POINT ( 'NONE',  ( 3.122153740306552905, 48.66551347115873227, 90.10183880294498238 ) ) ;
#20641=CARTESIAN_POINT ( 'NONE',  ( 1.868012774839550749, 39.13936707477651566, 94.32058879953099506 ) ) ;
#20643=CARTESIAN_POINT ( 'NONE',  ( 10.77494014480653561, 42.76218137147968434, 73.80433879953100984 ) ) ;
#20649=ORIENTED_EDGE ( 'NONE', *, *, #3385, .F. ) ;
#20650=CARTESIAN_POINT ( 'NONE',  ( 2.043125170982144745, 38.48583871533720213, 93.77371380123798872 ) ) ;
#20651=CARTESIAN_POINT ( 'NONE',  ( 2.043125170982144745, 38.48583871533720213, 95.02371380123798872 ) ) ;
#20652=DIRECTION ( 'NONE',  ( 0.000000000000000000, 2.168404344970984808E-15, -1.000000000000000000 ) ) ;
#20660=CARTESIAN_POINT ( 'NONE',  ( -0.9988176903691428077, 49.83852402762217082, 93.30496380123798872 ) ) ;
#20674=CARTESIAN_POINT ( 'NONE',  ( 5.080276094035328427, 40.73314705485743303, 95.05433879953100984 ) ) ;
#20680=PLANE ( 'NONE',  #78 ) ;
#20684=ORIENTED_EDGE ( 'NONE', *, *, #10262, .T. ) ;
#20687=CARTESIAN_POINT ( 'NONE',  ( 1.352400422481993658, 50.46853102219002096, 95.57058880123798872 ) ) ;
#20705=CARTESIAN_POINT ( 'NONE',  ( 6.198496396448986090, 45.68315280215533392, 91.74246380123798872 ) ) ;
#20706=VECTOR ( 'NONE', #12302, 1000.000000000000000 ) ;
#20717=FACE_OUTER_BOUND ( 'NONE', #16202, .T. ) ;
#20718=EDGE_LOOP ( 'NONE', ( #2611, #7078, #21025, #20593 ) ) ;
#20720=( GEOMETRIC_REPRESENTATION_CONTEXT ( 3 ) GLOBAL_UNCERTAINTY_ASSIGNED_CONTEXT ( ( #17844 ) ) GLOBAL_UNIT_ASSIGNED_CONTEXT ( ( #1678, #12847, #17740 ) ) REPRESENTATION_CONTEXT ( 'NONE', 'WORKASPACE' ) );
#20730=DIRECTION ( 'NONE',  ( 0.000000000000000000, -1.000000000000000000, -2.168404344970984808E-15 ) ) ;
#20739=LINE ( 'NONE', #1190, #20046 ) ;
#20740=CARTESIAN_POINT ( 'NONE',  ( 6.102441102155617969, 43.42752260303680600, 89.86746380294499659 ) ) ;
#20741=ORIENTED_EDGE ( 'NONE', *, *, #10377, .T. ) ;
#20744=CARTESIAN_POINT ( 'NONE',  ( 3.948530577815479337, 39.69684013992245752, 94.39871379953099506 ) ) ;
#20746=CARTESIAN_POINT ( 'NONE',  ( 11.22215374030650281, 42.76218137147968434, 77.40433879953098995 ) ) ;
#20753=CARTESIAN_POINT ( 'NONE',  ( 6.828503391016846891, 43.33193468930419101, 94.00808880123798872 ) ) ;
#20760=ORIENTED_EDGE ( 'NONE', *, *, #10656, .F. ) ;
#20765=CARTESIAN_POINT ( 'NONE',  ( 4.001624342216747010, 40.29782057951908314, 90.66473080991372058 ) ) ;
#20766=LINE ( 'NONE', #4497, #1684 ) ;
#20775=CARTESIAN_POINT ( 'NONE',  ( -4.337338579526520910, 46.33133051644502132, 92.55433879953099563 ) ) ;
#20776=CARTESIAN_POINT ( 'NONE',  ( 5.611423337425062385, 41.22389019960463230, 92.83621380123797451 ) ) ;
#20786=LINE ( 'NONE', #14310, #5405 ) ;
#20794=ORIENTED_EDGE ( 'NONE', *, *, #15109, .T. ) ;
#20796=LINE ( 'NONE', #1343, #12246 ) ;
#20799=DIRECTION ( 'NONE',  ( -0.000000000000000000, -0.000000000000000000, 1.000000000000000000 ) ) ;
#20807=ORIENTED_EDGE ( 'NONE', *, *, #8726, .F. ) ;
#20812=LINE ( 'NONE', #17942, #13135 ) ;
#20815=CARTESIAN_POINT ( 'NONE',  ( 1.352400422481993658, 50.46853102219002096, 93.22683880123798872 ) ) ;
#20823=CARTESIAN_POINT ( 'NONE',  ( 31.22215374030650281, 42.76218137147968434, 78.80433879953099563 ) ) ;
#20828=ORIENTED_EDGE ( 'NONE', *, *, #8390, .F. ) ;
#20838=FACE_OUTER_BOUND ( 'NONE', #6727, .T. ) ;
#20847=CARTESIAN_POINT ( 'NONE',  ( -4.500660556396669065, 42.81632233694663370, 90.57058880294496817 ) ) ;
#20855=CARTESIAN_POINT ( 'NONE',  ( 31.22215374030650281, 42.96218137147968008, 77.80433879953099563 ) ) ;
#20858=DIRECTION ( 'NONE',  ( 1.000000000000000000, -0.000000000000000000, -0.000000000000000000 ) ) ;
#20864=ORIENTED_EDGE ( 'NONE', *, *, #1337, .F. ) ;
#20866=CARTESIAN_POINT ( 'NONE',  ( -4.524181921268124462, 40.28999182795290324, 94.94558880123797451 ) ) ;
#20870=LINE ( 'NONE', #17282, #8250 ) ;
#20872=CARTESIAN_POINT ( 'NONE',  ( -1.218186307993342599, 38.53589529967370453, 95.05433879953095300 ) ) ;
#20873=EDGE_CURVE ( 'NONE', #2188, #7787, #6681, .T. ) ;
#20875=ORIENTED_EDGE ( 'NONE', *, *, #8807, .F. ) ;
#20877=CARTESIAN_POINT ( 'NONE',  ( 31.07218010054375412, 42.96218137147968008, 66.20574467885104752 ) ) ;
#20880=CARTESIAN_POINT ( 'NONE',  ( 5.420351613492021770, 41.31768866812478080, 95.05433879953098142 ) ) ;
#20884=CARTESIAN_POINT ( 'NONE',  ( 11.22215374030649926, 48.36218137147968577, 80.55433879953099563 ) ) ;
#20888=ORIENTED_EDGE ( 'NONE', *, *, #8534, .F. ) ;
#20892=EDGE_CURVE ( 'NONE', #5204, #899, #13493, .T. ) ;
#20896=CARTESIAN_POINT ( 'NONE',  ( 5.611423337425062385, 41.22389019960463230, 94.08621380123797451 ) ) ;
#20900=CARTESIAN_POINT ( 'NONE',  ( 4.987494971863720927, 47.58855820898865829, 93.46121379953098085 ) ) ;
#20901=VERTEX_POINT ( 'NONE', #15201 ) ;
#20910=CARTESIAN_POINT ( 'NONE',  ( 1.352400422481993658, 50.46853102219002096, 91.97683880123797451 ) ) ;
#20912=CARTESIAN_POINT ( 'NONE',  ( 4.987494971863720927, 47.58855820898865829, 90.02371380294498238 ) ) ;
#20918=DIRECTION ( 'NONE',  ( -1.402518428993831676E-16, 1.000000000000000000, 0.000000000000000000 ) ) ;
#20921=VERTEX_POINT ( 'NONE', #19967 ) ;
#20923=EDGE_CURVE ( 'NONE', #8675, #8877, #16590, .T. ) ;
#20926=ADVANCED_FACE ( 'NONE', ( #13600 ), #2010, .F. ) ;
#20932=CARTESIAN_POINT ( 'NONE',  ( -1.219056181836354558, 49.77488197367695477, 94.40612966814926210 ) ) ;
#20935=ADVANCED_FACE ( 'NONE', ( #18280 ), #13400, .F. ) ;
#20936=AXIS2_PLACEMENT_3D ( 'NONE', #15365, #17163, #2585 ) ;
#20953=ORIENTED_EDGE ( 'NONE', *, *, #6660, .F. ) ;
#20954=CARTESIAN_POINT ( 'NONE',  ( -2.416137431568557314, 39.07291177436112406, 94.86746380123797451 ) ) ;
#20956=CARTESIAN_POINT ( 'NONE',  ( 2.043125170982144745, 38.48583871533720213, 92.52371380123798872 ) ) ;
#20965=CARTESIAN_POINT ( 'NONE',  ( -0.3080929418689875576, 37.85583172076933778, 91.35183880123798872 ) ) ;
#20966=CARTESIAN_POINT ( 'NONE',  ( 2.043125170982144745, 38.48583871533720213, 95.02371380123798872 ) ) ;
#20967=EDGE_LOOP ( 'NONE', ( #20030, #12152 ) ) ;
#20971=CARTESIAN_POINT ( 'NONE',  ( 5.504730982882359847, 46.12534449621361432, 92.55433879953100984 ) ) ;
#20984=DIRECTION ( 'NONE',  ( -1.000000000000000000, -5.084437235940625660E-16, 0.000000000000000000 ) ) ;
#20989=EDGE_CURVE ( 'NONE', #1059, #15210, #2751, .T. ) ;
#20992=LINE ( 'NONE', #19110, #5779 ) ;
#20999=CARTESIAN_POINT ( 'NONE',  ( -3.777846259693486974, 51.36218137147968577, 93.55433879953098142 ) ) ;
#21001=CARTESIAN_POINT ( 'NONE',  ( -4.500660556396669065, 42.81632233694663370, 95.25808879953098085 ) ) ;
#21006=EDGE_CURVE ( 'NONE', #16680, #9248, #8368, .T. ) ;
#21007=AXIS2_PLACEMENT_3D ( 'NONE', #17997, #19580, #9402 ) ;
#21013=CARTESIAN_POINT ( 'NONE',  ( 2.043125170982144745, 38.48583871533720213, 92.52371380123798872 ) ) ;
#21025=ORIENTED_EDGE ( 'NONE', *, *, #14769, .F. ) ;
ENDSEC;
END-ISO-10303-21;
